ISO-10303-21;
HEADER;
FILE_DESCRIPTION (('STEP AP214'),
    '1' );
FILE_NAME ('11. Strainer.step',
    '2026-10-09T14:04:53',
    ( '' ),
    ( '' ),
    'SwSTEP 2.0',
    'SolidWorks 2021',
    '' );
FILE_SCHEMA (( 'AUTOMOTIVE_DESIGN' ));
ENDSEC;

DATA;
#2=B_SPLINE_CURVE_WITH_KNOTS ( 'NONE', 3,
 ( #85581, #66854, #35995, #58769, #77476, #471, #16702, #68867, #91667, #3588, #33983, #17781, #27909, #60775, #99743, #44042, #16163, #93663, #90059, #52119 ),
 .UNSPECIFIED., .F., .F.,
 ( 4, 2, 2, 2, 2, 2, 2, 2, 2, 4 ),
 ( 0.007078851032209184692, 0.007582385810731511952, 0.008085920589253840080, 0.008337687978515005011, 0.008589455367776168207, 0.009092990146298498069, 0.009596524924820827931, 0.01010005970334315779, 0.01060359448186548766, 0.01110712926038781752 ),
 .UNSPECIFIED. ) ;
#4=CARTESIAN_POINT ( 'NONE',  ( -5.124871413311637092, 52.11721697291532251, 6.039328222380278888 ) ) ;
#10=CARTESIAN_POINT ( 'NONE',  ( 28.43265695612079114, 17.35407036237645073, -40.99228818889015002 ) ) ;
#16=B_SPLINE_CURVE_WITH_KNOTS ( 'NONE', 3,
 ( #64877, #39563, #87576, #48148, #14717, #38505, #13662, #30413, #7160, #64366, #23384, #79992, #104270, #5579, #72952, #15794, #23929, #97239, #56222, #73482, #72438, #47616 ),
 .UNSPECIFIED., .F., .F.,
 ( 4, 2, 2, 2, 2, 2, 2, 2, 2, 2, 4 ),
 ( 0.007103997321553806935, 0.007607990259598500921, 0.008111983197643194907, 0.008363979666665547971, 0.008615976135687899301, 0.009119969073732612369, 0.009371965542754968903, 0.009623962011777323702, 0.01012795494982202810, 0.01063194788786673249, 0.01113594082591143689 ),
 .UNSPECIFIED. ) ;
#22=CARTESIAN_POINT ( 'NONE',  ( 1.380949872273418154E-15, 45.89575828009193259, -11.27631144943088337 ) ) ;
#56=CARTESIAN_POINT ( 'NONE',  ( 5.290067270632322405, 53.47475093287481940, 8.531152949374478212 ) ) ;
#58=CARTESIAN_POINT ( 'NONE',  ( -23.84378987347019674, 27.93349636785021772, 30.86234801138808947 ) ) ;
#68=VECTOR ( 'NONE', #490, 1000.000000000000000 ) ;
#74=CARTESIAN_POINT ( 'NONE',  ( -49.27082696441096488, 7.795205586015203636, -15.75806003941715083 ) ) ;
#93=CARTESIAN_POINT ( 'NONE',  ( -22.66566284726399516, 27.53292244466712546, -33.08065323819745629 ) ) ;
#101=VERTEX_POINT ( 'NONE', #42239 ) ;
#104=( LENGTH_UNIT ( ) NAMED_UNIT ( * ) SI_UNIT ( .MILLI., .METRE. ) );
#106=CARTESIAN_POINT ( 'NONE',  ( 2.607260012660386551E-19, 12.91535575337012354, -51.75000000000000711 ) ) ;
#110=CARTESIAN_POINT ( 'NONE',  ( 11.27248856952046729, 45.76231435389448876, 13.37350896801524058 ) ) ;
#111=FILL_AREA_STYLE_COLOUR ( '', #88260 ) ;
#119=EDGE_CURVE ( 'NONE', #62895, #77549, #30853, .T. ) ;
#120=CARTESIAN_POINT ( 'NONE',  ( 2.985641311035224431E-22, 35.08181111624585213, -27.25000000000000000 ) ) ;
#127=CARTESIAN_POINT ( 'NONE',  ( 48.59958381656775117, 10.21806572665720658, 14.48686862603841519 ) ) ;
#128=ORIENTED_EDGE ( 'NONE', *, *, #62777, .F. ) ;
#137=EDGE_LOOP ( 'NONE', ( #79684, #47625 ) ) ;
#145=CARTESIAN_POINT ( 'NONE',  ( 37.24841108779522614, 25.58895219176176283, 13.42546066398215210 ) ) ;
#153=ORIENTED_EDGE ( 'NONE', *, *, #75458, .T. ) ;
#174=ORIENTED_EDGE ( 'NONE', *, *, #30556, .F. ) ;
#177=EDGE_LOOP ( 'NONE', ( #37832, #56366 ) ) ;
#209=STYLED_ITEM ( 'NONE', ( #32664 ), #50486 ) ;
#210=ADVANCED_FACE ( 'NONE', ( #73405 ), #48071, .F. ) ;
#211=CARTESIAN_POINT ( 'NONE',  ( 48.02835407290503866, 11.61227450977245468, -14.35535821593549954 ) ) ;
#216=CARTESIAN_POINT ( 'NONE',  ( 1.013561713383841045, 53.56087209037478658, 9.749829111538236504 ) ) ;
#217=FACE_OUTER_BOUND ( 'NONE', #93796, .T. ) ;
#225=CARTESIAN_POINT ( 'NONE',  ( -9.957476778176042487, 44.05467513874048535, 12.94893335343420482 ) ) ;
#237=EDGE_LOOP ( 'NONE', ( #11496, #69196 ) ) ;
#239=CARTESIAN_POINT ( 'NONE',  ( 5.290067270632322405, -1.200000000000000030E-05, 8.531152949374478212 ) ) ;
#241=CARTESIAN_POINT ( 'NONE',  ( 6.529018613599237852, 51.53955942784660493, -6.914392934962513948 ) ) ;
#265=LINE ( 'NONE', #48842, #82040 ) ;
#270=CARTESIAN_POINT ( 'NONE',  ( 30.42269336643044397, 12.90989212739758685, 41.86604079465131889 ) ) ;
#295=CARTESIAN_POINT ( 'NONE',  ( 0.000000000000000000, 55.00000000000000000, 0.000000000000000000 ) ) ;
#301=CARTESIAN_POINT ( 'NONE',  ( 9.045746190732545600, 45.90313006749667579, 14.51680462862703891 ) ) ;
#315=CARTESIAN_POINT ( 'NONE',  ( 1.218045234088034112, 53.93925255856578360, -8.677002990697831208 ) ) ;
#320=PRESENTATION_STYLE_ASSIGNMENT (( #72655 ) ) ;
#328=EDGE_LOOP ( 'NONE', ( #41587, #87018 ) ) ;
#344=FILL_AREA_STYLE ('',( #10074 ) ) ;
#347=VERTEX_POINT ( 'NONE', #103552 ) ;
#350=LINE ( 'NONE', #100679, #26605 ) ;
#353=CARTESIAN_POINT ( 'NONE',  ( 5.581309233574441675E-23, 43.17555810750860701, -18.75000000000000355 ) ) ;
#356=CARTESIAN_POINT ( 'NONE',  ( -28.08625202345140792, 34.36930134029169892, -8.015757243435880142 ) ) ;
#383=CARTESIAN_POINT ( 'NONE',  ( 28.58272191126957651, 16.23375075743845031, 41.45992959583530535 ) ) ;
#390=CARTESIAN_POINT ( 'NONE',  ( -29.68315524076956535, 13.47185074185901499, 42.10535821593508388 ) ) ;
#393=CARTESIAN_POINT ( 'NONE',  ( -22.13658770490400229, 25.65638329602028733, 32.60403273639936117 ) ) ;
#397=EDGE_LOOP ( 'NONE', ( #26477, #74616, #27189, #53326 ) ) ;
#407=CARTESIAN_POINT ( 'NONE',  ( -26.78494459259576033, 34.86751637306745977, 7.587752381711101890 ) ) ;
#416=CARTESIAN_POINT ( 'NONE',  ( -16.80263806300990481, 45.55013935554968185, 6.657797401561873940 ) ) ;
#424=CARTESIAN_POINT ( 'NONE',  ( 9.810831326706606959, 53.41083018302243346, 2.841840335636323989 ) ) ;
#427=CARTESIAN_POINT ( 'NONE',  ( 16.48303619537878006, 45.94111582078985379, -4.157797401561770911 ) ) ;
#432=CARTESIAN_POINT ( 'NONE',  ( -30.55667715332060297, 16.37467338430767683, 39.95293003182839442 ) ) ;
#445=CARTESIAN_POINT ( 'NONE',  ( -16.96103378808793138, 43.64123910865905032, 4.188553803742784076 ) ) ;
#462=CARTESIAN_POINT ( 'NONE',  ( 9.781067317119404692, 51.26646010159761602, 3.095465610852687899 ) ) ;
#471=CARTESIAN_POINT ( 'NONE',  ( -17.58486903827841275, 43.20934354716421666, -6.234446319141409454 ) ) ;
#486=CARTESIAN_POINT ( 'NONE',  ( -38.18724015216890422, 25.28177589261053271, -13.30327295121670694 ) ) ;
#490=DIRECTION ( 'NONE',  ( -0.000000000000000000, 1.000000000000000000, -0.000000000000000000 ) ) ;
#492=VERTEX_POINT ( 'NONE', #52334 ) ;
#517=ORIENTED_EDGE ( 'NONE', *, *, #1884, .T. ) ;
#520=CARTESIAN_POINT ( 'NONE',  ( 24.46397269780010930, 25.31587970897912854, 32.08082341745669908 ) ) ;
#523=CARTESIAN_POINT ( 'NONE',  ( 4.964745198532805048, 53.54848248096784147, 8.490843834923378353 ) ) ;
#546=CARTESIAN_POINT ( 'NONE',  ( -27.10511071441183262, -1.200000000000000030E-05, 8.806984339686158236 ) ) ;
#547=ORIENTED_EDGE ( 'NONE', *, *, #27451, .T. ) ;
#556=CARTESIAN_POINT ( 'NONE',  ( -16.75187969033554936, 36.38380281757302015, -24.30698433968596106 ) ) ;
#571=B_SPLINE_CURVE_WITH_KNOTS ( 'NONE', 3,
 ( #27752, #101054, #45501, #20192, #77850, #78371, #12039, #68714, #35290, #43357, #53047, #20734, #85965, #84350, #76242, #36896, #68159, #52494, #69762, #44423 ),
 .UNSPECIFIED., .F., .F.,
 ( 4, 2, 2, 2, 2, 2, 2, 2, 2, 4 ),
 ( 0.003055152949284218288, 0.003559479741444611378, 0.003811643137524814429, 0.004063806533605017479, 0.004568133325765439193, 0.005072460117925860039, 0.006081113702246704333, 0.006585440494407136455, 0.006837603890487358588, 0.007089767286567579853 ),
 .UNSPECIFIED. ) ;
#579=CARTESIAN_POINT ( 'NONE',  ( 16.80323065652739345, 43.42158355246869661, -6.657797401561860617 ) ) ;
#599=CARTESIAN_POINT ( 'NONE',  ( 15.50560966020076847, 37.05331456527881784, 22.93063681418749766 ) ) ;
#604=CARTESIAN_POINT ( 'NONE',  ( 16.72321626032220721, 45.57697876764353140, 6.657797401561558637 ) ) ;
#610=SURFACE_SIDE_STYLE ('',( #91280 ) ) ;
#622=FACE_OUTER_BOUND ( 'NONE', #19692, .T. ) ;
#629=CARTESIAN_POINT ( 'NONE',  ( -46.86921974295896121, 18.15560460139520416, 16.08157171274191199 ) ) ;
#642=EDGE_CURVE ( 'NONE', #44079, #54759, #31287, .T. ) ;
#643=CARTESIAN_POINT ( 'NONE',  ( 0.5678805982759365101, 35.03118002593645741, -27.38332561059753090 ) ) ;
#645=CARTESIAN_POINT ( 'NONE',  ( 55.00000000000000000, 2.000000000000000000, 0.000000000000000000 ) ) ;
#652=CARTESIAN_POINT ( 'NONE',  ( 49.26018567526338643, 7.766323692793287492, 15.83099189872057622 ) ) ;
#653=VERTEX_POINT ( 'NONE', #24257 ) ;
#654=CARTESIAN_POINT ( 'NONE',  ( 0.6456527140175527535, 44.02049913527396541, 16.41655882843762981 ) ) ;
#684=CARTESIAN_POINT ( 'NONE',  ( -15.72023223728087693, 43.84211828279115508, 6.254247239864763941 ) ) ;
#698=FACE_BOUND ( 'NONE', #50405, .T. ) ;
#700=CARTESIAN_POINT ( 'NONE',  ( -29.68315524076956891, -1.200000000000000030E-05, 40.85535821593508388 ) ) ;
#705=DIRECTION ( 'NONE',  ( 0.000000000000000000, 0.000000000000000000, 1.000000000000000000 ) ) ;
#709=( LENGTH_UNIT ( ) NAMED_UNIT ( * ) SI_UNIT ( .MILLI., .METRE. ) );
#710=EDGE_CURVE ( 'NONE', #67680, #74647, #10178, .T. ) ;
#716=CARTESIAN_POINT ( 'NONE',  ( -5.290067270632269114, 51.34639538792298907, -8.531152949374520844 ) ) ;
#729=CARTESIAN_POINT ( 'NONE',  ( 0.6415787021996353090, 46.14597056523812313, 16.42407206998221980 ) ) ;
#733=CARTESIAN_POINT ( 'NONE',  ( -11.54075930460758670, 45.44590361214168439, -14.27956357151539102 ) ) ;
#738=CARTESIAN_POINT ( 'NONE',  ( -47.24255575150520059, 16.92138162734892148, -16.58509488952817179 ) ) ;
#741=VERTEX_POINT ( 'NONE', #18284 ) ;
#749=DIRECTION ( 'NONE',  ( 0.000000000000000000, 0.000000000000000000, 1.000000000000000000 ) ) ;
#751=CARTESIAN_POINT ( 'NONE',  ( 29.77184624873680718, 12.99572234387825276, 39.60535821593452255 ) ) ;
#754=CARTESIAN_POINT ( 'NONE',  ( 5.911454136186996777, 51.88613318027746857, 6.184812069074881791 ) ) ;
#768=CARTESIAN_POINT ( 'NONE',  ( 5.290067270632160756, 52.08006895350504806, -6.031152949374595451 ) ) ;
#828=FACE_OUTER_BOUND ( 'NONE', #105672, .T. ) ;
#832=CARTESIAN_POINT ( 'NONE',  ( 9.067083174484489305, 46.09712060844260151, 13.87005886985717673 ) ) ;
#845=ORIENTED_EDGE ( 'NONE', *, *, #101069, .T. ) ;
#870=DIRECTION ( 'NONE',  ( 0.000000000000000000, 1.000000000000000000, 0.000000000000000000 ) ) ;
#890=FACE_OUTER_BOUND ( 'NONE', #71798, .T. ) ;
#894=UNCERTAINTY_MEASURE_WITH_UNIT (LENGTH_MEASURE( 1.000000000000000082E-05 ), #12427, 'distance_accuracy_value', 'NONE');
#907=CARTESIAN_POINT ( 'NONE',  ( 15.98683276757948235, 34.48651532721294188, -24.05821932099534521 ) ) ;
#929=ADVANCED_FACE ( 'NONE', ( #69999, #102900, #43595, #61934, #36611 ), #42767, .F. ) ;
#930=DIRECTION ( 'NONE',  ( 0.000000000000000000, 0.000000000000000000, 1.000000000000000000 ) ) ;
#935=FILL_AREA_STYLE ('',( #31397 ) ) ;
#937=CARTESIAN_POINT ( 'NONE',  ( -26.11140572328752540, 35.05551467058084114, 8.044021159044859814 ) ) ;
#949=CARTESIAN_POINT ( 'NONE',  ( 16.75187969033571989, -1.200000000000000030E-05, 23.05698433968582961 ) ) ;
#951=ORIENTED_EDGE ( 'NONE', *, *, #67576, .F. ) ;
#959=CARTESIAN_POINT ( 'NONE',  ( 15.39894322001505955, 46.20524723896237163, -5.264004132386357782 ) ) ;
#976=CARTESIAN_POINT ( 'NONE',  ( -17.39377970932413220, 34.16992860090641670, -24.14261105171526012 ) ) ;
#978=CARTESIAN_POINT ( 'NONE',  ( 49.26518742571373366, 13.24133944402177399, 15.39083778843029648 ) ) ;
#981=STYLED_ITEM ( 'NONE', ( #5135 ), #100114 ) ;
#994=CARTESIAN_POINT ( 'NONE',  ( 8.718468385534640319, 51.50404178009831924, 4.031152949374445349 ) ) ;
#1002=CARTESIAN_POINT ( 'NONE',  ( -3.381870600466846067E-15, 46.21383923812598482, -16.24999999999995026 ) ) ;
#1068=CARTESIAN_POINT ( 'NONE',  ( -5.207264114973761515, 51.36227786629242331, 8.531152949374574135 ) ) ;
#1074=DIRECTION ( 'NONE',  ( 0.000000000000000000, 1.000000000000000000, -0.000000000000000000 ) ) ;
#1086=EDGE_CURVE ( 'NONE', #79581, #6418, #65173, .T. ) ;
#1098=CARTESIAN_POINT ( 'NONE',  ( -0.08431525725544751493, 53.39766064372322774, 10.24999999999997335 ) ) ;
#1128=CARTESIAN_POINT ( 'NONE',  ( -23.61948937802356951, 28.00997096501932759, 30.76980700055176499 ) ) ;
#1142=CARTESIAN_POINT ( 'NONE',  ( -48.02835407290533709, 9.771516447483559631, -16.85535821593460426 ) ) ;
#1147=CARTESIAN_POINT ( 'NONE',  ( 16.96000587140905225, 45.76999459631175426, 4.188133835394149074 ) ) ;
#1164=ORIENTED_EDGE ( 'NONE', *, *, #63234, .T. ) ;
#1168=DIRECTION ( 'NONE',  ( 0.000000000000000000, 0.000000000000000000, 1.000000000000000000 ) ) ;
#1170=CARTESIAN_POINT ( 'NONE',  ( -0.6177861184392186011, 18.48477677756791593, -49.40942936560928445 ) ) ;
#1177=ORIENTED_EDGE ( 'NONE', *, *, #63865, .F. ) ;
#1180=CARTESIAN_POINT ( 'NONE',  ( 6.898406705472277429E-15, 1.999999999999998224, 56.32976553137783782 ) ) ;
#1184=CARTESIAN_POINT ( 'NONE',  ( 0.3379004368769049083, 35.06844978857020578, -27.28504174633816959 ) ) ;
#1190=B_SPLINE_CURVE_WITH_KNOTS ( 'NONE', 3,
 ( #28714, #11947, #21678, #87456, #13537, #46453, #79342, #5462, #12470, #38385, #44333, #71247, #104145, #61596, #30288, #19573, #11408, #77227, #94491, #3342 ),
 .UNSPECIFIED., .F., .F.,
 ( 4, 2, 2, 2, 2, 2, 2, 2, 2, 4 ),
 ( 0.001455504135240683061, 0.001707392234674408663, 0.001959280334108134264, 0.002463056532975591104, 0.002966832731843047945, 0.003470608930710504785, 0.003974385129577961626, 0.004478161328445418032, 0.004981937527312874439, 0.005485713726180331713 ),
 .UNSPECIFIED. ) ;
#1207=CARTESIAN_POINT ( 'NONE',  ( 0.000000000000000000, -945.0000000000000000, 0.000000000000000000 ) ) ;
#1208=FACE_OUTER_BOUND ( 'NONE', #105262, .T. ) ;
#1211=CARTESIAN_POINT ( 'NONE',  ( 9.500496464815300968, 44.08937475915367088, -13.17128768611811296 ) ) ;
#1229=CARTESIAN_POINT ( 'NONE',  ( -22.10841373170487856, 28.16423242622105860, 31.35595207099942172 ) ) ;
#1248=CARTESIAN_POINT ( 'NONE',  ( -48.28140683493110430, 14.38570471689504338, 16.83761797438776142 ) ) ;
#1263=ADVANCED_FACE ( 'NONE', ( #66145 ), #27342, .F. ) ;
#1265=ORIENTED_EDGE ( 'NONE', *, *, #91724, .F. ) ;
#1272=( GEOMETRIC_REPRESENTATION_CONTEXT ( 3 ) GLOBAL_UNCERTAINTY_ASSIGNED_CONTEXT ( ( #22151 ) ) GLOBAL_UNIT_ASSIGNED_CONTEXT ( ( #20564, #2162, #100342 ) ) REPRESENTATION_CONTEXT ( 'NONE', 'WORKASPACE' ) );
#1273=COLOUR_RGB ( '', 0.40784314, 0.44705882, 0.49803922) ;
#1276=CARTESIAN_POINT ( 'NONE',  ( 0.2960973004666590525, 12.99320615743570251, -51.71653671273871566 ) ) ;
#1279=CARTESIAN_POINT ( 'NONE',  ( 22.57772903360667982, 26.07719920855362972, -30.87900892229609440 ) ) ;
#1286=ORIENTED_EDGE ( 'NONE', *, *, #100714, .F. ) ;
#1302=MECHANICAL_DESIGN_GEOMETRIC_PRESENTATION_REPRESENTATION('',(#87494),#101275);
#1326=SURFACE_SIDE_STYLE ('',( #75229 ) ) ;
#1332=EDGE_CURVE ( 'NONE', #15839, #4914, #2467, .T. ) ;
#1345=PRESENTATION_STYLE_ASSIGNMENT (( #91460 ) ) ;
#1347=STYLED_ITEM ( 'NONE', ( #52437 ), #59058 ) ;
#1350=CARTESIAN_POINT ( 'NONE',  ( 5.930156825389887310, 53.39845306454675011, 8.358120849896316429 ) ) ;
#1353=CARTESIAN_POINT ( 'NONE',  ( 30.10055902053774801, 13.03130292445773719, 42.03558690210214621 ) ) ;
#1356=( NAMED_UNIT ( * ) SI_UNIT ( $, .STERADIAN. ) SOLID_ANGLE_UNIT ( ) );
#1360=ORIENTED_EDGE ( 'NONE', *, *, #58649, .F. ) ;
#1394=CARTESIAN_POINT ( 'NONE',  ( 16.64348903516524203, 43.75610143575153188, 4.157797401561407646 ) ) ;
#1399=UNCERTAINTY_MEASURE_WITH_UNIT (LENGTH_MEASURE( 1.000000000000000082E-05 ), #35187, 'distance_accuracy_value', 'NONE');
#1408=ORIENTED_EDGE ( 'NONE', *, *, #104014, .T. ) ;
#1409=CARTESIAN_POINT ( 'NONE',  ( -16.58616928888070419, 36.42044334926446680, -24.29863715439297067 ) ) ;
#1414=CARTESIAN_POINT ( 'NONE',  ( 46.97231841192020596, 12.59348177918415956, 16.28806988207259110 ) ) ;
#1425=DIRECTION ( 'NONE',  ( -0.000000000000000000, -1.000000000000000000, -0.000000000000000000 ) ) ;
#1448=SHAPE_REPRESENTATION_RELATIONSHIP ( 'NONE' , 'NONE' ,  #38413, #89702 ) ;
#1450=CARTESIAN_POINT ( 'NONE',  ( 7.321407651878572231, 54.25251164017154082, -2.971923534686649049 ) ) ;
#1456=AXIS2_PLACEMENT_3D ( 'NONE', #15897, #40696, #88208 ) ;
#1461=CARTESIAN_POINT ( 'NONE',  ( 17.07643158642794390, 37.03581886162301373, -21.84712036628289056 ) ) ;
#1466=CARTESIAN_POINT ( 'NONE',  ( 15.52523732965139125, 34.97072044547751091, -22.76566327259062206 ) ) ;
#1475=EDGE_CURVE ( 'NONE', #36646, #93186, #88516, .T. ) ;
#1477=CARTESIAN_POINT ( 'NONE',  ( -29.68315524076957246, 18.29184282782463455, 39.60535821593508388 ) ) ;
#1491=CARTESIAN_POINT ( 'NONE',  ( 0.000000000000000000, 0.000000000000000000, 0.000000000000000000 ) ) ;
#1496=CARTESIAN_POINT ( 'NONE',  ( -26.34287197489002352, 35.00042356184812320, 7.802188285690729863 ) ) ;
#1511=CARTESIAN_POINT ( 'NONE',  ( 9.768787396428281866, 53.46522389469076586, 2.424760876876827176 ) ) ;
#1513=CARTESIAN_POINT ( 'NONE',  ( 15.39205472978306233, 46.19766366449148620, -5.347876573122199773 ) ) ;
#1518=CARTESIAN_POINT ( 'NONE',  ( -30.77329953031004450, 15.53171713056513603, 40.23250653748785766 ) ) ;
#1534=STYLED_ITEM ( 'NONE', ( #23767 ), #12836 ) ;
#1536=CARTESIAN_POINT ( 'NONE',  ( 49.03408319953887684, 14.13974658789363836, 14.85990013744586591 ) ) ;
#1537=CARTESIAN_POINT ( 'NONE',  ( -5.371856143885752388, 52.06043921290445553, -6.031152949374585681 ) ) ;
#1558=CARTESIAN_POINT ( 'NONE',  ( -0.1681987345962790426, 45.30391365246044444, -18.75000000000000355 ) ) ;
#1562=EDGE_CURVE ( 'NONE', #68982, #59035, #69233, .T. ) ;
#1569=CARTESIAN_POINT ( 'NONE',  ( 0.8394321637725764562, 37.08900195433652414, 27.57017630837880517 ) ) ;
#1573=CARTESIAN_POINT ( 'NONE',  ( -38.56699491466429208, 25.18982931514603507, -12.97440760532226456 ) ) ;
#1580=CARTESIAN_POINT ( 'NONE',  ( 16.02905770043921763, 43.70337463170952930, -6.507967097231396103 ) ) ;
#1611=ADVANCED_FACE ( 'NONE', ( #43741 ), #18978, .F. ) ;
#1621=CARTESIAN_POINT ( 'NONE',  ( 30.93163070004071358, 9.246556120444319404, -40.70059110212535103 ) ) ;
#1635=( NAMED_UNIT ( * ) SI_UNIT ( $, .STERADIAN. ) SOLID_ANGLE_UNIT ( ) );
#1638=VERTEX_POINT ( 'NONE', #16817 ) ;
#1639=DIRECTION ( 'NONE',  ( -0.000000000000000000, 1.000000000000000000, -0.000000000000000000 ) ) ;
#1647=CARTESIAN_POINT ( 'NONE',  ( -1.102159017229340288, 53.60731710284914442, 9.611294474598382820 ) ) ;
#1668=CARTESIAN_POINT ( 'NONE',  ( 36.44054363913070205, 26.07465808859272371, -11.65710653164109445 ) ) ;
#1670=FACE_OUTER_BOUND ( 'NONE', #60073, .T. ) ;
#1671=DIRECTION ( 'NONE',  ( 0.000000000000000000, 0.000000000000000000, 1.000000000000000000 ) ) ;
#1676=CARTESIAN_POINT ( 'NONE',  ( -9.647567108638854805, 44.08445422138064629, -13.07998335409894253 ) ) ;
#1677=EDGE_CURVE ( 'NONE', #46768, #83885, #76100, .T. ) ;
#1678=FILL_AREA_STYLE ('',( #40557 ) ) ;
#1682=AXIS2_PLACEMENT_3D ( 'NONE', #84062, #77570, #2597 ) ;
#1699=CARTESIAN_POINT ( 'NONE',  ( 17.88790647107491694, 45.31130133375065583, 5.552611910812898621 ) ) ;
#1703=COLOUR_RGB ( '', 0.66274510, 0.83137255, 0.94901961) ;
#1718=UNCERTAINTY_MEASURE_WITH_UNIT (LENGTH_MEASURE( 1.000000000000000082E-05 ), #26069, 'distance_accuracy_value', 'NONE');
#1726=CARTESIAN_POINT ( 'NONE',  ( -0.07733840395782722033, 18.87382441218279894, -49.24999999999998579 ) ) ;
#1743=VERTEX_POINT ( 'NONE', #86357 ) ;
#1744=CARTESIAN_POINT ( 'NONE',  ( 2.848917157793759055E-13, 44.08548369317517768, 16.24999999999732836 ) ) ;
#1754=CARTESIAN_POINT ( 'NONE',  ( -1.168005587324537631, 9.591777280503173131, -50.96219972952603428 ) ) ;
#1758=CARTESIAN_POINT ( 'NONE',  ( 9.658290426964626363, 43.42980812226979026, -15.25060361923008045 ) ) ;
#1763=PRESENTATION_STYLE_ASSIGNMENT (( #102066 ) ) ;
#1770=B_SPLINE_CURVE_WITH_KNOTS ( 'NONE', 3,
 ( #61089, #13033, #85908, #11982, #45960, #78842, #70760, #103656, #29805, #3376, #36841, #69708, #102601, #28753, #76715, #93458, #19606, #61636, #62681, #2826, #19070, #35782, #94527, #68660 ),
 .UNSPECIFIED., .F., .F.,
 ( 4, 2, 2, 2, 2, 2, 2, 2, 2, 2, 2, 4 ),
 ( 0.004982501964703170937, 0.005234564667989256501, 0.005486627371275342065, 0.005990752777847506254, 0.006494878184419670443, 0.006999003590991834632, 0.007251066294277914992, 0.007503128997563995352, 0.008007254404136160408, 0.008511379810708322863, 0.008763442513994400621, 0.009015505217280478378 ),
 .UNSPECIFIED. ) ;
#1774=CARTESIAN_POINT ( 'NONE',  ( 28.08444336946503483, 36.49846905662621310, -8.013953787025748454 ) ) ;
#1790=FACE_OUTER_BOUND ( 'NONE', #50901, .T. ) ;
#1805=COLOUR_RGB ( '', 0.09019608, 0.27058824, 0.51372549) ;
#1808=CARTESIAN_POINT ( 'NONE',  ( -0.8435576335715310181, 13.67164987635283246, 51.42579297825043483 ) ) ;
#1817=CARTESIAN_POINT ( 'NONE',  ( 1.160281544699517831, 17.00865987995647544, -50.01912393708035154 ) ) ;
#1842=ORIENTED_EDGE ( 'NONE', *, *, #18459, .F. ) ;
#1844=CYLINDRICAL_SURFACE ( 'NONE', #52417, 1.250000000000000222 ) ;
#1845=CARTESIAN_POINT ( 'NONE',  ( 5.290067270632321517, 52.08006895350504095, 6.031152949374479100 ) ) ;
#1846=VERTEX_POINT ( 'NONE', #93368 ) ;
#1855=ORIENTED_EDGE ( 'NONE', *, *, #100383, .F. ) ;
#1860=CARTESIAN_POINT ( 'NONE',  ( -37.24781850355250867, 27.71755434321492118, -13.42510649394979438 ) ) ;
#1865=CARTESIAN_POINT ( 'NONE',  ( -37.56673239365849781, 25.47613764497371136, 13.45617127781066280 ) ) ;
#1870=FACE_OUTER_BOUND ( 'NONE', #101862, .T. ) ;
#1884=EDGE_CURVE ( 'NONE', #38179, #40774, #29720, .T. ) ;
#1903=CARTESIAN_POINT ( 'NONE',  ( 4.684273348644264514E-15, 28.20649408426940141, 38.25000000000000000 ) ) ;
#1931=SURFACE_SIDE_STYLE ('',( #69881 ) ) ;
#1970=( LENGTH_UNIT ( ) NAMED_UNIT ( * ) SI_UNIT ( .MILLI., .METRE. ) );
#1974=VECTOR ( 'NONE', #25652, 1000.000000000000000 ) ;
#2001=DIRECTION ( 'NONE',  ( 0.000000000000000000, 1.000000000000000000, -0.000000000000000000 ) ) ;
#2005=CARTESIAN_POINT ( 'NONE',  ( 15.50677046609170162, 34.82766853602287682, -23.25192831108139657 ) ) ;
#2006=DIRECTION ( 'NONE',  ( 0.000000000000000000, 1.000000000000000000, -0.000000000000000000 ) ) ;
#2010=VECTOR ( 'NONE', #8185, 1000.000000000000000 ) ;
#2042=CARTESIAN_POINT ( 'NONE',  ( -7.482235987343121231, 54.13190626386991511, -3.435864714555328270 ) ) ;
#2067=DIRECTION ( 'NONE',  ( 0.000000000000000000, 0.000000000000000000, 1.000000000000000000 ) ) ;
#2072=CARTESIAN_POINT ( 'NONE',  ( 49.27079747525518627, 12.96457032161368872, 15.75812555157588335 ) ) ;
#2128=CARTESIAN_POINT ( 'NONE',  ( 1.625879232102889042E-15, 47.29617335651134624, -13.27631144943088515 ) ) ;
#2139=CARTESIAN_POINT ( 'NONE',  ( 5.290067270632157204, 54.20842449845687838, -6.031152949374584793 ) ) ;
#2150=CARTESIAN_POINT ( 'NONE',  ( 28.08507790984678465, 36.49817779799894879, 8.014648791690131446 ) ) ;
#2155=CARTESIAN_POINT ( 'NONE',  ( 30.82729297445905914, 10.08692072324638822, -40.33672416147567219 ) ) ;
#2162=( NAMED_UNIT ( * ) PLANE_ANGLE_UNIT ( ) SI_UNIT ( $, .RADIAN. ) );
#2163=ADVANCED_FACE ( 'NONE', ( #52768, #11764 ), #94845, .F. ) ;
#2180=CARTESIAN_POINT ( 'NONE',  ( -0.4142654402135939606, 53.41932298510439381, 10.18236585056131460 ) ) ;
#2191=AXIS2_PLACEMENT_3D ( 'NONE', #12585, #29355, #95652 ) ;
#2206=CARTESIAN_POINT ( 'NONE',  ( -15.43372845131082016, 46.13227632078329776, -5.762758105581760937 ) ) ;
#2212=CARTESIAN_POINT ( 'NONE',  ( -0.3371335334081437818, 45.31563508470815549, 18.71541435546660637 ) ) ;
#2218=CARTESIAN_POINT ( 'NONE',  ( -48.91516379432439976, 8.057663746602589327, -16.48802948946170233 ) ) ;
#2226=COLOUR_RGB ( '', 0.09019608, 0.27058824, 0.51372549) ;
#2236=DIRECTION ( 'NONE',  ( -0.000000000000000000, 1.000000000000000000, 0.000000000000000000 ) ) ;
#2237=FILL_AREA_STYLE ('',( #74540 ) ) ;
#2250=CARTESIAN_POINT ( 'NONE',  ( -47.24423074384419152, 16.91655035847128019, 16.58644287016946706 ) ) ;
#2254=CARTESIAN_POINT ( 'NONE',  ( 11.49350100829463805, 45.59260286365996961, 13.79671030421800104 ) ) ;
#2267=DIRECTION ( 'NONE',  ( 0.000000000000000000, 0.000000000000000000, -1.000000000000000000 ) ) ;
#2268=EDGE_CURVE ( 'NONE', #37002, #57955, #84033, .T. ) ;
#2269=CYLINDRICAL_SURFACE ( 'NONE', #68427, 1.250000000000000222 ) ;
#2282=CARTESIAN_POINT ( 'NONE',  ( -0.7725392102466939193, 13.06347760300539207, -49.51297689002939961 ) ) ;
#2295=ORIENTED_EDGE ( 'NONE', *, *, #82415, .F. ) ;
#2302=EDGE_LOOP ( 'NONE', ( #47141, #12270, #97467, #103494, #52732, #80515, #77317, #15258 ) ) ;
#2303=COLOUR_RGB ( '', 0.66274510, 0.83137255, 0.94901961) ;
#2321=CARTESIAN_POINT ( 'NONE',  ( 7.943457856580265819, 51.78228140934420765, -3.880460080061692629 ) ) ;
#2325=DIRECTION ( 'NONE',  ( -0.000000000000000000, 1.000000000000000000, -0.000000000000000000 ) ) ;
#2336=DIRECTION ( 'NONE',  ( 0.000000000000000000, 0.000000000000000000, 1.000000000000000000 ) ) ;
#2352=CARTESIAN_POINT ( 'NONE',  ( -26.35543691165159430, 34.76319968196727217, -9.819974411512054857 ) ) ;
#2353=CARTESIAN_POINT ( 'NONE',  ( -0.08421528330799921136, 44.08548369317413318, -16.25000000000000355 ) ) ;
#2361=SURFACE_SIDE_STYLE ('',( #43368 ) ) ;
#2363=CARTESIAN_POINT ( 'NONE',  ( -46.79790428518977308, 18.85533329945891978, -15.37169442865915236 ) ) ;
#2369=ORIENTED_EDGE ( 'NONE', *, *, #104134, .F. ) ;
#2371=CARTESIAN_POINT ( 'NONE',  ( 37.56673239365870387, 27.60449318992555945, 13.45617127780999134 ) ) ;
#2378=EDGE_CURVE ( 'NONE', #88738, #41320, #80775, .T. ) ;
#2383=CARTESIAN_POINT ( 'NONE',  ( 48.60240570037284158, 10.21057620019136003, -14.48840219382827321 ) ) ;
#2386=CARTESIAN_POINT ( 'NONE',  ( 5.371796735821363633, 52.06045347113851562, 6.031152949374357419 ) ) ;
#2387=ORIENTED_EDGE ( 'NONE', *, *, #58333, .T. ) ;
#2392=AXIS2_PLACEMENT_3D ( 'NONE', #60995, #43727, #42125 ) ;
#2402=CARTESIAN_POINT ( 'NONE',  ( 49.18736646279173641, 13.60337276043470389, -15.12866845614532352 ) ) ;
#2405=DIRECTION ( 'NONE',  ( 0.000000000000000000, 1.000000000000000000, 0.000000000000000000 ) ) ;
#2425=ORIENTED_EDGE ( 'NONE', *, *, #15135, .F. ) ;
#2433=CARTESIAN_POINT ( 'NONE',  ( 29.68315524077034340, 18.29184282782460969, 39.60535821593451544 ) ) ;
#2437=CARTESIAN_POINT ( 'NONE',  ( -7.369762991775258065, 54.30878687387412640, 2.388529231885675674 ) ) ;
#2448=CARTESIAN_POINT ( 'NONE',  ( 9.096683260177623964, 53.76343451018224329, -1.649683610281133417 ) ) ;
#2459=CARTESIAN_POINT ( 'NONE',  ( 4.296529052608091703, 53.80523624942429706, -8.056204503449647447 ) ) ;
#2467=LINE ( 'NONE', #28391, #22008 ) ;
#2474=CARTESIAN_POINT ( 'NONE',  ( -23.21751746555280249, -1.200000000000000030E-05, -30.70617127781034839 ) ) ;
#2484=EDGE_LOOP ( 'NONE', ( #45656, #81810, #78497, #10601 ) ) ;
#2500=CARTESIAN_POINT ( 'NONE',  ( -46.81211797174974265, 13.24924033427093129, -15.90734432316361158 ) ) ;
#2502=FACE_BOUND ( 'NONE', #9476, .T. ) ;
#2516=CARTESIAN_POINT ( 'NONE',  ( 28.46830025707781076, 12.99948816575240151, -40.55052036360860512 ) ) ;
#2522=ORIENTED_EDGE ( 'NONE', *, *, #82081, .F. ) ;
#2529=EDGE_CURVE ( 'NONE', #74150, #74647, #53708, .T. ) ;
#2543=PRESENTATION_STYLE_ASSIGNMENT (( #45678 ) ) ;
#2556=ORIENTED_EDGE ( 'NONE', *, *, #29649, .T. ) ;
#2562=CARTESIAN_POINT ( 'NONE',  ( -37.56673239365863282, -1.200000000000000030E-05, -12.20617127781024713 ) ) ;
#2587=STYLED_ITEM ( 'NONE', ( #104117 ), #63298 ) ;
#2589=SURFACE_STYLE_FILL_AREA ( #84593 ) ;
#2597=DIRECTION ( 'NONE',  ( 0.000000000000000000, 0.000000000000000000, 1.000000000000000000 ) ) ;
#2614=COLOUR_RGB ( '', 0.31764706, 0.68627451, 0.89019608) ;
#2617=CARTESIAN_POINT ( 'NONE',  ( -10.90994580868044217, 43.80550646406358339, -13.06265761667911818 ) ) ;
#2624=DIRECTION ( 'NONE',  ( 0.000000000000000000, -0.3420201433256727652, -0.9396926207859068736 ) ) ;
#2636=CARTESIAN_POINT ( 'NONE',  ( -24.29660821760276690, 25.57666289385988634, -31.30556287864644105 ) ) ;
#2641=CARTESIAN_POINT ( 'NONE',  ( 0.08485693624074397423, 36.30024107553217050, 29.75000000000000000 ) ) ;
#2693=CARTESIAN_POINT ( 'NONE',  ( 28.35797521712592939, 36.30483405049672285, 8.953371298144853441 ) ) ;
#2713=AXIS2_PLACEMENT_3D ( 'NONE', #83592, #84676, #9166 ) ;
#2740=CARTESIAN_POINT ( 'NONE',  ( 16.64348903516496492, 43.47556584774762456, -6.657797401562562278 ) ) ;
#2759=CARTESIAN_POINT ( 'NONE',  ( -28.18165013807819363, 36.45077351536222920, 8.150803961754188975 ) ) ;
#2774=DIRECTION ( 'NONE',  ( 0.000000000000000000, 0.000000000000000000, 1.000000000000000000 ) ) ;
#2780=AXIS2_PLACEMENT_3D ( 'NONE', #38368, #105202, #96587 ) ;
#2787=CARTESIAN_POINT ( 'NONE',  ( -10.28624191511820207, -1.200000000000000030E-05, 14.15779740156163946 ) ) ;
#2794=ORIENTED_EDGE ( 'NONE', *, *, #73377, .F. ) ;
#2824=CARTESIAN_POINT ( 'NONE',  ( 4.733165431326070832E-26, 13.70447791526910919, -49.25000000000000000 ) ) ;
#2826=CARTESIAN_POINT ( 'NONE',  ( -17.16184658094835314, 36.31812281971417633, 24.24086490087779922 ) ) ;
#2829=CONICAL_SURFACE ( 'NONE', #16622, 11.96035173608223090, 1.221730476396025722 ) ;
#2832=CARTESIAN_POINT ( 'NONE',  ( 9.040080106534270854, 43.92515280565064018, -14.03042987452793788 ) ) ;
#2834=CARTESIAN_POINT ( 'NONE',  ( -4.048979898151962686, 53.98330245238265945, -7.635038885512192230 ) ) ;
#2836=ADVANCED_FACE ( 'NONE', ( #67115 ), #3976, .F. ) ;
#2854=ORIENTED_EDGE ( 'NONE', *, *, #51839, .T. ) ;
#2857=CARTESIAN_POINT ( 'NONE',  ( -1.249627314476824180, 27.80309404206683155, -39.33848994184150172 ) ) ;
#2863=CARTESIAN_POINT ( 'NONE',  ( 47.55680477683365126, 16.06931990738367233, -16.76905664007707841 ) ) ;
#2896=EDGE_LOOP ( 'NONE', ( #24599, #12781 ) ) ;
#2905=CARTESIAN_POINT ( 'NONE',  ( -10.28624191512074226, 46.12099395432516502, 12.90779740155501187 ) ) ;
#2916=CARTESIAN_POINT ( 'NONE',  ( 5.290067270632455632, 51.34639538792298197, 8.531152949374481764 ) ) ;
#2959=( GEOMETRIC_REPRESENTATION_CONTEXT ( 3 ) GLOBAL_UNCERTAINTY_ASSIGNED_CONTEXT ( ( #93375 ) ) GLOBAL_UNIT_ASSIGNED_CONTEXT ( ( #93969, #105623, #78297 ) ) REPRESENTATION_CONTEXT ( 'NONE', 'WORKASPACE' ) );
#2983=CARTESIAN_POINT ( 'NONE',  ( 9.183451665179635626, 53.50050700487116728, -3.876548107677253441 ) ) ;
#3009=CARTESIAN_POINT ( 'NONE',  ( -23.38216085046615689, 27.34669553923654561, -33.20617127781036260 ) ) ;
#3041=CARTESIAN_POINT ( 'NONE',  ( -47.57454933833918176, 12.59078750739570829, -14.43852527042941070 ) ) ;
#3060=DIRECTION ( 'NONE',  ( -0.000000000000000000, 1.000000000000000000, -0.000000000000000000 ) ) ;
#3061=CARTESIAN_POINT ( 'NONE',  ( 16.96324018633373143, 45.77154698568147495, -4.157797401561765582 ) ) ;
#3066=( LENGTH_UNIT ( ) NAMED_UNIT ( * ) SI_UNIT ( .MILLI., .METRE. ) );
#3072=DIRECTION ( 'NONE',  ( 0.000000000000000000, 1.000000000000000000, 0.000000000000000000 ) ) ;
#3081=FACE_OUTER_BOUND ( 'NONE', #80474, .T. ) ;
#3163=CARTESIAN_POINT ( 'NONE',  ( -11.53040807487433739, 43.41108915750923813, -13.95613592774078882 ) ) ;
#3164=CARTESIAN_POINT ( 'NONE',  ( -1.219175067079236729, 36.86153658035306080, 28.18154403026957766 ) ) ;
#3184=CARTESIAN_POINT ( 'NONE',  ( -23.54609178594817820, 25.19604284925236470, -33.16510347394218172 ) ) ;
#3192=VERTEX_POINT ( 'NONE', #64856 ) ;
#3201=MECHANICAL_DESIGN_GEOMETRIC_PRESENTATION_REPRESENTATION('',(#101367),#18705);
#3207=CARTESIAN_POINT ( 'NONE',  ( -37.56673239365849781, 27.88554838446201600, 10.95617127781066102 ) ) ;
#3209=CARTESIAN_POINT ( 'NONE',  ( -15.88102029263269444, 46.13028405480689997, 4.403441971141869971 ) ) ;
#3245=VECTOR ( 'NONE', #95115, 1000.000000000000000 ) ;
#3246=CARTESIAN_POINT ( 'NONE',  ( 29.68315524076959377, 13.12249633091058243, -39.60535821593525441 ) ) ;
#3254=CYLINDRICAL_SURFACE ( 'NONE', #78822, 1.250000000000001110 ) ;
#3271=CARTESIAN_POINT ( 'NONE',  ( 23.38216085046638781, 27.34669553923654561, 33.20617127781017786 ) ) ;
#3273=CARTESIAN_POINT ( 'NONE',  ( -17.83066785977178625, 36.70615155823221443, -22.40577935710505386 ) ) ;
#3288=CARTESIAN_POINT ( 'NONE',  ( -1.099010308150110360, 36.97177997581172804, -27.88336368392158349 ) ) ;
#3331=CARTESIAN_POINT ( 'NONE',  ( 29.99961410214308799, 17.76511157208309655, -39.64372791628649395 ) ) ;
#3342=CARTESIAN_POINT ( 'NONE',  ( 16.75187969033571989, 34.99134772383131065, 21.80698433968582961 ) ) ;
#3346=CARTESIAN_POINT ( 'NONE',  ( 0.1553986885509386628, 12.93312546826206777, 51.74235877965696062 ) ) ;
#3349=EDGE_LOOP ( 'NONE', ( #102749, #95468, #60400, #41036 ) ) ;
#3369=CARTESIAN_POINT ( 'NONE',  ( -8.240492251933538626, 51.94749170291629525, -1.561714456288526787 ) ) ;
#3374=CARTESIAN_POINT ( 'NONE',  ( -1.411247199636991373E-12, 7.746009256445978153, -51.75000000000450484 ) ) ;
#3376=CARTESIAN_POINT ( 'NONE',  ( -17.96008057617824605, 36.59330496951920253, 22.69888471349226577 ) ) ;
#3383=CARTESIAN_POINT ( 'NONE',  ( -4.063221008705400372, 54.18599283795405341, -6.989960337625931608 ) ) ;
#3385=CARTESIAN_POINT ( 'NONE',  ( -9.268669127170596767, 46.19464124546546913, -13.41262564492496345 ) ) ;
#3390=MECHANICAL_DESIGN_GEOMETRIC_PRESENTATION_REPRESENTATION('',(#98015),#65374);
#3393=CARTESIAN_POINT ( 'NONE',  ( 27.10511071441176867, 36.60571256639526894, -10.05698433968634653 ) ) ;
#3410=CARTESIAN_POINT ( 'NONE',  ( -0.7863538930209251765, 27.39022669171391300, -40.48520517837179256 ) ) ;
#3415=CARTESIAN_POINT ( 'NONE',  ( 46.79638705082384575, 18.85256363620282016, -15.38003188690575662 ) ) ;
#3417=CARTESIAN_POINT ( 'NONE',  ( -10.28624191511820207, 43.99263840937192782, 12.90779740156163768 ) ) ;
#3419=CARTESIAN_POINT ( 'NONE',  ( -48.26904874857379468, 16.21976735686916271, 14.37315625587772949 ) ) ;
#3421=FACE_OUTER_BOUND ( 'NONE', #40838, .T. ) ;
#3458=VECTOR ( 'NONE', #102172, 1000.000000000000227 ) ;
#3459=CARTESIAN_POINT ( 'NONE',  ( -17.86128288688793120, 34.21128401912330474, 23.65645931953497438 ) ) ;
#3460=CARTESIAN_POINT ( 'NONE',  ( 9.204171687489081322, 45.78377104600746605, -14.80353108812691687 ) ) ;
#3465=CARTESIAN_POINT ( 'NONE',  ( 49.19520577559729446, 7.745679164654342586, -16.05969994618069308 ) ) ;
#3484=CARTESIAN_POINT ( 'NONE',  ( 49.24354615586579342, 13.35554545791556968, -15.29900703100353176 ) ) ;
#3487=CARTESIAN_POINT ( 'NONE',  ( -10.28624191511820207, -1.200000000000000030E-05, 12.90779740156163768 ) ) ;
#3490=CARTESIAN_POINT ( 'NONE',  ( 0.000000000000000000, 27.68727484027578356, 0.000000000000000000 ) ) ;
#3500=EDGE_LOOP ( 'NONE', ( #100297, #70026, #20225, #20569 ) ) ;
#3515=CARTESIAN_POINT ( 'NONE',  ( 30.36582766586239046, 16.93822630193517398, 39.80117229897599174 ) ) ;
#3527=VECTOR ( 'NONE', #7053, 1000.000000000000000 ) ;
#3531=CARTESIAN_POINT ( 'NONE',  ( 9.323684072238750176, 53.46633439451886005, -3.784536294736342565 ) ) ;
#3567=CARTESIAN_POINT ( 'NONE',  ( -1.248789410298115632, 51.75335132569763630, -8.832271914632384480 ) ) ;
#3586=LINE ( 'NONE', #28420, #62108 ) ;
#3588=CARTESIAN_POINT ( 'NONE',  ( -17.86524139598605743, 43.17258651664646152, -5.721017747561236710 ) ) ;
#3609=CARTESIAN_POINT ( 'NONE',  ( -9.810837553057309535, 51.28247512958390075, 2.841815975853968723 ) ) ;
#3624=FILL_AREA_STYLE_COLOUR ( '', #42979 ) ;
#3650=SURFACE_STYLE_USAGE ( .BOTH. , #52178 ) ;
#3651=CARTESIAN_POINT ( 'NONE',  ( 0.3379341052171724313, 36.31244600152816560, -29.71494666831264198 ) ) ;
#3657=SURFACE_STYLE_USAGE ( .BOTH. , #53265 ) ;
#3667=ORIENTED_EDGE ( 'NONE', *, *, #92544, .T. ) ;
#3695=CARTESIAN_POINT ( 'NONE',  ( 0.2950248152710058802, 7.823291154770383393, -51.71678101502384806 ) ) ;
#3716=VERTEX_POINT ( 'NONE', #65854 ) ;
#3725=CARTESIAN_POINT ( 'NONE',  ( -23.21751746555280249, 25.98869614573808207, -30.70617127781034839 ) ) ;
#3732=CARTESIAN_POINT ( 'NONE',  ( 15.50702112914487785, 36.95515616017750204, -23.25462944313571967 ) ) ;
#3771=EDGE_LOOP ( 'NONE', ( #80434, #74263 ) ) ;
#3781=CARTESIAN_POINT ( 'NONE',  ( 30.42742517972242666, 7.740625494265016115, -41.86256052107409431 ) ) ;
#3782=FACE_OUTER_BOUND ( 'NONE', #91838, .T. ) ;
#3784=ORIENTED_EDGE ( 'NONE', *, *, #54002, .F. ) ;
#3789=SURFACE_STYLE_USAGE ( .BOTH. , #69591 ) ;
#3799=ORIENTED_EDGE ( 'NONE', *, *, #32312, .T. ) ;
#3804=SURFACE_STYLE_FILL_AREA ( #77695 ) ;
#3816=CARTESIAN_POINT ( 'NONE',  ( -5.455379837882870397, 51.31468677425149849, 8.531152949374572358 ) ) ;
#3822=EDGE_CURVE ( 'NONE', #34804, #14145, #76595, .T. ) ;
#3827=CARTESIAN_POINT ( 'NONE',  ( -5.290067270632214047, 53.47475093287474124, -8.531152949374821048 ) ) ;
#3829=CARTESIAN_POINT ( 'NONE',  ( -16.32471966984383371, 45.71573795642331106, -6.626903219538490930 ) ) ;
#3839=CARTESIAN_POINT ( 'NONE',  ( -0.7852806286178579676, 46.11106221562390317, 16.51405864586197225 ) ) ;
#3845=CARTESIAN_POINT ( 'NONE',  ( -49.07509721567202376, 8.836758769845310724, -14.91787708872438856 ) ) ;
#3855=ADVANCED_FACE ( 'NONE', ( #101937 ), #12387, .F. ) ;
#3880=CARTESIAN_POINT ( 'NONE',  ( -3.312116827214752676E-14, 12.91535575336970965, 51.75000000000017764 ) ) ;
#3886=ADVANCED_FACE ( 'NONE', ( #11316 ), #3254, .F. ) ;
#3902=CARTESIAN_POINT ( 'NONE',  ( -7.315365623647276827, 52.17029336129217398, -2.633652021638295704 ) ) ;
#3906=CARTESIAN_POINT ( 'NONE',  ( -27.92784172790835839, 34.23327901736961820, 9.751711673318832041 ) ) ;
#3907=CARTESIAN_POINT ( 'NONE',  ( -0.2984172751366608867, 7.825053155909972524, -51.71602382706492307 ) ) ;
#3909=UNCERTAINTY_MEASURE_WITH_UNIT (LENGTH_MEASURE( 1.000000000000000082E-05 ), #80965, 'distance_accuracy_value', 'NONE');
#3914=CARTESIAN_POINT ( 'NONE',  ( 17.08457507770788908, 34.19635311626529983, -24.27368305446641727 ) ) ;
#3919=CARTESIAN_POINT ( 'NONE',  ( -9.954785814282052669, 46.18621183893549897, -12.94079623093657183 ) ) ;
#3930=EDGE_CURVE ( 'NONE', #54691, #54576, #96518, .T. ) ;
#3945=AXIS2_PLACEMENT_3D ( 'NONE', #41279, #83864, #82265 ) ;
#3947=CARTESIAN_POINT ( 'NONE',  ( -10.45131719755852728, 43.22378321881971175, 15.40779740156164479 ) ) ;
#3976=CYLINDRICAL_SURFACE ( 'NONE', #16992, 1.250000000000001110 ) ;
#3987=CARTESIAN_POINT ( 'NONE',  ( 1.152188841818234133E-13, -1.200000000000000030E-05, 50.50000000000000000 ) ) ;
#3993=CARTESIAN_POINT ( 'NONE',  ( -17.08308936354170982, 34.91790941067561249, 21.80698433968612449 ) ) ;
#3998=CARTESIAN_POINT ( 'NONE',  ( 49.22180010227521052, 7.740565218139805914, -15.98496799241697808 ) ) ;
#4010=CARTESIAN_POINT ( 'NONE',  ( 49.07662235626771263, 14.00107037724277248, -14.92012541985465646 ) ) ;
#4018=DIRECTION ( 'NONE',  ( 0.000000000000000000, 1.000000000000000000, 0.000000000000000000 ) ) ;
#4025=CARTESIAN_POINT ( 'NONE',  ( 1.106009303435988578, 12.12314782375359101, 49.90128369131649322 ) ) ;
#4028=CARTESIAN_POINT ( 'NONE',  ( 22.19860641359351305, 28.18788469371686745, -31.21259335822235315 ) ) ;
#4038=( LENGTH_UNIT ( ) NAMED_UNIT ( * ) SI_UNIT ( .MILLI., .METRE. ) );
#4056=ORIENTED_EDGE ( 'NONE', *, *, #100828, .T. ) ;
#4061=CARTESIAN_POINT ( 'NONE',  ( 9.647447593234698360, 53.40512216555158176, -3.402356764703239111 ) ) ;
#4072=ORIENTED_EDGE ( 'NONE', *, *, #96963, .T. ) ;
#4084=B_SPLINE_CURVE_WITH_KNOTS ( 'NONE', 3,
 ( #62873, #95761, #104365, #79566, #55276, #30517, #63414, #11634, #20868, #37026, #77454, #3567, #36504, #28952, #45102, #69371, #77982, #4098, #61824, #94720 ),
 .UNSPECIFIED., .F., .F.,
 ( 4, 2, 2, 2, 2, 2, 2, 2, 2, 4 ),
 ( 0.007074730525056170845, 0.007326744003114083262, 0.007578757481171995679, 0.008082784437287823115, 0.008586811393403649684, 0.009090838349519476252, 0.009594865305635304556, 0.01009889226175113112, 0.01060291921786695943, 0.01110694617398278600 ),
 .UNSPECIFIED. ) ;
#4085=FILL_AREA_STYLE ('',( #93087 ) ) ;
#4091=VERTEX_POINT ( 'NONE', #22110 ) ;
#4098=CARTESIAN_POINT ( 'NONE',  ( -0.3381277199951053247, 52.16423866172722512, -7.785256431692882728 ) ) ;
#4112=ORIENTED_EDGE ( 'NONE', *, *, #78990, .T. ) ;
#4120=EDGE_LOOP ( 'NONE', ( #40129, #23758, #8743, #4072 ) ) ;
#4133=LINE ( 'NONE', #102829, #103012 ) ;
#4155=DIRECTION ( 'NONE',  ( 0.000000000000000000, 0.000000000000000000, 1.000000000000000000 ) ) ;
#4162=CARTESIAN_POINT ( 'NONE',  ( -0.08435185965673104580, 25.16821295365207334, -40.75000000000000711 ) ) ;
#4167=LINE ( 'NONE', #73106, #78661 ) ;
#4183=PRESENTATION_STYLE_ASSIGNMENT (( #71554 ) ) ;
#4196=CARTESIAN_POINT ( 'NONE',  ( -16.75187969033554936, 34.99134772383131065, -21.80698433968595751 ) ) ;
#4220=ORIENTED_EDGE ( 'NONE', *, *, #21653, .T. ) ;
#4226=LINE ( 'NONE', #29600, #51798 ) ;
#4227=ORIENTED_EDGE ( 'NONE', *, *, #100714, .T. ) ;
#4247=STYLED_ITEM ( 'NONE', ( #26921 ), #41549 ) ;
#4254=EDGE_CURVE ( 'NONE', #98888, #54301, #40852, .T. ) ;
#4268=CARTESIAN_POINT ( 'NONE',  ( -38.78825536228157489, 27.29347880557803308, 12.52013247353241177 ) ) ;
#4275=CARTESIAN_POINT ( 'NONE',  ( -30.93381850223239482, 8.838939540955959018, 40.91347331214245031 ) ) ;
#4277=EDGE_CURVE ( 'NONE', #61560, #22182, #94749, .T. ) ;
#4286=CARTESIAN_POINT ( 'NONE',  ( -16.48462266119839015, 43.81152415571271064, -4.165346518886126503 ) ) ;
#4299=CARTESIAN_POINT ( 'NONE',  ( 28.35336936217584025, 36.33375255386920344, 8.699746290353250089 ) ) ;
#4324=CARTESIAN_POINT ( 'NONE',  ( -21.98976603507239247, 28.09591002020466632, 31.66807300705238504 ) ) ;
#4328=CARTESIAN_POINT ( 'NONE',  ( 24.23713502960781341, 27.31419257049584104, 32.69873751732569644 ) ) ;
#4329=( NAMED_UNIT ( * ) SI_UNIT ( $, .STERADIAN. ) SOLID_ANGLE_UNIT ( ) );
#4330=CARTESIAN_POINT ( 'NONE',  ( -17.37733725250675221, 36.93507598878604625, -21.96268678933289920 ) ) ;
#4331=EDGE_CURVE ( 'NONE', #87056, #65902, #19364, .T. ) ;
#4339=CARTESIAN_POINT ( 'NONE',  ( 0.000000000000000000, 2.000000000000000000, 0.000000000000000000 ) ) ;
#4340=CARTESIAN_POINT ( 'NONE',  ( -1.220556079094060831, 51.58127574836134244, 9.313543911585616897 ) ) ;
#4344=CARTESIAN_POINT ( 'NONE',  ( 37.40740465628558553, 25.81286408686213463, -10.95617127781081024 ) ) ;
#4352=CARTESIAN_POINT ( 'NONE',  ( -23.21751746555280249, -1.200000000000000030E-05, -31.95617127781034839 ) ) ;
#4388=CARTESIAN_POINT ( 'NONE',  ( 30.80732993440513567, 13.24159032961889437, -41.41050123719151088 ) ) ;
#4398=CARTESIAN_POINT ( 'NONE',  ( -47.29141116144595003, 18.29911311166173959, 14.59113362281949655 ) ) ;
#4427=CARTESIAN_POINT ( 'NONE',  ( -28.31493636581005546, 34.24499175938969842, 8.451752357833321128 ) ) ;
#4428=CARTESIAN_POINT ( 'NONE',  ( 8.559508646656407649, -1.200000000000000030E-05, 2.781152949374444461 ) ) ;
#4454=AXIS2_PLACEMENT_3D ( 'NONE', #949, #50581, #34468 ) ;
#4464=VECTOR ( 'NONE', #43185, 1000.000000000000000 ) ;
#4485=CARTESIAN_POINT ( 'NONE',  ( -8.559508646656389885, 53.96349637827586321, -1.531152949374502859 ) ) ;
#4501=CARTESIAN_POINT ( 'NONE',  ( 28.02682550970785513, 34.39574914770449965, -7.958842414421645195 ) ) ;
#4509=DIRECTION ( 'NONE',  ( 1.150791560227848051E-16, -0.3420201433256733758, 0.9396926207859066515 ) ) ;
#4529=AXIS2_PLACEMENT_3D ( 'NONE', #7434, #32286, #47895 ) ;
#4532=B_SPLINE_CURVE_WITH_KNOTS ( 'NONE', 3,
 ( #7905, #32756, #96931, #80733, #74238, #89901, #72649, #73161, #31689, #315, #106063, #23602, #33280, #64575, #97441, #99033, #56985, #25198, #89384, #99573, #17623, #66691 ),
 .UNSPECIFIED., .F., .F.,
 ( 4, 2, 2, 2, 2, 2, 2, 2, 2, 2, 4 ),
 ( 0.003183879630746418773, 0.003435849579571543036, 0.003687819528396666865, 0.004191759426046917127, 0.004695699323697167388, 0.005199639221347416781, 0.006207519016647917304, 0.006459488965473041133, 0.006711458914298166697, 0.006963428863123290527, 0.007215398811948416091 ),
 .UNSPECIFIED. ) ;
#4536=CARTESIAN_POINT ( 'NONE',  ( 49.22174280021646808, 12.91003493663461832, -15.98497293138166597 ) ) ;
#4541=STYLED_ITEM ( 'NONE', ( #100191 ), #57681 ) ;
#4542=CARTESIAN_POINT ( 'NONE',  ( -37.56673239365851913, 25.75719283951025673, 10.95617127780993449 ) ) ;
#4570=( NAMED_UNIT ( * ) SI_UNIT ( $, .STERADIAN. ) SOLID_ANGLE_UNIT ( ) );
#4607=CARTESIAN_POINT ( 'NONE',  ( 5.290067270632157204, 54.20842449845687838, -6.031152949374584793 ) ) ;
#4608=CARTESIAN_POINT ( 'NONE',  ( 16.32209425763040755, 43.86680992065402052, 4.189051175685120754 ) ) ;
#4614=CARTESIAN_POINT ( 'NONE',  ( 27.10511071441197117, 36.60571256639528315, 10.05698433968570704 ) ) ;
#4617=CARTESIAN_POINT ( 'NONE',  ( -23.97722388339740007, 27.87827700592711722, -30.95083563548404015 ) ) ;
#4627=ORIENTED_EDGE ( 'NONE', *, *, #39626, .T. ) ;
#4628=COLOUR_RGB ( '', 0.31764706, 0.68627451, 0.89019608) ;
#4650=DIRECTION ( 'NONE',  ( 0.000000000000000000, 1.000000000000000000, -0.000000000000000000 ) ) ;
#4653=CARTESIAN_POINT ( 'NONE',  ( 0.000000000000000000, 25.16329480281783759, 0.000000000000000000 ) ) ;
#4666=CARTESIAN_POINT ( 'NONE',  ( 16.75187969033515145, 34.25544727262118982, -24.30698433968624883 ) ) ;
#4684=MECHANICAL_DESIGN_GEOMETRIC_PRESENTATION_REPRESENTATION('',(#94301),#44329);
#4696=FACE_BOUND ( 'NONE', #66261, .T. ) ;
#4702=VECTOR ( 'NONE', #84172, 1000.000000000000000 ) ;
#4711=CARTESIAN_POINT ( 'NONE',  ( 0.000000000000000000, -1.200000000000000030E-05, -16.25000000000000000 ) ) ;
#4716=VECTOR ( 'NONE', #46555, 1000.000000000000000 ) ;
#4719=FACE_OUTER_BOUND ( 'NONE', #90286, .T. ) ;
#4737=DIRECTION ( 'NONE',  ( -0.000000000000000000, -1.000000000000000000, -0.000000000000000000 ) ) ;
#4746=CARTESIAN_POINT ( 'NONE',  ( 0.6187971826122187213, 13.31391316207858644, -49.41005251785713170 ) ) ;
#4748=EDGE_CURVE ( 'NONE', #23687, #78599, #34869, .T. ) ;
#4783=( LENGTH_UNIT ( ) NAMED_UNIT ( * ) SI_UNIT ( .MILLI., .METRE. ) );
#4788=CARTESIAN_POINT ( 'NONE',  ( -8.559508646656381003, 51.83514083332404709, -1.531152949374265049 ) ) ;
#4797=DIRECTION ( 'NONE',  ( 0.000000000000000000, 1.000000000000000000, -0.000000000000000000 ) ) ;
#4830=ORIENTED_EDGE ( 'NONE', *, *, #61343, .F. ) ;
#4858=EDGE_LOOP ( 'NONE', ( #13622, #5605 ) ) ;
#4859=CARTESIAN_POINT ( 'NONE',  ( 16.48376536647090873, 45.65789762114239636, -6.657797401561987627 ) ) ;
#4880=CARTESIAN_POINT ( 'NONE',  ( 37.56673239365899519, 25.75719283951025318, -10.95617127780834998 ) ) ;
#4888=CARTESIAN_POINT ( 'NONE',  ( -1.011530059480323152, 34.89403417720795630, 27.74769827951694978 ) ) ;
#4891=UNCERTAINTY_MEASURE_WITH_UNIT (LENGTH_MEASURE( 1.000000000000000082E-05 ), #30005, 'distance_accuracy_value', 'NONE');
#4904=CARTESIAN_POINT ( 'NONE',  ( -49.26505482459800334, 8.072780847947164773, -15.39015249100678240 ) ) ;
#4913=CARTESIAN_POINT ( 'NONE',  ( -15.79195268148549758, 35.06869440440700458, 22.25194163443071460 ) ) ;
#4914=VERTEX_POINT ( 'NONE', #80059 ) ;
#4930=( LENGTH_UNIT ( ) NAMED_UNIT ( * ) SI_UNIT ( .MILLI., .METRE. ) );
#4937=CARTESIAN_POINT ( 'NONE',  ( -47.06916318994504422, 18.66170694578063660, 14.79344423761920169 ) ) ;
#4940=CARTESIAN_POINT ( 'NONE',  ( 0.7794294244140879124, 13.54093176544609634, 51.48168560154597628 ) ) ;
#4971=UNCERTAINTY_MEASURE_WITH_UNIT (LENGTH_MEASURE( 1.000000000000000082E-05 ), #58294, 'distance_accuracy_value', 'NONE');
#4980=FACE_OUTER_BOUND ( 'NONE', #53912, .T. ) ;
#4989=FACE_OUTER_BOUND ( 'NONE', #77943, .T. ) ;
#4995=ORIENTED_EDGE ( 'NONE', *, *, #97134, .F. ) ;
#5004=CARTESIAN_POINT ( 'NONE',  ( -10.28624191512074226, 46.12099395432516502, 12.90779740155501187 ) ) ;
#5025=EDGE_LOOP ( 'NONE', ( #10965, #75798, #56164, #33809 ) ) ;
#5028=CIRCLE ( 'NONE', #49744, 22.55262289886175964 ) ;
#5034=CARTESIAN_POINT ( 'NONE',  ( -48.55387420720941805, 13.84642135131182883, -16.74239769522730015 ) ) ;
#5053=CARTESIAN_POINT ( 'NONE',  ( 10.28624191512063746, 46.12099395432516502, -12.90779740155508826 ) ) ;
#5055=ORIENTED_EDGE ( 'NONE', *, *, #27995, .F. ) ;
#5060=B_SPLINE_CURVE_WITH_KNOTS ( 'NONE', 3,
 ( #86852, #4859, #79267, #5390, #38312, #71173, #104067, #54973, #87904, #1513, #959, #73823, #57623, #25869, #106718, #33940, #66808, #99697, #427, #16118 ),
 .UNSPECIFIED., .F., .F.,
 ( 4, 2, 2, 2, 2, 2, 2, 2, 2, 4 ),
 ( 0.001107850312301166765, 0.001612907343245353377, 0.002117964374189539988, 0.002623021405133726600, 0.003128078436077913211, 0.003380606951550005432, 0.003633135467022097220, 0.004138192497966280796, 0.004643249528910464372, 0.005148306559854647080 ),
 .UNSPECIFIED. ) ;
#5068=( NAMED_UNIT ( * ) PLANE_ANGLE_UNIT ( ) SI_UNIT ( $, .RADIAN. ) );
#5079=LINE ( 'NONE', #46072, #36214 ) ;
#5108=VERTEX_POINT ( 'NONE', #39099 ) ;
#5135=PRESENTATION_STYLE_ASSIGNMENT (( #24004 ) ) ;
#5144=CARTESIAN_POINT ( 'NONE',  ( 26.35623858825801591, 36.89120352755210774, 9.820590063098430633 ) ) ;
#5146=EDGE_CURVE ( 'NONE', #36049, #60190, #75410, .T. ) ;
#5152=STYLED_ITEM ( 'NONE', ( #72058 ), #90915 ) ;
#5179=CARTESIAN_POINT ( 'NONE',  ( -37.56673239365863282, 25.47613764497371847, -13.45617127781024891 ) ) ;
#5197=CARTESIAN_POINT ( 'NONE',  ( 3.840629472727446691E-14, -1.200000000000000030E-05, 29.75000000000000355 ) ) ;
#5200=EDGE_CURVE ( 'NONE', #86888, #37002, #96796, .T. ) ;
#5205=EDGE_CURVE ( 'NONE', #45709, #31195, #54775, .T. ) ;
#5220=B_SPLINE_CURVE_WITH_KNOTS ( 'NONE', 3,
 ( #94494, #61059, #93953, #20106, #52950, #77765, #86413, #12474, #40477, #23801, #15140, #80397, #8104, #55579, #65818, #90632, #89569, #39959, #48557, #31369, #105222, #56650, #64763, #98181, #5976, #7043, #64246, #88515 ),
 .UNSPECIFIED., .F., .F.,
 ( 4, 2, 2, 2, 2, 2, 2, 2, 2, 2, 2, 2, 2, 4 ),
 ( 0.007040904414468357811, 0.007507994684082224500, 0.007741539818889156543, 0.007975084953696087720, 0.008208630088503018896, 0.008442175223309951806, 0.008909265492923803750, 0.009376355762537657429, 0.009843446032151509373, 0.01077762657137921153, 0.01171180711060691194, 0.01264598764983461410, 0.01358016818906231452, 0.01451434872829001493 ),
 .UNSPECIFIED. ) ;
#5277=CARTESIAN_POINT ( 'NONE',  ( -7.313038074512826725, 52.12733562386607389, 2.972571716980497492 ) ) ;
#5287=DIRECTION ( 'NONE',  ( -0.000000000000000000, 1.000000000000000000, 0.000000000000000000 ) ) ;
#5288=EDGE_LOOP ( 'NONE', ( #73036, #35357 ) ) ;
#5298=ORIENTED_EDGE ( 'NONE', *, *, #54205, .T. ) ;
#5301=LINE ( 'NONE', #93389, #76670 ) ;
#5317=FILL_AREA_STYLE_COLOUR ( '', #93989 ) ;
#5323=CARTESIAN_POINT ( 'NONE',  ( -26.02892717936697053, 37.04797716037987243, 9.463389932884222588 ) ) ;
#5336=CARTESIAN_POINT ( 'NONE',  ( -49.02571528365156439, 7.903708718522313603, 16.36159347772456130 ) ) ;
#5344=CARTESIAN_POINT ( 'NONE',  ( -30.48982775277903201, 7.748378201987720537, 41.81310123456335504 ) ) ;
#5362=VERTEX_POINT ( 'NONE', #96133 ) ;
#5370=ORIENTED_EDGE ( 'NONE', *, *, #84729, .F. ) ;
#5390=CARTESIAN_POINT ( 'NONE',  ( 16.02987949830365011, 45.83140534720696735, -6.508315408883887265 ) ) ;
#5406=CARTESIAN_POINT ( 'NONE',  ( -1.250645447352602302, 51.63769438765763908, 9.152833739580529482 ) ) ;
#5415=CARTESIAN_POINT ( 'NONE',  ( -9.041223022389656805, 43.82561790570887439, -14.35408047631669248 ) ) ;
#5438=DIRECTION ( 'NONE',  ( 0.000000000000000000, 0.000000000000000000, 1.000000000000000000 ) ) ;
#5443=CIRCLE ( 'NONE', #55383, 63.00000000000000000 ) ;
#5459=CARTESIAN_POINT ( 'NONE',  ( 36.31378453431777587, 28.20125269961366854, 12.06226767304767478 ) ) ;
#5462=CARTESIAN_POINT ( 'NONE',  ( 17.76962432240387812, 34.18902918576760186, 23.80189063641344305 ) ) ;
#5488=B_SPLINE_CURVE_WITH_KNOTS ( 'NONE', 3,
 ( #70972, #30010, #86125, #103350, #37051, #87701, #69917, #46693, #73606, #57954, #105974, #89816, #66060, #73066, #8350, #65000, #49871, #48795, #40188, #7809, #90877, #98937, #15916, #97356, #33190, #32119, #31601, #7281, #751, #56890 ),
 .UNSPECIFIED., .F., .F.,
 ( 4, 2, 2, 2, 2, 2, 2, 2, 2, 2, 2, 2, 2, 2, 4 ),
 ( 0.01451434872829011555, 0.01497952839231836766, 0.01521211822433249199, 0.01544470805634661631, 0.01567729788836074237, 0.01590988772037486496, 0.01637506738440312748, 0.01684024704843139000, 0.01730542671245965253, 0.01823578604051618104, 0.01916614536857271303, 0.02009650469662924155, 0.02102686402468577354, 0.02149204368871403953, 0.02195722335274230899 ),
 .UNSPECIFIED. ) ;
#5526=CARTESIAN_POINT ( 'NONE',  ( 10.91152070480431568, 45.93327767897820024, -13.06343554040043919 ) ) ;
#5527=CARTESIAN_POINT ( 'NONE',  ( 46.95966155981695778, 18.79500983735056963, -14.95375697514157132 ) ) ;
#5529=DIRECTION ( 'NONE',  ( 0.000000000000000000, 0.000000000000000000, 1.000000000000000000 ) ) ;
#5552=CARTESIAN_POINT ( 'NONE',  ( -48.15057074821032757, 16.50253122541020190, -14.35535821593460604 ) ) ;
#5555=CARTESIAN_POINT ( 'NONE',  ( 27.10511071441176867, 34.75829513984540142, -7.556984339686343866 ) ) ;
#5564=( NAMED_UNIT ( * ) PLANE_ANGLE_UNIT ( ) SI_UNIT ( $, .RADIAN. ) );
#5579=CARTESIAN_POINT ( 'NONE',  ( -38.76857929379224288, 27.37303770309710416, -11.85268573845290696 ) ) ;
#5584=CARTESIAN_POINT ( 'NONE',  ( 11.07233799575516286, 45.30046846812411587, 15.14426123305342387 ) ) ;
#5590=CARTESIAN_POINT ( 'NONE',  ( -16.64348903516496136, 45.60392139269943357, -6.657797401562710604 ) ) ;
#5604=CARTESIAN_POINT ( 'NONE',  ( 38.56444062946145834, 27.31873531207203598, 12.97723241238764658 ) ) ;
#5605=ORIENTED_EDGE ( 'NONE', *, *, #88459, .T. ) ;
#5606=CARTESIAN_POINT ( 'NONE',  ( 10.28624191511840458, 43.25714326066859172, 15.40779740156149202 ) ) ;
#5656=CARTESIAN_POINT ( 'NONE',  ( 16.64348903516524203, 43.75610143575153188, 4.157797401561407646 ) ) ;
#5673=CARTESIAN_POINT ( 'NONE',  ( -24.43671627503044164, 25.27466499483696794, 32.24378702798332341 ) ) ;
#5690=EDGE_CURVE ( 'NONE', #6418, #79581, #32131, .T. ) ;
#5722=CARTESIAN_POINT ( 'NONE',  ( 4.387778976649724167E-15, 34.08768991669519721, 35.82893434829263413 ) ) ;
#5782=FACE_OUTER_BOUND ( 'NONE', #78734, .T. ) ;
#5787=SURFACE_STYLE_USAGE ( .BOTH. , #50882 ) ;
#5788=CARTESIAN_POINT ( 'NONE',  ( 0.1682240322482835559, 26.07813853931757464, -38.24999999999999289 ) ) ;
#5797=CARTESIAN_POINT ( 'NONE',  ( 16.75187969033571989, 36.38380281757302726, 24.30698433968583316 ) ) ;
#5806=AXIS2_PLACEMENT_3D ( 'NONE', #98417, #88220, #47205 ) ;
#5809=EDGE_CURVE ( 'NONE', #39760, #36282, #54555, .T. ) ;
#5811=VERTEX_POINT ( 'NONE', #24338 ) ;
#5834=CARTESIAN_POINT ( 'NONE',  ( -25.91464401492078906, 37.21125547857348437, 8.416521324649474778 ) ) ;
#5842=( NAMED_UNIT ( * ) SI_UNIT ( $, .STERADIAN. ) SOLID_ANGLE_UNIT ( ) );
#5852=CARTESIAN_POINT ( 'NONE',  ( -29.77394335381484680, 8.177826981235281067, 42.10535821593507677 ) ) ;
#5869=CARTESIAN_POINT ( 'NONE',  ( -5.290067270632216712, -1.200000000000000030E-05, 8.531152949374556371 ) ) ;
#5875=CARTESIAN_POINT ( 'NONE',  ( 0.000000000000000000, 25.16329480281783759, -46.61112130868859538 ) ) ;
#5876=ORIENTED_EDGE ( 'NONE', *, *, #27936, .F. ) ;
#5877=FACE_OUTER_BOUND ( 'NONE', #76338, .T. ) ;
#5889=EDGE_LOOP ( 'NONE', ( #14627, #105460 ) ) ;
#5900=DIRECTION ( 'NONE',  ( -0.000000000000000000, 1.000000000000000000, 0.000000000000000000 ) ) ;
#5901=CARTESIAN_POINT ( 'NONE',  ( 0.1682410636899299150, 27.29656849860388235, -40.74999999999998579 ) ) ;
#5914=CARTESIAN_POINT ( 'NONE',  ( -30.74966693359947811, 13.13370859069518204, -41.50962874632944022 ) ) ;
#5925=CARTESIAN_POINT ( 'NONE',  ( -0.4140825127594466304, 34.19547899467610819, 29.68239057791232938 ) ) ;
#5976=CARTESIAN_POINT ( 'NONE',  ( -29.09375146990846872, 9.378808818926360757, -41.96648843557836983 ) ) ;
#5981=CARTESIAN_POINT ( 'NONE',  ( 37.88408281519146925, 25.64317620387171814, 10.98673829482864406 ) ) ;
#5990=CARTESIAN_POINT ( 'NONE',  ( -28.65204159835574771, 18.70303032895464668, -40.14586416981832429 ) ) ;
#6007=LINE ( 'NONE', #14093, #97586 ) ;
#6013=CARTESIAN_POINT ( 'NONE',  ( 6.534102926715305237, 53.62242791884023063, -7.078184780914639873 ) ) ;
#6043=CARTESIAN_POINT ( 'NONE',  ( 11.07117956952415483, 45.30041971330287964, -15.14528042430110766 ) ) ;
#6071=CARTESIAN_POINT ( 'NONE',  ( 15.90885615318885016, 37.20836610827222302, 22.13023378396293239 ) ) ;
#6077=VECTOR ( 'NONE', #95314, 1000.000000000000000 ) ;
#6101=SURFACE_STYLE_USAGE ( .BOTH. , #47090 ) ;
#6111=FILL_AREA_STYLE_COLOUR ( '', #26962 ) ;
#6114=FILL_AREA_STYLE_COLOUR ( '', #53388 ) ;
#6118=CARTESIAN_POINT ( 'NONE',  ( -36.47968809679790780, 26.06923311369085638, 11.58333936845124690 ) ) ;
#6124=CARTESIAN_POINT ( 'NONE',  ( 38.64291280000707474, 27.44880098965157345, 11.54947501064066806 ) ) ;
#6174=CARTESIAN_POINT ( 'NONE',  ( -15.73298926836856992, 37.19132885152136936, 22.31337215277960695 ) ) ;
#6180=CARTESIAN_POINT ( 'NONE',  ( 0.3382058652630261508, 35.06838561256219577, 27.28521124779242157 ) ) ;
#6182=CARTESIAN_POINT ( 'NONE',  ( 26.49278565071599445, 36.83346926003848409, 9.908164042044147024 ) ) ;
#6184=ORIENTED_EDGE ( 'NONE', *, *, #42121, .F. ) ;
#6188=CARTESIAN_POINT ( 'NONE',  ( -4.650164881889539359, 52.18144192692520278, -6.194387419916259852 ) ) ;
#6190=UNCERTAINTY_MEASURE_WITH_UNIT (LENGTH_MEASURE( 1.000000000000000082E-05 ), #101582, 'distance_accuracy_value', 'NONE');
#6192=CARTESIAN_POINT ( 'NONE',  ( -0.3347025688926246745, 43.19007807389648690, -18.70729546860571446 ) ) ;
#6200=CARTESIAN_POINT ( 'NONE',  ( 22.10772461237692355, 26.03542649978865953, -31.35794278042768113 ) ) ;
#6208=CARTESIAN_POINT ( 'NONE',  ( 0.6406553905574651209, 54.23511180506763196, 7.923516270499307623 ) ) ;
#6213=DIRECTION ( 'NONE',  ( 0.000000000000000000, 0.000000000000000000, 1.000000000000000000 ) ) ;
#6219=ORIENTED_EDGE ( 'NONE', *, *, #93016, .F. ) ;
#6229=EDGE_LOOP ( 'NONE', ( #77598, #60893, #50809, #55908 ) ) ;
#6235=CARTESIAN_POINT ( 'NONE',  ( 47.03591514779354554, 18.70176887044719294, 14.84266952052376176 ) ) ;
#6303=CARTESIAN_POINT ( 'NONE',  ( 0.3383111667213267171, 25.18062061424821607, -40.71479504876042910 ) ) ;
#6311=( NAMED_UNIT ( * ) PLANE_ANGLE_UNIT ( ) SI_UNIT ( $, .RADIAN. ) );
#6314=FACE_OUTER_BOUND ( 'NONE', #32475, .T. ) ;
#6315=ADVANCED_FACE ( 'NONE', ( #3081 ), #53754, .F. ) ;
#6324=EDGE_CURVE ( 'NONE', #38799, #58472, #52683, .T. ) ;
#6329=CARTESIAN_POINT ( 'NONE',  ( -27.86871601328855874, 36.37495722881055826, 9.810583054065073583 ) ) ;
#6346=CYLINDRICAL_SURFACE ( 'NONE', #83658, 1.250000000000001110 ) ;
#6356=UNCERTAINTY_MEASURE_WITH_UNIT (LENGTH_MEASURE( 1.000000000000000082E-05 ), #52707, 'distance_accuracy_value', 'NONE');
#6366=VECTOR ( 'NONE', #63515, 1000.000000000000000 ) ;
#6370=CARTESIAN_POINT ( 'NONE',  ( -37.88646966148060358, 27.49864696007435683, 13.42567359854803932 ) ) ;
#6378=FILL_AREA_STYLE ('',( #73771 ) ) ;
#6381=CARTESIAN_POINT ( 'NONE',  ( 29.35512824071881255, 13.99081654327145507, 42.06953762909855499 ) ) ;
#6393=AXIS2_PLACEMENT_3D ( 'NONE', #52758, #68428, #2067 ) ;
#6410=CARTESIAN_POINT ( 'NONE',  ( -7.474625967136768523, 54.29719554478052146, -2.154566369991844699 ) ) ;
#6412=CYLINDRICAL_SURFACE ( 'NONE', #4454, 1.250000000000001110 ) ;
#6418=VERTEX_POINT ( 'NONE', #24071 ) ;
#6440=COLOUR_RGB ( '', 0.31764706, 0.68627451, 0.89019608) ;
#6441=CARTESIAN_POINT ( 'NONE',  ( -30.82851008854539998, 15.24887380073562504, -40.33969805263218689 ) ) ;
#6444=B_SPLINE_CURVE_WITH_KNOTS ( 'NONE', 3,
 ( #17132, #16046, #50525, #32796, #33863, #9011, #66735, #6892, #65668, #98551, #74280, #99078, #99620, #39812, #356, #40325, #106105, #24182, #57025, #24702 ),
 .UNSPECIFIED., .F., .F.,
 ( 4, 2, 2, 2, 2, 2, 2, 2, 2, 4 ),
 ( 0.007062422899244994931, 0.007566298266050987611, 0.008070173632856980292, 0.008322111316259981836, 0.008574048999662985115, 0.009077924366468989939, 0.009581799733274994763, 0.01008567510008100132, 0.01058955046688700441, 0.01109342583369301097 ),
 .UNSPECIFIED. ) ;
#6446=CARTESIAN_POINT ( 'NONE',  ( 48.69590189480657472, 13.58600142653058818, 16.66526863408493853 ) ) ;
#6451=CIRCLE ( 'NONE', #66761, 13.27631144943088515 ) ;
#6453=CARTESIAN_POINT ( 'NONE',  ( 4.271055963817978807, 52.15840228002415557, -6.537475947608907489 ) ) ;
#6456=DIRECTION ( 'NONE',  ( -0.000000000000000000, 1.000000000000000000, -0.000000000000000000 ) ) ;
#6473=CARTESIAN_POINT ( 'NONE',  ( 21.97741296367617991, 27.90380497738007293, 32.31715157276715189 ) ) ;
#6475=SURFACE_STYLE_USAGE ( .BOTH. , #64216 ) ;
#6476=CARTESIAN_POINT ( 'NONE',  ( 0.000000000000000000, 47.29617335651134624, 0.000000000000000000 ) ) ;
#6481=CARTESIAN_POINT ( 'NONE',  ( 23.21751746555303342, -1.200000000000000030E-05, 31.95617127781017075 ) ) ;
#6502=CARTESIAN_POINT ( 'NONE',  ( 26.94485550679278063, 34.53204227594014952, -10.05698433968635719 ) ) ;
#6517=CARTESIAN_POINT ( 'NONE',  ( -29.27130674176756031, 18.74791880384168863, -39.67321021315769514 ) ) ;
#6519=DIRECTION ( 'NONE',  ( 1.150791560227848297E-16, -0.3420201433256725987, 0.9396926207859068736 ) ) ;
#6534=COLOUR_RGB ( '', 0.40784314, 0.44705882, 0.49803922) ;
#6555=FACE_OUTER_BOUND ( 'NONE', #24199, .T. ) ;
#6573=CARTESIAN_POINT ( 'NONE',  ( 10.45066360978653641, 46.08369782028255202, -12.90779740156203914 ) ) ;
#6582=DIRECTION ( 'NONE',  ( 0.000000000000000000, 1.000000000000000000, 0.000000000000000000 ) ) ;
#6597=EDGE_CURVE ( 'NONE', #23687, #34601, #84307, .T. ) ;
#6627=CYLINDRICAL_SURFACE ( 'NONE', #95634, 1.250000000000001110 ) ;
#6639=CARTESIAN_POINT ( 'NONE',  ( -1.248782720325924522, 16.17015974394703903, -50.36890103335689162 ) ) ;
#6646=SURFACE_STYLE_FILL_AREA ( #47626 ) ;
#6661=CARTESIAN_POINT ( 'NONE',  ( 38.81498927201410254, 27.33046494171043861, 12.09893127910710220 ) ) ;
#6663=CARTESIAN_POINT ( 'NONE',  ( 10.85169291771124911, 43.18003339092611270, 15.27576842164405946 ) ) ;
#6670=LINE ( 'NONE', #30992, #28969 ) ;
#6689=AXIS2_PLACEMENT_3D ( 'NONE', #23700, #23166, #72226 ) ;
#6707=CARTESIAN_POINT ( 'NONE',  ( 27.85283950832558375, 34.47317612687007937, 7.792265204343589602 ) ) ;
#6724=DIRECTION ( 'NONE',  ( -0.000000000000000000, 1.000000000000000000, -0.000000000000000000 ) ) ;
#6725=B_SPLINE_CURVE_WITH_KNOTS ( 'NONE', 3,
 ( #90781, #73507, #8780, #32566, #16345, #8250, #106406, #16895, #50300, #72976, #49775, #98331, #9302, #65437, #49231, #652, #42212, #64906, #97790, #82677, #23954, #24487, #41164, #57323, #89719, #40621, #74045, #127, #65962, #41687, #33617, #66489 ),
 .UNSPECIFIED., .F., .F.,
 ( 4, 2, 2, 2, 2, 2, 2, 2, 2, 2, 2, 2, 2, 2, 2, 4 ),
 ( 0.01223842624040720820, 0.01316182229273521118, 0.01362352031889921961, 0.01408521834506322977, 0.01431606735814522705, 0.01454691637122722432, 0.01477776538430922160, 0.01500861439739121887, 0.01523946341047322656, 0.01547031242355523251, 0.01593201044971924440, 0.01639370847588325283, 0.01685540650204726473, 0.01777880255437528506, 0.01870219860670330886, 0.01962559465903132919 ),
 .UNSPECIFIED. ) ;
#6731=CARTESIAN_POINT ( 'NONE',  ( -24.35655756968438013, 25.22426415880443784, 32.47765811203136366 ) ) ;
#6732=VERTEX_POINT ( 'NONE', #67693 ) ;
#6733=EDGE_CURVE ( 'NONE', #54018, #67401, #98163, .T. ) ;
#6735=CARTESIAN_POINT ( 'NONE',  ( -1.102351293730349013, 43.39607531963768849, -18.11074648114046681 ) ) ;
#6738=DIRECTION ( 'NONE',  ( 0.000000000000000000, 0.000000000000000000, 1.000000000000000000 ) ) ;
#6752=CARTESIAN_POINT ( 'NONE',  ( -2.324561895696642773E-13, 53.39766064372246746, 10.25000000000230038 ) ) ;
#6778=CARTESIAN_POINT ( 'NONE',  ( 46.96293930799767224, 18.79139706470995108, 14.94845605815066136 ) ) ;
#6802=( LENGTH_UNIT ( ) NAMED_UNIT ( * ) SI_UNIT ( .MILLI., .METRE. ) );
#6821=CARTESIAN_POINT ( 'NONE',  ( -0.3380055730847335571, 53.40879994520549445, -10.21500750740870700 ) ) ;
#6845=CARTESIAN_POINT ( 'NONE',  ( 0.8403905909943980568, 25.95797979004243317, -38.57101967074649451 ) ) ;
#6864=CARTESIAN_POINT ( 'NONE',  ( -27.10511071441182906, 36.60571256639526894, 10.05698433968618488 ) ) ;
#6867=EDGE_CURVE ( 'NONE', #3716, #7616, #83995, .T. ) ;
#6876=CARTESIAN_POINT ( 'NONE',  ( 21.97273450119370963, 25.82538667424861245, 32.15393027124035541 ) ) ;
#6889=CARTESIAN_POINT ( 'NONE',  ( 10.28624191511809371, 45.38549880562041494, -15.40779740156171762 ) ) ;
#6892=CARTESIAN_POINT ( 'NONE',  ( -28.19190453213781566, 34.18019048552498163, -9.430186636756511476 ) ) ;
#6906=ORIENTED_EDGE ( 'NONE', *, *, #12047, .T. ) ;
#6917=( GEOMETRIC_REPRESENTATION_CONTEXT ( 3 ) GLOBAL_UNCERTAINTY_ASSIGNED_CONTEXT ( ( #105595 ) ) GLOBAL_UNIT_ASSIGNED_CONTEXT ( ( #11210, #10683, #60343 ) ) REPRESENTATION_CONTEXT ( 'NONE', 'WORKASPACE' ) );
#6918=EDGE_CURVE ( 'NONE', #50266, #77582, #74043, .T. ) ;
#6927=CARTESIAN_POINT ( 'NONE',  ( -28.23212443805781646, 36.30340067818252692, -9.354155958373395308 ) ) ;
#6938=VERTEX_POINT ( 'NONE', #76168 ) ;
#6942=CARTESIAN_POINT ( 'NONE',  ( 10.91084845930706670, 43.80514505252456559, -13.06319618974774954 ) ) ;
#6947=EDGE_LOOP ( 'NONE', ( #62730, #30411, #85038, #28426 ) ) ;
#6952=CARTESIAN_POINT ( 'NONE',  ( -47.14566430936581298, 12.03638540833422965, 16.50097935118110115 ) ) ;
#6955=ORIENTED_EDGE ( 'NONE', *, *, #36004, .F. ) ;
#6967=CARTESIAN_POINT ( 'NONE',  ( -1.012227586502681520, 25.34501299846268196, 40.25169118181511152 ) ) ;
#6969=AXIS2_PLACEMENT_3D ( 'NONE', #105752, #15678, #48567 ) ;
#6979=CARTESIAN_POINT ( 'NONE',  ( -17.71939945264027116, 43.32309323114717614, 4.750313492600014342 ) ) ;
#6981=CARTESIAN_POINT ( 'NONE',  ( 48.76802610285364636, 13.46002349908646600, 16.61772763643222106 ) ) ;
#7008=DIRECTION ( 'NONE',  ( 0.000000000000000000, 0.000000000000000000, 1.000000000000000000 ) ) ;
#7012=CARTESIAN_POINT ( 'NONE',  ( -16.42305555460499278, 34.33297338635910023, 24.27376821836415388 ) ) ;
#7014=ORIENTED_EDGE ( 'NONE', *, *, #50545, .F. ) ;
#7033=ORIENTED_EDGE ( 'NONE', *, *, #73524, .F. ) ;
#7043=CARTESIAN_POINT ( 'NONE',  ( -29.35352825446822678, 8.824359840618493322, -42.06917583815513240 ) ) ;
#7044=EDGE_CURVE ( 'NONE', #52941, #21651, #84274, .T. ) ;
#7053=DIRECTION ( 'NONE',  ( -0.000000000000000000, 1.000000000000000000, -0.000000000000000000 ) ) ;
#7067=ADVANCED_FACE ( 'NONE', ( #34696 ), #2269, .F. ) ;
#7073=CARTESIAN_POINT ( 'NONE',  ( 29.68315524076925982, 18.29184282782464166, -39.60535821593530414 ) ) ;
#7081=STYLED_ITEM ( 'NONE', ( #92364 ), #7853 ) ;
#7083=EDGE_CURVE ( 'NONE', #16331, #62158, #81478, .T. ) ;
#7108=CARTESIAN_POINT ( 'NONE',  ( 11.36508313652854163, 45.70357710343880342, -13.50657646266327383 ) ) ;
#7136=CARTESIAN_POINT ( 'NONE',  ( 0.3381961372621271056, 43.18747244270107188, -18.71485033559731548 ) ) ;
#7137=CARTESIAN_POINT ( 'NONE',  ( -37.88481199253353537, 25.64605156355563054, 10.95617127781058997 ) ) ;
#7139=CARTESIAN_POINT ( 'NONE',  ( 37.56673239365841255, 25.47613764497371136, -13.45617127781092215 ) ) ;
#7142=FACE_BOUND ( 'NONE', #92578, .T. ) ;
#7154=( NAMED_UNIT ( * ) PLANE_ANGLE_UNIT ( ) SI_UNIT ( $, .RADIAN. ) );
#7160=CARTESIAN_POINT ( 'NONE',  ( -38.69367500482761812, 27.29977269400058049, -12.75349522650845202 ) ) ;
#7176=FACE_OUTER_BOUND ( 'NONE', #86838, .T. ) ;
#7181=CARTESIAN_POINT ( 'NONE',  ( 0.4143732981959021844, 52.15072962189677952, -7.817691439387481012 ) ) ;
#7204=CARTESIAN_POINT ( 'NONE',  ( -9.324472166507712600, 51.33783191909205357, -3.783589396988578102 ) ) ;
#7205=CARTESIAN_POINT ( 'NONE',  ( -6.465258847094798256, 53.70062699890282687, 6.847807190413986334 ) ) ;
#7249=CARTESIAN_POINT ( 'NONE',  ( -4.331568300327791832, 52.16491803293271801, -6.474400360773702623 ) ) ;
#7255=CARTESIAN_POINT ( 'NONE',  ( 0.3383419327415344013, 51.28045727062713866, 10.21496599268967387 ) ) ;
#7257=CARTESIAN_POINT ( 'NONE',  ( -16.75187969033531132, 34.25544727262101219, -24.30698433968676753 ) ) ;
#7265=CARTESIAN_POINT ( 'NONE',  ( 47.44718022415288772, 11.18620753528884748, -16.71882890723522053 ) ) ;
#7272=LINE ( 'NONE', #32658, #40148 ) ;
#7281=CARTESIAN_POINT ( 'NONE',  ( 29.85247340496056268, 12.86254483752417954, 39.61457847635354312 ) ) ;
#7296=CARTESIAN_POINT ( 'NONE',  ( 47.90443661882645898, 17.06459462766588331, 14.35535821593427386 ) ) ;
#7325=CARTESIAN_POINT ( 'NONE',  ( 1.249688359482191702, 45.80160873406245514, -17.33761737426925720 ) ) ;
#7342=CARTESIAN_POINT ( 'NONE',  ( -30.04499556692276840, 7.904673525308127502, -42.05327650403284423 ) ) ;
#7354=FILL_AREA_STYLE_COLOUR ( '', #80280 ) ;
#7359=FACE_OUTER_BOUND ( 'NONE', #55272, .T. ) ;
#7393=ADVANCED_FACE ( 'NONE', ( #71015 ), #80156, .F. ) ;
#7420=UNCERTAINTY_MEASURE_WITH_UNIT (LENGTH_MEASURE( 1.000000000000000082E-05 ), #62957, 'distance_accuracy_value', 'NONE');
#7434=CARTESIAN_POINT ( 'NONE',  ( 8.559508646656350805, -1.200000000000000030E-05, -2.781152949374623873 ) ) ;
#7436=CARTESIAN_POINT ( 'NONE',  ( 28.72970484482231157, 18.79180695567419335, 40.04448862869247705 ) ) ;
#7443=CARTESIAN_POINT ( 'NONE',  ( -16.03025389958261471, 43.70290146489438854, -6.508476644219860496 ) ) ;
#7444=CARTESIAN_POINT ( 'NONE',  ( -28.04619325667753671, 36.33495877514008754, -9.633940839559739899 ) ) ;
#7455=EDGE_CURVE ( 'NONE', #1846, #17567, #24788, .T. ) ;
#7459=STYLED_ITEM ( 'NONE', ( #87569 ), #21810 ) ;
#7469=CARTESIAN_POINT ( 'NONE',  ( -17.89653557359973135, 45.30873500717390101, 5.550246105160095311 ) ) ;
#7476=STYLED_ITEM ( 'NONE', ( #63430 ), #97074 ) ;
#7478=FILL_AREA_STYLE_COLOUR ( '', #69112 ) ;
#7487=CARTESIAN_POINT ( 'NONE',  ( -1.250037319930029422, 25.67361690534498209, 39.34156006938558647 ) ) ;
#7488=CARTESIAN_POINT ( 'NONE',  ( 0.3381493856820239063, 28.19327355359043707, -38.28513279055599838 ) ) ;
#7509=CARTESIAN_POINT ( 'NONE',  ( -28.45522292534199238, 11.90502831567347108, 41.11935372236940367 ) ) ;
#7516=CARTESIAN_POINT ( 'NONE',  ( 36.80507370451574189, 28.12589318819196649, -11.20093102687100917 ) ) ;
#7520=CARTESIAN_POINT ( 'NONE',  ( 28.34305552550043572, 34.21798169499945175, -8.615066575622451595 ) ) ;
#7526=CARTESIAN_POINT ( 'NONE',  ( 23.13516888326557108, 27.39820858062318365, 33.20617127781017786 ) ) ;
#7532=CIRCLE ( 'NONE', #81357, 35.82893434829263413 ) ;
#7534=ORIENTED_EDGE ( 'NONE', *, *, #35573, .F. ) ;
#7540=ORIENTED_EDGE ( 'NONE', *, *, #43975, .F. ) ;
#7554=CARTESIAN_POINT ( 'NONE',  ( -27.10511071441192144, -1.200000000000000030E-05, -10.05698433968589178 ) ) ;
#7562=CARTESIAN_POINT ( 'NONE',  ( 0.000000000000000000, -1.200000000000000030E-05, 9.000000000000000000 ) ) ;
#7592=CARTESIAN_POINT ( 'NONE',  ( 29.59455828143345002, 18.41848238274120675, -39.60535821593530414 ) ) ;
#7601=SURFACE_STYLE_USAGE ( .BOTH. , #39478 ) ;
#7616=VERTEX_POINT ( 'NONE', #13166 ) ;
#7632=CARTESIAN_POINT ( 'NONE',  ( 17.39155808811583981, 43.47117665187093394, -4.393666077417568872 ) ) ;
#7635=CARTESIAN_POINT ( 'NONE',  ( -5.290067270632214047, 53.47475093287474124, -8.531152949374821048 ) ) ;
#7651=CARTESIAN_POINT ( 'NONE',  ( 29.68315524076925982, 18.29184282782464166, -39.60535821593530414 ) ) ;
#7662=( LENGTH_UNIT ( ) NAMED_UNIT ( * ) SI_UNIT ( .MILLI., .METRE. ) );
#7671=CARTESIAN_POINT ( 'NONE',  ( -21.97121321732668520, 28.05118154993451896, -31.83013537814909100 ) ) ;
#7679=CIRCLE ( 'NONE', #67980, 63.00000000000000000 ) ;
#7681=COLOUR_RGB ( '', 0.09019608, 0.27058824, 0.51372549) ;
#7703=ORIENTED_EDGE ( 'NONE', *, *, #34461, .T. ) ;
#7713=CARTESIAN_POINT ( 'NONE',  ( 11.12982131476287151, 43.17719099323872456, 15.08403851094887393 ) ) ;
#7723=B_SPLINE_CURVE_WITH_KNOTS ( 'NONE', 3,
 ( #89340, #74191, #48320, #75252, #1353, #34315, #81214, #270, #33237, #25153, #19740, #26236, #83886, #12121, #100601, #42905, #27301, #100069, #35922, #101141, #10525, #52577, #51517, #35380, #10000, #3515, #84961, #11047, #84435, #2433 ),
 .UNSPECIFIED., .F., .F.,
 ( 4, 2, 2, 2, 2, 2, 2, 2, 2, 2, 2, 2, 2, 2, 4 ),
 ( 0.01423689679755356548, 0.01470129771271625439, 0.01493349817029759712, 0.01516569862787893984, 0.01539789908546028256, 0.01563009954304162355, 0.01586230000062296627, 0.01609450045820430900, 0.01655890137336699444, 0.01702330228852967989, 0.01795210411885506466, 0.01888090594918044943, 0.01980970777950582726, 0.02073850960983120856, 0.02166731144015658639 ),
 .UNSPECIFIED. ) ;
#7728=CARTESIAN_POINT ( 'NONE',  ( -9.538807954918411269, 51.45370039332727430, -1.987949993770493640 ) ) ;
#7736=ORIENTED_EDGE ( 'NONE', *, *, #39875, .F. ) ;
#7761=CARTESIAN_POINT ( 'NONE',  ( 27.71747584658618990, 34.52906169721746465, 7.705713108082328233 ) ) ;
#7794=CARTESIAN_POINT ( 'NONE',  ( 47.36504548439808104, 12.99580092579926394, -14.54285468146550286 ) ) ;
#7800=CARTESIAN_POINT ( 'NONE',  ( 0.8381057929850254107, 54.17571162905289839, 8.069066988206341051 ) ) ;
#7809=CARTESIAN_POINT ( 'NONE',  ( 30.82780738024936795, 10.08347807711982647, 40.33814864067983308 ) ) ;
#7812=CARTESIAN_POINT ( 'NONE',  ( 9.538609665898690082, 51.45378591545190972, -1.987744869269434167 ) ) ;
#7815=EDGE_CURVE ( 'NONE', #56223, #95054, #37616, .T. ) ;
#7816=DIRECTION ( 'NONE',  ( -0.000000000000000000, -1.000000000000000000, -0.000000000000000000 ) ) ;
#7826=CARTESIAN_POINT ( 'NONE',  ( 46.86404804693373194, 18.87323894068634544, 15.14441118170455702 ) ) ;
#7852=EDGE_CURVE ( 'NONE', #56430, #653, #92970, .T. ) ;
#7853=ADVANCED_FACE ( 'NONE', ( #28751 ), #35780, .F. ) ;
#7871=CARTESIAN_POINT ( 'NONE',  ( 16.58796880667331664, 35.02769128435444657, 21.80698433968581185 ) ) ;
#7884=CARTESIAN_POINT ( 'NONE',  ( 48.02835407290504577, -1.200000000000000030E-05, -15.60535821593549954 ) ) ;
#7893=CARTESIAN_POINT ( 'NONE',  ( 10.11986806485398382, 46.15873290010524954, 12.90779740156148847 ) ) ;
#7905=CARTESIAN_POINT ( 'NONE',  ( -7.199040112754230057E-19, 54.30758622938872549, -7.749999999999999112 ) ) ;
#7922=ORIENTED_EDGE ( 'NONE', *, *, #77308, .T. ) ;
#7925=CARTESIAN_POINT ( 'NONE',  ( 24.35704318349077724, 25.22446577928139533, -32.47660146702440187 ) ) ;
#7957=CARTESIAN_POINT ( 'NONE',  ( 7.308187696580947801, 54.29028184318244143, -2.719951076200258555 ) ) ;
#7979=CARTESIAN_POINT ( 'NONE',  ( 0.000000000000000000, 43.19193163660326462, 0.000000000000000000 ) ) ;
#7982=FACE_OUTER_BOUND ( 'NONE', #24291, .T. ) ;
#7993=ORIENTED_EDGE ( 'NONE', *, *, #65157, .F. ) ;
#8026=CARTESIAN_POINT ( 'NONE',  ( -1.011932115878593219, 25.89208366899141822, 38.74812953189098153 ) ) ;
#8030=B_SPLINE_CURVE_WITH_KNOTS ( 'NONE', 3,
 ( #86999, #6573, #21747, #5526, #29838, #38970, #7108, #45999, #96667, #40023, #13604, #31432, #38451, #64308, #71843, #6043, #104212, #14131, #72894, #95605, #31944, #97179 ),
 .UNSPECIFIED., .F., .F.,
 ( 4, 2, 2, 2, 2, 2, 2, 2, 2, 2, 4 ),
 ( 0.004989850371616175867, 0.005493891472670150294, 0.005997932573724123854, 0.006501973674778097415, 0.007006014775832071842, 0.007258035326359059056, 0.007510055876886046269, 0.008014096977940018962, 0.008518138078993993390, 0.008770158629520980603, 0.009022179180047967817 ),
 .UNSPECIFIED. ) ;
#8041=CARTESIAN_POINT ( 'NONE',  ( -16.91676434013897889, 34.22373756221627161, -24.29887300997501143 ) ) ;
#8044=LINE ( 'NONE', #90033, #105303 ) ;
#8045=CARTESIAN_POINT ( 'NONE',  ( -6.528653810299468674, 51.53967708196228870, -6.914260884958386200 ) ) ;
#8052=B_SPLINE_CURVE_WITH_KNOTS ( 'NONE', 3,
 ( #70350, #80014, #95683, #31507, #87602, #5604, #55720, #64388, #72459, #6661, #47115, #23409, #62277, #6124, #95164, #48173, #29392, #78959, #54134, #96751 ),
 .UNSPECIFIED., .F., .F.,
 ( 4, 2, 2, 2, 2, 2, 2, 2, 2, 4 ),
 ( 0.003115351416494580722, 0.003619732534144853853, 0.004124113651795126984, 0.004628494769445400114, 0.005132875887095674113, 0.005385066445920808076, 0.005637257004745941172, 0.006141638122396208231, 0.006646019240046476158, 0.007150400357696743217 ),
 .UNSPECIFIED. ) ;
#8064=CARTESIAN_POINT ( 'NONE',  ( 27.42290749620547174, 34.64384839456566567, -7.587773793964464275 ) ) ;
#8087=CARTESIAN_POINT ( 'NONE',  ( -4.063605838664956948, 54.18614975339210105, 6.989214199201114752 ) ) ;
#8098=VERTEX_POINT ( 'NONE', #98207 ) ;
#8104=CARTESIAN_POINT ( 'NONE',  ( -28.56337834059306857, 13.37291324415824967, -40.29174292248585942 ) ) ;
#8106=CARTESIAN_POINT ( 'NONE',  ( 38.11263331122286502, 25.30373840940857733, 13.33358277375596934 ) ) ;
#8122=CARTESIAN_POINT ( 'NONE',  ( 4.080491234651538512, 53.97779284277786616, 7.633990763273022395 ) ) ;
#8126=CARTESIAN_POINT ( 'NONE',  ( -4.188615833753505768, 52.12906257371965779, 6.684248842317088268 ) ) ;
#8129=ORIENTED_EDGE ( 'NONE', *, *, #30072, .F. ) ;
#8136=CARTESIAN_POINT ( 'NONE',  ( 28.43341640144443616, 17.76796145515717384, -40.78017990900054457 ) ) ;
#8149=ORIENTED_EDGE ( 'NONE', *, *, #6867, .F. ) ;
#8157=CARTESIAN_POINT ( 'NONE',  ( 6.275044998973871913, 53.84125641896091707, 6.495149306109316178 ) ) ;
#8164=AXIS2_PLACEMENT_3D ( 'NONE', #22312, #20208, #44984 ) ;
#8182=CARTESIAN_POINT ( 'NONE',  ( 17.73120223245296856, 43.18351831125497853, -6.029418843961513730 ) ) ;
#8185=DIRECTION ( 'NONE',  ( -0.000000000000000000, 1.000000000000000000, -0.000000000000000000 ) ) ;
#8187=CARTESIAN_POINT ( 'NONE',  ( -24.43733964430245464, 27.40365649514079394, 32.24112188980101479 ) ) ;
#8199=CARTESIAN_POINT ( 'NONE',  ( -49.22360526642673051, 7.740778690624813940, -15.97911514197237004 ) ) ;
#8202=CARTESIAN_POINT ( 'NONE',  ( -37.56673239365849781, 25.47613764497371136, 13.45617127781066280 ) ) ;
#8209=PRESENTATION_STYLE_ASSIGNMENT (( #42171 ) ) ;
#8218=CARTESIAN_POINT ( 'NONE',  ( -22.37441460685026229, 28.20471216883542809, -31.02949312230854417 ) ) ;
#8230=( NAMED_UNIT ( * ) SI_UNIT ( $, .STERADIAN. ) SOLID_ANGLE_UNIT ( ) );
#8237=( LENGTH_UNIT ( ) NAMED_UNIT ( * ) SI_UNIT ( .MILLI., .METRE. ) );
#8242=CARTESIAN_POINT ( 'NONE',  ( 0.1685512285012792377, 34.17188553058026912, -29.75000000000017408 ) ) ;
#8250=CARTESIAN_POINT ( 'NONE',  ( 48.69610342378920365, 8.416294429711179248, 16.66514711138992766 ) ) ;
#8265=CARTESIAN_POINT ( 'NONE',  ( 36.95213568995131226, 25.70510572952699846, 13.30629215880022542 ) ) ;
#8277=EDGE_CURVE ( 'NONE', #78054, #84082, #70995, .T. ) ;
#8298=CARTESIAN_POINT ( 'NONE',  ( 28.32642421089389728, 34.16878765831202713, 9.122000601312000967 ) ) ;
#8301=B_SPLINE_CURVE_WITH_KNOTS ( 'NONE', 3,
 ( #5656, #64440, #4608, #97314, #29450, #54720, #58461, #90833, #17484, #24531, #99424, #8304, #25054, #89771, #105931, #41737, #8833, #16948, #56849, #41208 ),
 .UNSPECIFIED., .F., .F.,
 ( 4, 2, 2, 2, 2, 2, 2, 2, 2, 4 ),
 ( 0.007810650867913536757, 0.008315688271542333657, 0.008820725675171128821, 0.009073244376985522067, 0.009325763078799911843, 0.009830800482428691395, 0.01033583788605746748, 0.01084087528968624703, 0.01134591269331502485, 0.01185095009694380266 ),
 .UNSPECIFIED. ) ;
#8304=CARTESIAN_POINT ( 'NONE',  ( 15.39690552766064613, 44.03715051710484119, 5.599647415943061368 ) ) ;
#8315=CARTESIAN_POINT ( 'NONE',  ( -4.189401774500377762, 52.12935225592999444, -6.682816396052760233 ) ) ;
#8316=EDGE_LOOP ( 'NONE', ( #30025, #45259, #76709, #69377 ) ) ;
#8319=ORIENTED_EDGE ( 'NONE', *, *, #102147, .F. ) ;
#8321=CARTESIAN_POINT ( 'NONE',  ( 0.1699848995827469844, 52.17551178379408583, 7.758783086627383696 ) ) ;
#8325=CARTESIAN_POINT ( 'NONE',  ( 0.08468841732357029750, 45.30391365246045154, 18.75000000000001066 ) ) ;
#8330=CARTESIAN_POINT ( 'NONE',  ( -9.658328022721306638, 45.55814826547296548, 15.25063005797924021 ) ) ;
#8333=CARTESIAN_POINT ( 'NONE',  ( 47.14566430936571351, 12.03638540833419057, -16.50097935118144221 ) ) ;
#8341=CARTESIAN_POINT ( 'NONE',  ( 0.1686817482576933591, 53.39766064372319221, 10.25000000000005862 ) ) ;
#8347=ADVANCED_FACE ( 'NONE', ( #5877, #53903, #70633, #79775, #95435 ), #93331, .T. ) ;
#8350=CARTESIAN_POINT ( 'NONE',  ( 30.90161637171750897, 8.443258198712152662, 41.14563328228290118 ) ) ;
#8356=AXIS2_PLACEMENT_3D ( 'NONE', #17616, #32751, #34354 ) ;
#8388=CARTESIAN_POINT ( 'NONE',  ( -1.219174438273753269, 25.73254055012321118, -39.18059869567464659 ) ) ;
#8389=CARTESIAN_POINT ( 'NONE',  ( -9.773376050962504280, 53.39758879002604175, 3.091049154870361360 ) ) ;
#8393=CARTESIAN_POINT ( 'NONE',  ( -0.6444474511539225459, 44.02069286197071563, 16.41606151047013640 ) ) ;
#8411=CARTESIAN_POINT ( 'NONE',  ( 15.96818781713877122, 35.08569730947720444, 22.06864763194606738 ) ) ;
#8433=CARTESIAN_POINT ( 'NONE',  ( 9.268669127170699795, 46.19464124546547623, 13.41262564492488529 ) ) ;
#8449=SURFACE_STYLE_FILL_AREA ( #48893 ) ;
#8460=CARTESIAN_POINT ( 'NONE',  ( 47.36715592893483517, 12.99186701195487537, 14.54160185453288001 ) ) ;
#8471=EDGE_CURVE ( 'NONE', #13222, #95845, #68531, .T. ) ;
#8493=CARTESIAN_POINT ( 'NONE',  ( 7.739116699011762357, 54.23361630046057513, -1.834387929005254048 ) ) ;
#8500=CARTESIAN_POINT ( 'NONE',  ( -16.64348903516521005, -1.200000000000000030E-05, -5.407797401561534656 ) ) ;
#8510=CARTESIAN_POINT ( 'NONE',  ( 28.77636872657296863, 18.82904586931653768, 39.99174360897747960 ) ) ;
#8511=CARTESIAN_POINT ( 'NONE',  ( 23.21751746555144180, 27.38103382803512176, -33.20617127781698485 ) ) ;
#8534=CARTESIAN_POINT ( 'NONE',  ( -26.94399930113149466, 34.53233444631757010, 10.05698433968616001 ) ) ;
#8545=CARTESIAN_POINT ( 'NONE',  ( -46.79100380508925383, 13.36652303332998670, 15.81652940118016204 ) ) ;
#8550=ORIENTED_EDGE ( 'NONE', *, *, #33675, .T. ) ;
#8555=CARTESIAN_POINT ( 'NONE',  ( 15.88324666189021350, 46.12968798971461837, 4.401569153914933530 ) ) ;
#8563=CARTESIAN_POINT ( 'NONE',  ( -30.36547348172779692, 16.93923362554432899, 39.80091097816897161 ) ) ;
#8577=CARTESIAN_POINT ( 'NONE',  ( -17.39136371670011627, 43.47128242272506782, 4.393265579572654289 ) ) ;
#8579=CARTESIAN_POINT ( 'NONE',  ( 27.10511071441176867, -1.200000000000000030E-05, -7.556984339686343866 ) ) ;
#8593=CARTESIAN_POINT ( 'NONE',  ( 36.64247849049904460, 27.97083273922043389, -13.05156522269073882 ) ) ;
#8597=ORIENTED_EDGE ( 'NONE', *, *, #25694, .T. ) ;
#8622=FACE_BOUND ( 'NONE', #56341, .T. ) ;
#8626=ORIENTED_EDGE ( 'NONE', *, *, #101510, .F. ) ;
#8659=CARTESIAN_POINT ( 'NONE',  ( -4.330505743362791371, 52.16474262961963149, 6.475687689770104782 ) ) ;
#8716=CARTESIAN_POINT ( 'NONE',  ( -24.00241574749204432, 27.29294457708168409, 32.94367910540178457 ) ) ;
#8743=ORIENTED_EDGE ( 'NONE', *, *, #84944, .T. ) ;
#8744=CARTESIAN_POINT ( 'NONE',  ( 25.85221525804374920, 37.20477182923430348, -8.663606034466162953 ) ) ;
#8758=EDGE_CURVE ( 'NONE', #77582, #21651, #6451, .T. ) ;
#8762=CARTESIAN_POINT ( 'NONE',  ( -0.1547218309332313857, 18.85536929889913083, -49.25755043093464991 ) ) ;
#8769=EDGE_LOOP ( 'NONE', ( #53741, #38687 ) ) ;
#8778=CARTESIAN_POINT ( 'NONE',  ( 8.238386871430398273, 51.94821137183647863, 1.562230139517037486 ) ) ;
#8780=CARTESIAN_POINT ( 'NONE',  ( 48.28061695858884406, 9.217865022612262038, 16.83796839065893991 ) ) ;
#8786=( GEOMETRIC_REPRESENTATION_CONTEXT ( 3 ) GLOBAL_UNCERTAINTY_ASSIGNED_CONTEXT ( ( #58103 ) ) GLOBAL_UNIT_ASSIGNED_CONTEXT ( ( #75743, #56887, #89814 ) ) REPRESENTATION_CONTEXT ( 'NONE', 'WORKASPACE' ) );
#8791=SURFACE_SIDE_STYLE ('',( #41699 ) ) ;
#8798=CARTESIAN_POINT ( 'NONE',  ( 6.692326732991420724E-21, 18.87382441218278828, -49.25000000000000000 ) ) ;
#8824=ORIENTED_EDGE ( 'NONE', *, *, #52102, .T. ) ;
#8832=( NAMED_UNIT ( * ) PLANE_ANGLE_UNIT ( ) SI_UNIT ( $, .RADIAN. ) );
#8833=CARTESIAN_POINT ( 'NONE',  ( 16.02985501006017444, 43.70305530208896982, 6.508335557365128032 ) ) ;
#8836=CARTESIAN_POINT ( 'NONE',  ( -29.68315524077004852, -1.200000000000000030E-05, -40.85535821593474282 ) ) ;
#8839=DIRECTION ( 'NONE',  ( 0.000000000000000000, 0.000000000000000000, 1.000000000000000000 ) ) ;
#8847=CARTESIAN_POINT ( 'NONE',  ( -0.5340012606292878772, 13.17865866240859241, 51.63689604381274734 ) ) ;
#8855=CARTESIAN_POINT ( 'NONE',  ( 0.6252597638487128462, 13.29621446636062210, -51.58647352287361798 ) ) ;
#8863=CARTESIAN_POINT ( 'NONE',  ( -46.92723468898989125, 18.82863087225937448, -15.00902207511727404 ) ) ;
#8865=EDGE_LOOP ( 'NONE', ( #31554, #29797 ) ) ;
#8879=DIRECTION ( 'NONE',  ( 0.000000000000000000, -0.3420201433256733758, -0.9396926207859066515 ) ) ;
#8900=EDGE_CURVE ( 'NONE', #653, #56430, #101751, .T. ) ;
#8906=SURFACE_STYLE_USAGE ( .BOTH. , #1326 ) ;
#8914=CARTESIAN_POINT ( 'NONE',  ( 38.75698381667141490, 25.16721628702945424, -12.59717980438506224 ) ) ;
#8939=CARTESIAN_POINT ( 'NONE',  ( 16.12370107433553201, 34.43117400368613801, 24.14989126905659944 ) ) ;
#8976=CARTESIAN_POINT ( 'NONE',  ( 8.241142027370402801, 54.07563880005658774, 1.561398477666883888 ) ) ;
#9011=CARTESIAN_POINT ( 'NONE',  ( -28.04617107623481331, 34.20660251098871640, -9.634014743738612552 ) ) ;
#9015=B_SPLINE_CURVE_WITH_KNOTS ( 'NONE', 3,
 ( #80607, #97859, #46661, #104912, #89781, #31051, #79559, #63406, #23479, #5673, #71459, #6731, #104358, #15351, #30506, #48237, #39655, #96300, #22425, #72525 ),
 .UNSPECIFIED., .F., .F.,
 ( 4, 2, 2, 2, 2, 2, 2, 2, 2, 4 ),
 ( 0.006849800839412230336, 0.007353416717026173451, 0.007857032594640116566, 0.008864264349868001061, 0.009116072288674979124, 0.009367880227481957187, 0.009619688166288935249, 0.009871496105095911577, 0.01037511198270986770, 0.01087872786032382383 ),
 .UNSPECIFIED. ) ;
#9022=ADVANCED_FACE ( 'NONE', ( #47833 ), #64062, .F. ) ;
#9026=CARTESIAN_POINT ( 'NONE',  ( 17.99842623603791480, 36.44670248777274679, -23.18063615129692678 ) ) ;
#9036=MECHANICAL_DESIGN_GEOMETRIC_PRESENTATION_REPRESENTATION('',(#53857),#41770);
#9041=LINE ( 'NONE', #82943, #89730 ) ;
#9044=CARTESIAN_POINT ( 'NONE',  ( -29.27137781856736609, 18.74786498819646496, 39.67318581983477088 ) ) ;
#9053=FILL_AREA_STYLE ('',( #89985 ) ) ;
#9073=CARTESIAN_POINT ( 'NONE',  ( -47.90347347824249624, 10.05236241843093481, 16.85535821593516559 ) ) ;
#9087=CARTESIAN_POINT ( 'NONE',  ( -30.59538916938590702, 12.96143355072256753, 41.71318167414145961 ) ) ;
#9101=CARTESIAN_POINT ( 'NONE',  ( -16.64348903516517098, 43.47556584774767430, 6.657797401561654560 ) ) ;
#9117=CARTESIAN_POINT ( 'NONE',  ( 36.94526041798086169, 28.08663898282346949, -11.10947391786501193 ) ) ;
#9126=CARTESIAN_POINT ( 'NONE',  ( -1.010142498354813734, 46.02241059309989879, -16.74584960336704498 ) ) ;
#9135=CARTESIAN_POINT ( 'NONE',  ( 0.1685051182689021043, 36.30322183991232521, 29.74144779452618792 ) ) ;
#9154=EDGE_CURVE ( 'NONE', #59570, #96186, #51565, .T. ) ;
#9157=( NAMED_UNIT ( * ) PLANE_ANGLE_UNIT ( ) SI_UNIT ( $, .RADIAN. ) );
#9166=DIRECTION ( 'NONE',  ( 0.000000000000000000, 0.000000000000000000, 1.000000000000000000 ) ) ;
#9172=CARTESIAN_POINT ( 'NONE',  ( 4.329523338144593225, 54.29298348168710930, 6.476737974868277625 ) ) ;
#9182=ADVANCED_FACE ( 'NONE', ( #71463 ), #60752, .F. ) ;
#9209=CARTESIAN_POINT ( 'NONE',  ( -0.7844422002871876964, 53.48242548866619472, 9.987131087015052699 ) ) ;
#9213=EDGE_CURVE ( 'NONE', #101, #25485, #59350, .T. ) ;
#9234=DIRECTION ( 'NONE',  ( -0.000000000000000000, 1.000000000000000000, -0.000000000000000000 ) ) ;
#9249=VERTEX_POINT ( 'NONE', #47713 ) ;
#9253=CARTESIAN_POINT ( 'NONE',  ( 16.19972009820076053, 36.53460074923752643, 24.18132016187593081 ) ) ;
#9258=CARTESIAN_POINT ( 'NONE',  ( 16.80257523370087114, 45.55115703057131782, 6.650239426131699716 ) ) ;
#9265=EDGE_CURVE ( 'NONE', #66067, #59308, #10419, .T. ) ;
#9269=CARTESIAN_POINT ( 'NONE',  ( 26.94613272717667485, 36.94238820718163652, -7.556984339686274588 ) ) ;
#9271=FACE_OUTER_BOUND ( 'NONE', #21002, .T. ) ;
#9277=CARTESIAN_POINT ( 'NONE',  ( 29.68315524076925982, 18.29184282782464166, -39.60535821593530414 ) ) ;
#9282=PRESENTATION_STYLE_ASSIGNMENT (( #58924 ) ) ;
#9286=CARTESIAN_POINT ( 'NONE',  ( -16.75187969033532553, -1.200000000000000030E-05, 21.80698433968612093 ) ) ;
#9287=CARTESIAN_POINT ( 'NONE',  ( 10.45249458729220571, 46.08328249563464141, 12.90779740156148847 ) ) ;
#9301=COLOUR_RGB ( '', 0.40784314, 0.44705882, 0.49803922) ;
#9302=CARTESIAN_POINT ( 'NONE',  ( 49.13582233779577280, 7.783546568855205017, 16.18978396958228672 ) ) ;
#9304=CARTESIAN_POINT ( 'NONE',  ( 0.3342801499821536626, 44.06880204852024718, 16.29260926128794651 ) ) ;
#9315=SURFACE_STYLE_USAGE ( .BOTH. , #17450 ) ;
#9317=CARTESIAN_POINT ( 'NONE',  ( 9.083636026015101450, 43.76992373826562499, -14.50792011570289830 ) ) ;
#9322=ORIENTED_EDGE ( 'NONE', *, *, #59087, .F. ) ;
#9330=CARTESIAN_POINT ( 'NONE',  ( -15.66802374774660045, 43.86792895834400952, 6.193618902369640189 ) ) ;
#9346=FACE_BOUND ( 'NONE', #101062, .T. ) ;
#9355=DIRECTION ( 'NONE',  ( 1.150791560227848297E-16, -0.3420201433256725987, 0.9396926207859068736 ) ) ;
#9365=( GEOMETRIC_REPRESENTATION_CONTEXT ( 3 ) GLOBAL_UNCERTAINTY_ASSIGNED_CONTEXT ( ( #101586 ) ) GLOBAL_UNIT_ASSIGNED_CONTEXT ( ( #85448, #77353, #12072 ) ) REPRESENTATION_CONTEXT ( 'NONE', 'WORKASPACE' ) );
#9374=CARTESIAN_POINT ( 'NONE',  ( 0.7722239243178034007, 18.23336398057940499, -49.51275493678145523 ) ) ;
#9377=CARTESIAN_POINT ( 'NONE',  ( 23.05228496585736053, 26.02496755577630694, -30.70617127781075695 ) ) ;
#9379=CARTESIAN_POINT ( 'NONE',  ( -47.57405721301101664, 17.76112721455490373, -14.43871205879859687 ) ) ;
#9397=CARTESIAN_POINT ( 'NONE',  ( 9.781924074846555683, 51.26649690293741912, -3.092456821203221740 ) ) ;
#9408=CARTESIAN_POINT ( 'NONE',  ( 24.31833665363000918, 25.57798547635034581, 31.28409169986229443 ) ) ;
#9413=CARTESIAN_POINT ( 'NONE',  ( -36.56974102123706416, 28.18271022055501263, -11.43420612882628618 ) ) ;
#9420=B_SPLINE_CURVE_WITH_KNOTS ( 'NONE', 3,
 ( #53048, #84352, #10445, #76244, #27754, #52496, #92421, #68162, #69243, #43359, #36897, #102116, #51965, #102658, #76776, #100521, #11499, #2352, #28273, #44425, #85415, #20737 ),
 .UNSPECIFIED., .F., .F.,
 ( 4, 2, 2, 2, 2, 2, 2, 2, 2, 2, 4 ),
 ( 0.003020842387534908389, 0.003273441169516790126, 0.003526039951498671863, 0.003778638733480553600, 0.004031237515462435771, 0.004536435079426195775, 0.005041632643389954913, 0.005546830207353714917, 0.006052027771317474922, 0.006557225335281234926, 0.007062422899244994931 ),
 .UNSPECIFIED. ) ;
#9437=CARTESIAN_POINT ( 'NONE',  ( -1.011134924304563754, 43.89348651028122816, 16.74734961794866095 ) ) ;
#9446=DIRECTION ( 'NONE',  ( 0.000000000000000000, -0.9221233147934838614, -0.3868961001538753219 ) ) ;
#9447=B_SPLINE_CURVE_WITH_KNOTS ( 'NONE', 3,
 ( #85399, #53029, #3419, #43867, #99973, #83783, #76759, #85952, #67090, #51421, #18014, #9896, #67626, #93501, #19648, #35820, #42804, #34753, #12023, #52481, #68701, #10428, #44955, #68146, #28258, #11482, #44410, #1248, #43344, #101040 ),
 .UNSPECIFIED., .F., .F.,
 ( 4, 2, 2, 2, 2, 2, 2, 2, 2, 2, 2, 2, 2, 2, 4 ),
 ( 0.01036701337735790318, 0.01128271447499395834, 0.01219841557263001523, 0.01311411667026607039, 0.01357196721908409884, 0.01402981776790212555, 0.01448766831672015400, 0.01471659359112916995, 0.01494551886553818418, 0.01517444413994720187, 0.01540336941435621609, 0.01586121996317423760, 0.01631907051199225911, 0.01677692106081028062, 0.01769262215844630975 ),
 .UNSPECIFIED. ) ;
#9476=EDGE_LOOP ( 'NONE', ( #85383, #97446 ) ) ;
#9481=VECTOR ( 'NONE', #60677, 1000.000000000000000 ) ;
#9501=CARTESIAN_POINT ( 'NONE',  ( 8.559508646656407649, 53.96349637827586321, 1.531152949374444239 ) ) ;
#9510=CARTESIAN_POINT ( 'NONE',  ( 47.50656546823845616, 12.72630541683656702, 14.46671989142039472 ) ) ;
#9511=UNCERTAINTY_MEASURE_WITH_UNIT (LENGTH_MEASURE( 1.000000000000000082E-05 ), #65286, 'distance_accuracy_value', 'NONE');
#9518=STYLED_ITEM ( 'NONE', ( #8209 ), #63047 ) ;
#9521=CARTESIAN_POINT ( 'NONE',  ( -47.36715592893472859, 12.99186701195485938, -14.54160185453320331 ) ) ;
#9526=SURFACE_STYLE_FILL_AREA ( #344 ) ;
#9564=COLOUR_RGB ( '', 0.66274510, 0.83137255, 0.94901961) ;
#9587=EDGE_LOOP ( 'NONE', ( #76088, #8626, #71562, #64861 ) ) ;
#9608=ORIENTED_EDGE ( 'NONE', *, *, #27451, .F. ) ;
#9617=EDGE_CURVE ( 'NONE', #94562, #86521, #83774, .T. ) ;
#9632=ADVANCED_FACE ( 'NONE', ( #39271 ), #93912, .F. ) ;
#9671=EDGE_CURVE ( 'NONE', #88738, #14520, #5301, .T. ) ;
#9676=CARTESIAN_POINT ( 'NONE',  ( 15.42181578661909747, 44.08896874612430139, -5.093856415474347976 ) ) ;
#9679=CARTESIAN_POINT ( 'NONE',  ( -38.17791925832861466, 27.65688341279261664, 11.10440149930134091 ) ) ;
#9681=ORIENTED_EDGE ( 'NONE', *, *, #74405, .F. ) ;
#9707=( GEOMETRIC_REPRESENTATION_CONTEXT ( 3 ) GLOBAL_UNCERTAINTY_ASSIGNED_CONTEXT ( ( #68580 ) ) GLOBAL_UNIT_ASSIGNED_CONTEXT ( ( #104340, #8832, #16946 ) ) REPRESENTATION_CONTEXT ( 'NONE', 'WORKASPACE' ) );
#9709=CARTESIAN_POINT ( 'NONE',  ( 4.151327550446272774, 54.24139430477373480, 6.759075926815422797 ) ) ;
#9726=SURFACE_SIDE_STYLE ('',( #18948 ) ) ;
#9748=ORIENTED_EDGE ( 'NONE', *, *, #100472, .F. ) ;
#9770=CARTESIAN_POINT ( 'NONE',  ( -23.86089617542280550, 27.29447341560883089, 33.04113357524851580 ) ) ;
#9775=SURFACE_STYLE_FILL_AREA ( #17904 ) ;
#9806=( GEOMETRIC_REPRESENTATION_CONTEXT ( 3 ) GLOBAL_UNCERTAINTY_ASSIGNED_CONTEXT ( ( #94448 ) ) GLOBAL_UNIT_ASSIGNED_CONTEXT ( ( #6802, #48310, #80682 ) ) REPRESENTATION_CONTEXT ( 'NONE', 'WORKASPACE' ) );
#9815=CARTESIAN_POINT ( 'NONE',  ( -48.02835407290515946, 14.94086294439721030, 16.85535821593516559 ) ) ;
#9818=CARTESIAN_POINT ( 'NONE',  ( 10.91073407590456057, 45.93358294599330094, 13.06300009034433351 ) ) ;
#9844=( LENGTH_UNIT ( ) NAMED_UNIT ( * ) SI_UNIT ( .MILLI., .METRE. ) );
#9846=ORIENTED_EDGE ( 'NONE', *, *, #29456, .T. ) ;
#9848=SURFACE_STYLE_USAGE ( .BOTH. , #83737 ) ;
#9858=VERTEX_POINT ( 'NONE', #97469 ) ;
#9860=VECTOR ( 'NONE', #38116, 1000.000000000000000 ) ;
#9875=DIRECTION ( 'NONE',  ( 0.000000000000000000, 0.000000000000000000, 1.000000000000000000 ) ) ;
#9893=CARTESIAN_POINT ( 'NONE',  ( -10.85130948263470785, 43.18006360272092792, 15.27593722711275070 ) ) ;
#9896=CARTESIAN_POINT ( 'NONE',  ( -49.24354615586529604, 13.35554545791851666, 15.29900703100092407 ) ) ;
#9907=CARTESIAN_POINT ( 'NONE',  ( -5.124946335852966328, 51.37806724455837326, -8.531152949374570582 ) ) ;
#9909=CARTESIAN_POINT ( 'NONE',  ( -0.07780686506603742836, 18.87382441218277407, 49.24999999999999289 ) ) ;
#9913=CARTESIAN_POINT ( 'NONE',  ( -0.7814574642159710649, 43.98401667755953781, -16.51064847437958605 ) ) ;
#9915=CARTESIAN_POINT ( 'NONE',  ( 9.757377548409222196E-14, 52.17923068443732149, -7.749999999998994582 ) ) ;
#9920=CARTESIAN_POINT ( 'NONE',  ( 0.9433870083987758726, 17.83644259124481479, -49.67632658074430196 ) ) ;
#9923=CARTESIAN_POINT ( 'NONE',  ( -9.507180395705038478, 46.21450860196618038, 13.17662286211865386 ) ) ;
#9924=B_SPLINE_CURVE_WITH_KNOTS ( 'NONE', 3,
 ( #7635, #39512, #97713, #56173, #22810, #73971, #56721, #65365, #33025, #98257, #23332, #90709, #105291, #80998, #15744, #48627, #38977, #71850, #81513, #104756 ),
 .UNSPECIFIED., .F., .F.,
 ( 4, 2, 2, 2, 2, 2, 2, 2, 2, 4 ),
 ( 0.006900400531842612595, 0.007152251793637217671, 0.007404103055431822747, 0.007907805579021032899, 0.008411508102610243051, 0.008915210626199449734, 0.009418913149788658151, 0.009922615673377864834, 0.01042631819696707152, 0.01093002072055627993 ),
 .UNSPECIFIED. ) ;
#9943=EDGE_CURVE ( 'NONE', #6938, #12797, #16725, .T. ) ;
#9952=ORIENTED_EDGE ( 'NONE', *, *, #78245, .T. ) ;
#9962=AXIS2_PLACEMENT_3D ( 'NONE', #12630, #68781, #62806 ) ;
#9965=CARTESIAN_POINT ( 'NONE',  ( -37.56673239365971284, 27.88554838446211548, -10.95617127780556466 ) ) ;
#9966=LINE ( 'NONE', #74687, #82556 ) ;
#9980=CARTESIAN_POINT ( 'NONE',  ( 0.07750125733394593042, 7.746009256456432901, 51.75000000000002842 ) ) ;
#9984=CARTESIAN_POINT ( 'NONE',  ( 38.78101150684803144, 25.16816242078845534, -12.51454816041207785 ) ) ;
#10000=CARTESIAN_POINT ( 'NONE',  ( 30.55657801806797735, 16.37492758275030980, 39.95287151819740501 ) ) ;
#10002=( LENGTH_UNIT ( ) NAMED_UNIT ( * ) SI_UNIT ( .MILLI., .METRE. ) );
#10009=CARTESIAN_POINT ( 'NONE',  ( -30.80805190526311321, 8.074044156869284450, -41.40902236837665384 ) ) ;
#10026=ORIENTED_EDGE ( 'NONE', *, *, #33603, .F. ) ;
#10041=PRODUCT_DEFINITION_CONTEXT ( 'detailed design', #84455, 'design' ) ;
#10048=EDGE_LOOP ( 'NONE', ( #28503, #4995, #42626, #845 ) ) ;
#10055=CARTESIAN_POINT ( 'NONE',  ( -16.18722300313207896, 37.20509570188509940, -21.93860808728204859 ) ) ;
#10059=CARTESIAN_POINT ( 'NONE',  ( 46.77684132781884330, 13.57955522726353692, 15.57752954476143437 ) ) ;
#10060=CARTESIAN_POINT ( 'NONE',  ( 0.000000000000000000, 0.000000000000000000, 0.000000000000000000 ) ) ;
#10066=ORIENTED_EDGE ( 'NONE', *, *, #46407, .T. ) ;
#10068=CARTESIAN_POINT ( 'NONE',  ( -47.14545574308343845, 12.03700443135205056, -16.50078943917375796 ) ) ;
#10069=CARTESIAN_POINT ( 'NONE',  ( -36.58584895476980847, 25.86851599530958268, -12.99742464195551150 ) ) ;
#10074=FILL_AREA_STYLE_COLOUR ( '', #13939 ) ;
#10100=VECTOR ( 'NONE', #53201, 1000.000000000000000 ) ;
#10105=CARTESIAN_POINT ( 'NONE',  ( -8.559508646656370345, -1.200000000000000030E-05, 2.781152949374564365 ) ) ;
#10107=CARTESIAN_POINT ( 'NONE',  ( 16.18602784294493802, 35.07682394434411322, -21.93920426711484950 ) ) ;
#10108=SURFACE_STYLE_FILL_AREA ( #25821 ) ;
#10117=CARTESIAN_POINT ( 'NONE',  ( 1.637502573363885733E-19, 51.26930509877138320, -10.24999999999999822 ) ) ;
#10130=CARTESIAN_POINT ( 'NONE',  ( -10.28624191511820207, 45.38549880562041494, 15.40779740156164124 ) ) ;
#10132=LINE ( 'NONE', #58146, #11219 ) ;
#10136=SURFACE_STYLE_FILL_AREA ( #44654 ) ;
#10139=ORIENTED_EDGE ( 'NONE', *, *, #77742, .T. ) ;
#10152=CARTESIAN_POINT ( 'NONE',  ( 9.381644744338347053, 53.45431541546333420, 3.726433245770410796 ) ) ;
#10163=CARTESIAN_POINT ( 'NONE',  ( -7.943779790039141808, 51.78215888541748768, 3.880567839249599693 ) ) ;
#10172=CARTESIAN_POINT ( 'NONE',  ( 48.15057074821019256, 16.50253122541073125, 14.35535821593427386 ) ) ;
#10178=B_SPLINE_CURVE_WITH_KNOTS ( 'NONE', 3,
 ( #73829, #82992, #17739, #106723, #50599, #34486, #8563, #432, #75425, #1518, #41464, #41996, #49552, #59263, #50086, #98629, #74354, #99159, #82459, #33401, #9087, #43072, #57105, #66272, #25317, #84055, #74876, #33944, #67353, #40935 ),
 .UNSPECIFIED., .F., .F.,
 ( 4, 2, 2, 2, 2, 2, 2, 2, 2, 2, 2, 2, 2, 2, 4 ),
 ( 0.008103130636685088387, 0.008563624816068822476, 0.009024118995452558301, 0.009945107354220028215, 0.01086609571298749813, 0.01178708407175496631, 0.01270807243052244143, 0.01316856660990617899, 0.01362906078928991654, 0.01408955496867365237, 0.01431980205836551334, 0.01455004914805737085, 0.01478029623774923182, 0.01501054332744109106, 0.01547103750682481647 ),
 .UNSPECIFIED. ) ;
#10180=CARTESIAN_POINT ( 'NONE',  ( 0.1691555275570714445, 46.21383923812596350, -16.25000000000000000 ) ) ;
#10199=EDGE_CURVE ( 'NONE', #91282, #104078, #79057, .T. ) ;
#10215=VECTOR ( 'NONE', #22991, 1000.000000000000000 ) ;
#10240=EDGE_CURVE ( 'NONE', #66410, #5108, #60720, .T. ) ;
#10253=VERTEX_POINT ( 'NONE', #82227 ) ;
#10255=CARTESIAN_POINT ( 'NONE',  ( 28.32636678626138504, 36.29712012945766020, 9.122391396881491588 ) ) ;
#10272=ORIENTED_EDGE ( 'NONE', *, *, #8471, .F. ) ;
#10274=LINE ( 'NONE', #77145, #4464 ) ;
#10277=DIRECTION ( 'NONE',  ( 0.000000000000000000, 0.000000000000000000, 1.000000000000000000 ) ) ;
#10282=CARTESIAN_POINT ( 'NONE',  ( -2.324561895696642773E-13, 53.39766064372246746, 10.25000000000230038 ) ) ;
#10294=CARTESIAN_POINT ( 'NONE',  ( -29.68315524077005207, 13.47185074185902209, -42.10535821593474282 ) ) ;
#10301=CARTESIAN_POINT ( 'NONE',  ( -0.6462866794873234344, 37.14682203640808211, -27.41685252655225113 ) ) ;
#10302=CARTESIAN_POINT ( 'NONE',  ( 0.000000000000000000, -1.200000000000000030E-05, -17.50000000000000000 ) ) ;
#10304=CARTESIAN_POINT ( 'NONE',  ( 23.21751746555220564, -1.200000000000000030E-05, -33.20617127781077471 ) ) ;
#10306=DIRECTION ( 'NONE',  ( 0.000000000000000000, 0.000000000000000000, 1.000000000000000000 ) ) ;
#10308=UNCERTAINTY_MEASURE_WITH_UNIT (LENGTH_MEASURE( 1.000000000000000082E-05 ), #12986, 'distance_accuracy_value', 'NONE');
#10313=CARTESIAN_POINT ( 'NONE',  ( -0.3377801289881405822, 46.20008771969307304, 16.28498333803777598 ) ) ;
#10333=DIRECTION ( 'NONE',  ( 0.000000000000000000, 1.000000000000000000, 0.000000000000000000 ) ) ;
#10336=CARTESIAN_POINT ( 'NONE',  ( 26.18069599319563068, 36.97239296640589146, -9.652207212211994403 ) ) ;
#10343=UNCERTAINTY_MEASURE_WITH_UNIT (LENGTH_MEASURE( 1.000000000000000082E-05 ), #104, 'distance_accuracy_value', 'NONE');
#10346=VERTEX_POINT ( 'NONE', #101617 ) ;
#10354=LINE ( 'NONE', #9286, #70925 ) ;
#10367=DIRECTION ( 'NONE',  ( 0.000000000000000000, -0.000000000000000000, 1.000000000000000000 ) ) ;
#10368=CARTESIAN_POINT ( 'NONE',  ( 7.808540133805411010, 51.84039965102822833, 3.793121522970396065 ) ) ;
#10369=CARTESIAN_POINT ( 'NONE',  ( 0.000000000000000000, 0.000000000000000000, 13.27631144943088515 ) ) ;
#10372=CARTESIAN_POINT ( 'NONE',  ( 1.010771448917421544, 43.89380339074816817, 16.74650787413497355 ) ) ;
#10377=CARTESIAN_POINT ( 'NONE',  ( -7.370387608271186330, 52.18044071326720967, -2.386534409371826371 ) ) ;
#10380=VECTOR ( 'NONE', #49909, 1000.000000000000000 ) ;
#10382=CARTESIAN_POINT ( 'NONE',  ( -0.07775081836201770680, 7.746009256456749092, -51.74999999999986500 ) ) ;
#10386=CARTESIAN_POINT ( 'NONE',  ( 10.28624191511809371, 43.99263840937192782, -12.90779740156171407 ) ) ;
#10389=B_SPLINE_CURVE_WITH_KNOTS ( 'NONE', 3,
 ( #9277, #43259, #77219, #3331, #42184, #75615, #59457, #35192, #43783, #35734, #92325, #92859, #19027, #20637, #103096, #53477, #96061, #4388, #85867, #55044, #12992, #104135, #30279, #86399, #53981, #95524, #21151, #71238, #22193, #46958 ),
 .UNSPECIFIED., .F., .F.,
 ( 4, 2, 2, 2, 2, 2, 2, 2, 2, 2, 2, 2, 2, 2, 4 ),
 ( 0.008103130636685064100, 0.008563624816068786047, 0.009024118995452509728, 0.009945107354219958826, 0.01086609571298740792, 0.01178708407175485702, 0.01270807243052230612, 0.01316856660990603500, 0.01362906078928976215, 0.01408955496867348930, 0.01431980205836536416, 0.01455004914805723901, 0.01478029623774911386, 0.01501054332744098871, 0.01547103750682472800 ),
 .UNSPECIFIED. ) ;
#10391=CARTESIAN_POINT ( 'NONE',  ( -5.290067270632214047, 53.47475093287474124, -8.531152949374821048 ) ) ;
#10399=CIRCLE ( 'NONE', #19083, 24.55262289886175964 ) ;
#10419=B_SPLINE_CURVE_WITH_KNOTS ( 'NONE', 3,
 ( #105437, #47185, #80085, #6192, #39128, #104917, #31576, #63935, #6735, #96823, #22953, #39658, #80612, #43360, #76245, #9913, #25622, #98910, #16967, #35293, #2353, #18032 ),
 .UNSPECIFIED., .F., .F.,
 ( 4, 2, 2, 2, 2, 2, 2, 2, 2, 2, 4 ),
 ( 0.007315589541698120334, 0.007567575265297590316, 0.007819560988897061166, 0.008323532436096002865, 0.008827503883294946299, 0.009331475330493889733, 0.009835446777692833167, 0.01033941822489177487, 0.01084338967209071830, 0.01109537539569019002, 0.01134736111928966174 ),
 .UNSPECIFIED. ) ;
#10426=CARTESIAN_POINT ( 'NONE',  ( -11.54058046252955627, 43.31680132832994445, 14.28235035768446082 ) ) ;
#10428=CARTESIAN_POINT ( 'NONE',  ( -48.98918515124638162, 13.11539385479550113, 16.41516879933075046 ) ) ;
#10445=CARTESIAN_POINT ( 'NONE',  ( -26.94610874357095298, 34.81329346479147802, -7.564552669781196670 ) ) ;
#10455=CARTESIAN_POINT ( 'NONE',  ( -46.97290287162347511, 17.76084728355517584, -16.28892042402491924 ) ) ;
#10456=EDGE_LOOP ( 'NONE', ( #57486, #62517, #89486, #11686 ) ) ;
#10473=CARTESIAN_POINT ( 'NONE',  ( 48.15129163819126035, 9.495040186444088093, -16.85535821593549954 ) ) ;
#10476=ORIENTED_EDGE ( 'NONE', *, *, #38880, .F. ) ;
#10491=AXIS2_PLACEMENT_3D ( 'NONE', #73821, #56564, #40394 ) ;
#10493=CARTESIAN_POINT ( 'NONE',  ( 6.429306121731439561, 51.32037123737740103, -7.802259468956040500 ) ) ;
#10500=EDGE_CURVE ( 'NONE', #52941, #9249, #78393, .T. ) ;
#10501=DIRECTION ( 'NONE',  ( 0.000000000000000000, 0.000000000000000000, 1.000000000000000000 ) ) ;
#10508=ADVANCED_FACE ( 'NONE', ( #62757 ), #78922, .F. ) ;
#10509=CARTESIAN_POINT ( 'NONE',  ( 1.235549969621061006, 10.15115531407437999, 50.72583874370463519 ) ) ;
#10512=CARTESIAN_POINT ( 'NONE',  ( 37.88767513972955214, 25.36992872674205657, -13.42525127874668023 ) ) ;
#10514=CONICAL_SURFACE ( 'NONE', #36372, 33.82893434829263413, 1.221730476396026610 ) ;
#10525=CARTESIAN_POINT ( 'NONE',  ( 30.90725857724351044, 14.69157187025844813, 40.57373053090514503 ) ) ;
#10535=CARTESIAN_POINT ( 'NONE',  ( 1.011751391879055717, 27.47325995063050641, 40.25199818947412211 ) ) ;
#10536=CARTESIAN_POINT ( 'NONE',  ( -30.92868852183901396, 8.704894651777072667, -40.98784967800754941 ) ) ;
#10552=DIRECTION ( 'NONE',  ( -0.000000000000000000, -1.000000000000000000, -0.000000000000000000 ) ) ;
#10555=VECTOR ( 'NONE', #63961, 1000.000000000000000 ) ;
#10562=PRESENTATION_STYLE_ASSIGNMENT (( #27876 ) ) ;
#10570=VECTOR ( 'NONE', #93807, 1000.000000000000000 ) ;
#10572=UNCERTAINTY_MEASURE_WITH_UNIT (LENGTH_MEASURE( 1.000000000000000082E-05 ), #64046, 'distance_accuracy_value', 'NONE');
#10575=CARTESIAN_POINT ( 'NONE',  ( 7.808293529262138932, 53.96887308738315880, 3.792886552870250672 ) ) ;
#10593=CARTESIAN_POINT ( 'NONE',  ( -36.47299678459301475, 26.07223862938034387, -11.57805873600646329 ) ) ;
#10601=ORIENTED_EDGE ( 'NONE', *, *, #8758, .F. ) ;
#10608=CARTESIAN_POINT ( 'NONE',  ( 29.33080127677424187, 13.52978328598926971, -39.65469037846457212 ) ) ;
#10609=CARTESIAN_POINT ( 'NONE',  ( 17.81928184698852746, 45.39461501854594161, -4.975624619099646928 ) ) ;
#10624=CARTESIAN_POINT ( 'NONE',  ( 17.51195277503147452, 36.87917477456677062, -22.05183216906725363 ) ) ;
#10628=CYLINDRICAL_SURFACE ( 'NONE', #53890, 1.250000000000000000 ) ;
#10649=CARTESIAN_POINT ( 'NONE',  ( -1.100802702663628896, 27.96907460577615012, 38.88676574253319274 ) ) ;
#10650=CARTESIAN_POINT ( 'NONE',  ( 4.387778976649723378E-15, 29.08768991669519721, -35.82893434829263413 ) ) ;
#10672=CARTESIAN_POINT ( 'NONE',  ( 15.56661972382058501, 46.04807679453924152, 6.063442319127587687 ) ) ;
#10683=( NAMED_UNIT ( * ) PLANE_ANGLE_UNIT ( ) SI_UNIT ( $, .RADIAN. ) );
#10711=ORIENTED_EDGE ( 'NONE', *, *, #44818, .T. ) ;
#10722=CARTESIAN_POINT ( 'NONE',  ( -24.42503034277509499, 25.46443454461794076, -31.59611462731667331 ) ) ;
#10728=AXIS2_PLACEMENT_3D ( 'NONE', #14983, #57033, #47878 ) ;
#10743=FACE_OUTER_BOUND ( 'NONE', #37690, .T. ) ;
#10751=EDGE_CURVE ( 'NONE', #1743, #15047, #42744, .T. ) ;
#10784=SURFACE_STYLE_USAGE ( .BOTH. , #36195 ) ;
#10814=ORIENTED_EDGE ( 'NONE', *, *, #103889, .T. ) ;
#10817=CARTESIAN_POINT ( 'NONE',  ( 36.32858960327170905, 26.02883040073359666, -12.39689931504920395 ) ) ;
#10819=CARTESIAN_POINT ( 'NONE',  ( -0.7827516548123796269, 37.11091899138959604, -27.51176826853287594 ) ) ;
#10826=CARTESIAN_POINT ( 'NONE',  ( -15.39075092899651942, 46.20845424323130146, -5.262406961020227314 ) ) ;
#10838=CARTESIAN_POINT ( 'NONE',  ( -48.80467726777875015, 9.660151405757225973, -14.61811727277458495 ) ) ;
#10864=DIRECTION ( 'NONE',  ( 0.000000000000000000, 1.000000000000000000, -0.000000000000000000 ) ) ;
#10872=CARTESIAN_POINT ( 'NONE',  ( -0.3577666611213474179, 18.74973685375030641, -49.30079757914840854 ) ) ;
#10876=CARTESIAN_POINT ( 'NONE',  ( 16.96276686007057322, 43.64335858091297382, 4.157797401561411199 ) ) ;
#10890=SURFACE_STYLE_FILL_AREA ( #100452 ) ;
#10902=CARTESIAN_POINT ( 'NONE',  ( -1.107233591667432293, 12.11777053784344282, -49.90351304355277762 ) ) ;
#10913=DIRECTION ( 'NONE',  ( 0.000000000000000000, 1.000000000000000000, -0.000000000000000000 ) ) ;
#10914=MECHANICAL_DESIGN_GEOMETRIC_PRESENTATION_REPRESENTATION('',(#69550),#88487);
#10916=CARTESIAN_POINT ( 'NONE',  ( -9.721734870800478490, 46.20860777233757233, -13.03934063175032954 ) ) ;
#10921=CARTESIAN_POINT ( 'NONE',  ( -15.53402121140690184, 43.94041489164831660, 5.989367130121264537 ) ) ;
#10936=CARTESIAN_POINT ( 'NONE',  ( -0.1699168734760051480, 28.20319722039545596, -38.25876859947282327 ) ) ;
#10941=MECHANICAL_DESIGN_GEOMETRIC_PRESENTATION_REPRESENTATION('',(#76401),#103965);
#10942=CARTESIAN_POINT ( 'NONE',  ( 48.02835407290414338, 14.94086294439859408, -16.85535821593631667 ) ) ;
#10952=FILL_AREA_STYLE_COLOUR ( '', #6534 ) ;
#10956=ORIENTED_EDGE ( 'NONE', *, *, #41015, .T. ) ;
#10958=( GEOMETRIC_REPRESENTATION_CONTEXT ( 3 ) GLOBAL_UNCERTAINTY_ASSIGNED_CONTEXT ( ( #10343 ) ) GLOBAL_UNIT_ASSIGNED_CONTEXT ( ( #104, #49751, #49210 ) ) REPRESENTATION_CONTEXT ( 'NONE', 'WORKASPACE' ) );
#10959=CARTESIAN_POINT ( 'NONE',  ( 4.048442073968021582, 51.85559909576627291, -7.633306776926700898 ) ) ;
#10965=ORIENTED_EDGE ( 'NONE', *, *, #7852, .F. ) ;
#10982=CARTESIAN_POINT ( 'NONE',  ( -46.81266956378431843, 18.41561415511115740, -15.90959751601133831 ) ) ;
#10999=CARTESIAN_POINT ( 'NONE',  ( 49.09793955338178506, 7.820164633611708993, -16.25544133048972739 ) ) ;
#11016=CARTESIAN_POINT ( 'NONE',  ( -36.94654418156419950, 28.08625268104305661, -11.10888460376342124 ) ) ;
#11017=B_SPLINE_CURVE_WITH_KNOTS ( 'NONE', 3,
 ( #49645, #75518, #99795, #58825, #100323, #82553, #41561, #9172, #34038, #34574, #9709, #42085, #82003, #24352, #8122, #91717, #74444, #42619, #57196, #26484, #523, #17838, #33486, #99246 ),
 .UNSPECIFIED., .F., .F.,
 ( 4, 2, 2, 2, 2, 2, 2, 2, 2, 2, 2, 4 ),
 ( 0.007071253621610506558, 0.007323632620172739610, 0.007576011618734973529, 0.008080769615859441368, 0.008333148614421678757, 0.008585527612983914411, 0.009090285610108389189, 0.009595043607232863966, 0.01009980160435733701, 0.01060455960148180832, 0.01085693860004404571, 0.01110931759860628310 ),
 .UNSPECIFIED. ) ;
#11023=DIRECTION ( 'NONE',  ( 0.000000000000000000, 0.000000000000000000, -1.000000000000000000 ) ) ;
#11030=CARTESIAN_POINT ( 'NONE',  ( 0.5302602878479981685, 13.43200846721745023, 49.36160310769543713 ) ) ;
#11033=EDGE_CURVE ( 'NONE', #35979, #12685, #14779, .T. ) ;
#11042=( NAMED_UNIT ( * ) SI_UNIT ( $, .STERADIAN. ) SOLID_ANGLE_UNIT ( ) );
#11047=CARTESIAN_POINT ( 'NONE',  ( 30.00306714711529921, 17.76853250946123097, 39.63934773235497744 ) ) ;
#11049=( NAMED_UNIT ( * ) PLANE_ANGLE_UNIT ( ) SI_UNIT ( $, .RADIAN. ) );
#11056=CARTESIAN_POINT ( 'NONE',  ( 0.7847287007732014485, 27.38973784147641055, 40.48658148275971769 ) ) ;
#11057=CARTESIAN_POINT ( 'NONE',  ( -30.75880901179656846, 7.960713337733316131, -41.50491223544449326 ) ) ;
#11070=ORIENTED_EDGE ( 'NONE', *, *, #106748, .F. ) ;
#11072=DIRECTION ( 'NONE',  ( 0.000000000000000000, 0.000000000000000000, 1.000000000000000000 ) ) ;
#11090=UNCERTAINTY_MEASURE_WITH_UNIT (LENGTH_MEASURE( 1.000000000000000082E-05 ), #10002, 'distance_accuracy_value', 'NONE');
#11115=DIRECTION ( 'NONE',  ( -0.000000000000000000, 1.000000000000000000, -0.000000000000000000 ) ) ;
#11118=CARTESIAN_POINT ( 'NONE',  ( 5.612461429774295851, 54.11923096040738557, 6.070761239882453530 ) ) ;
#11129=CARTESIAN_POINT ( 'NONE',  ( 29.08094203968477487, 13.68582110885885861, -39.75724343093586555 ) ) ;
#11139=CARTESIAN_POINT ( 'NONE',  ( 0.000000000000000000, 0.000000000000000000, 0.000000000000000000 ) ) ;
#11141=EDGE_CURVE ( 'NONE', #60788, #38588, #51709, .T. ) ;
#11162=DIRECTION ( 'NONE',  ( 0.000000000000000000, 0.000000000000000000, -1.000000000000000000 ) ) ;
#11169=B_SPLINE_CURVE_WITH_KNOTS ( 'NONE', 3,
 ( #73665, #106568, #24627, #84440, #20282, #102206, #77404, #11587, #45054, #35386, #2437, #36980, #35927, #92513, #60189, #53133, #68253, #70380 ),
 .UNSPECIFIED., .F., .F.,
 ( 4, 2, 2, 2, 2, 2, 2, 2, 4 ),
 ( 0.002770935648931494456, 0.003276907721204434191, 0.003782879793477374360, 0.004794823938023257300, 0.005047809974159726300, 0.005300796010296196167, 0.005806768082569134168, 0.006312740154842072168, 0.006818712227115010169 ),
 .UNSPECIFIED. ) ;
#11177=CARTESIAN_POINT ( 'NONE',  ( 1.196618058419959393E-20, 36.30024107553216339, -29.75000000000000355 ) ) ;
#11190=CARTESIAN_POINT ( 'NONE',  ( -48.02835407290516656, 11.61227450977240494, 14.35535821593516559 ) ) ;
#11210=( LENGTH_UNIT ( ) NAMED_UNIT ( * ) SI_UNIT ( .MILLI., .METRE. ) );
#11219=VECTOR ( 'NONE', #93721, 1000.000000000000000 ) ;
#11227=CARTESIAN_POINT ( 'NONE',  ( 48.26750065955900482, 16.22349350713542293, 14.37287707152939120 ) ) ;
#11234=CARTESIAN_POINT ( 'NONE',  ( -11.42607455529675065, 43.22995051892015539, -14.67755458576255201 ) ) ;
#11235=CARTESIAN_POINT ( 'NONE',  ( -1.100561925788291262, 36.97067097995192597, 27.88635067314485028 ) ) ;
#11250=CARTESIAN_POINT ( 'NONE',  ( -24.17891642670491947, 25.18055287771648665, -32.75954025174772966 ) ) ;
#11270=CARTESIAN_POINT ( 'NONE',  ( -16.48376536647094781, 45.65789762114239636, 6.657797401561870387 ) ) ;
#11312=DIRECTION ( 'NONE',  ( -0.000000000000000000, -1.000000000000000000, -0.000000000000000000 ) ) ;
#11316=FACE_OUTER_BOUND ( 'NONE', #82783, .T. ) ;
#11324=CARTESIAN_POINT ( 'NONE',  ( 4.684274960302871098E-15, 26.07813853931757464, 38.25000000000000000 ) ) ;
#11357=CARTESIAN_POINT ( 'NONE',  ( -9.523678393152335886, 43.48341758817304026, -15.16113424488535344 ) ) ;
#11358=CARTESIAN_POINT ( 'NONE',  ( -16.02938566285134669, 45.83159863292935654, -6.508120059605710495 ) ) ;
#11371=CARTESIAN_POINT ( 'NONE',  ( -28.34317069729203098, 36.34622212941757624, 8.615775889579945002 ) ) ;
#11387=ORIENTED_EDGE ( 'NONE', *, *, #21653, .F. ) ;
#11399=SURFACE_STYLE_FILL_AREA ( #104136 ) ;
#11408=CARTESIAN_POINT ( 'NONE',  ( 17.37570930947881465, 34.80728798345248975, 21.96198386118272339 ) ) ;
#11412=CARTESIAN_POINT ( 'NONE',  ( 0.3591563125534498746, 18.74881295153323535, 49.30117588463760825 ) ) ;
#11434=CARTESIAN_POINT ( 'NONE',  ( -7.308237722677127124, 52.16199744752358214, -2.719250781937797345 ) ) ;
#11438=CARTESIAN_POINT ( 'NONE',  ( -0.6261581091747900896, 8.128258333189501528, -51.58587807493976385 ) ) ;
#11452=CARTESIAN_POINT ( 'NONE',  ( -4.185364993345132234, 53.85950711538551872, -7.946775408610140090 ) ) ;
#11454=CARTESIAN_POINT ( 'NONE',  ( -9.182151393623367852, 45.78138532639618319, -14.82507784383112792 ) ) ;
#11457=CARTESIAN_POINT ( 'NONE',  ( -5.290067270634260410, 52.08006895350597176, -6.031152949369843697 ) ) ;
#11460=CARTESIAN_POINT ( 'NONE',  ( 27.26440085636200550, 36.55135662950691966, -10.05698433968642469 ) ) ;
#11478=CARTESIAN_POINT ( 'NONE',  ( 47.50459250088609053, 17.89957706894796985, -14.46754909258835298 ) ) ;
#11480=CARTESIAN_POINT ( 'NONE',  ( -10.28624191511820207, 43.25714326066858462, 15.40779740156164124 ) ) ;
#11482=CARTESIAN_POINT ( 'NONE',  ( -48.55172137731392468, 13.85052760073561373, 16.74335408647196033 ) ) ;
#11496=ORIENTED_EDGE ( 'NONE', *, *, #61844, .F. ) ;
#11499=CARTESIAN_POINT ( 'NONE',  ( -26.12422881270600783, 34.87013364854426101, -9.598205162888435282 ) ) ;
#11509=( NAMED_UNIT ( * ) SI_UNIT ( $, .STERADIAN. ) SOLID_ANGLE_UNIT ( ) );
#11530=CARTESIAN_POINT ( 'NONE',  ( 48.15068916914983532, 11.33291430652588971, -14.35535821593549954 ) ) ;
#11549=CARTESIAN_POINT ( 'NONE',  ( 48.02835407290504577, 16.78162100668611956, -14.35535821593549954 ) ) ;
#11577=STYLED_ITEM ( 'NONE', ( #67036 ), #7067 ) ;
#11587=CARTESIAN_POINT ( 'NONE',  ( -7.308109670146557768, 54.29019187464274410, 2.720881023164113177 ) ) ;
#11597=CARTESIAN_POINT ( 'NONE',  ( 8.875907993205162327, 53.84819675155885932, -1.561518095665555883 ) ) ;
#11634=CARTESIAN_POINT ( 'NONE',  ( -1.015626162675523636, 51.43337680269377898, -9.747245237717404365 ) ) ;
#11641=ORIENTED_EDGE ( 'NONE', *, *, #9213, .F. ) ;
#11651=ORIENTED_EDGE ( 'NONE', *, *, #73377, .T. ) ;
#11668=CARTESIAN_POINT ( 'NONE',  ( 28.43271360265383052, 12.18326821505114310, -40.99299228862982147 ) ) ;
#11671=CARTESIAN_POINT ( 'NONE',  ( -9.635469362647075542, 51.40912437293231818, 2.123716195014139885 ) ) ;
#11675=LINE ( 'NONE', #68345, #24374 ) ;
#11686=ORIENTED_EDGE ( 'NONE', *, *, #96581, .T. ) ;
#11699=AXIS2_PLACEMENT_3D ( 'NONE', #98900, #24535, #59006 ) ;
#11711=CARTESIAN_POINT ( 'NONE',  ( -0.7857478027959594602, 28.10741379899660686, 38.51436396715669730 ) ) ;
#11764=FACE_BOUND ( 'NONE', #76874, .T. ) ;
#11769=EDGE_CURVE ( 'NONE', #34743, #35444, #67764, .T. ) ;
#11794=CARTESIAN_POINT ( 'NONE',  ( 16.58679117417341686, 36.41790041698921954, -24.30698433968622396 ) ) ;
#11797=CARTESIAN_POINT ( 'NONE',  ( -4.959056880045103810, 54.27782031566443521, 6.063933026178952801 ) ) ;
#11852=FILL_AREA_STYLE ('',( #93319 ) ) ;
#11854=ORIENTED_EDGE ( 'NONE', *, *, #46154, .F. ) ;
#11860=FILL_AREA_STYLE ('',( #53402 ) ) ;
#11864=ORIENTED_EDGE ( 'NONE', *, *, #39960, .T. ) ;
#11875=DIRECTION ( 'NONE',  ( -0.000000000000000000, 1.000000000000000000, -0.000000000000000000 ) ) ;
#11880=CARTESIAN_POINT ( 'NONE',  ( -17.07807050392511528, 37.03766137757074972, -21.83949354139809174 ) ) ;
#11894=ORIENTED_EDGE ( 'NONE', *, *, #43026, .F. ) ;
#11896=CARTESIAN_POINT ( 'NONE',  ( 36.31862201025842296, 26.04192262955948678, -12.31455456606723331 ) ) ;
#11925=ORIENTED_EDGE ( 'NONE', *, *, #6918, .T. ) ;
#11947=CARTESIAN_POINT ( 'NONE',  ( 16.83488000812927510, 34.23830427773977902, 24.30698433968583316 ) ) ;
#11950=CARTESIAN_POINT ( 'NONE',  ( 17.89028079457004239, 43.21736803053038045, 5.218346154640485679 ) ) ;
#11951=VERTEX_POINT ( 'NONE', #53701 ) ;
#11979=CARTESIAN_POINT ( 'NONE',  ( -28.18087625354337789, 34.32284550959429481, 8.149263751191908156 ) ) ;
#11982=CARTESIAN_POINT ( 'NONE',  ( -17.07643158642811798, 37.03581886162301373, 21.84712036628276977 ) ) ;
#11987=CARTESIAN_POINT ( 'NONE',  ( 6.133828225839772941, 53.39918049015730617, -8.207320443802755605 ) ) ;
#11992=CARTESIAN_POINT ( 'NONE',  ( -10.28624191511830155, 45.38549880562041494, -15.40779740156157196 ) ) ;
#12002=AXIS2_PLACEMENT_3D ( 'NONE', #85078, #19337, #11162 ) ;
#12023=CARTESIAN_POINT ( 'NONE',  ( -49.19536753090093129, 12.91488588853528618, 16.05939653828475144 ) ) ;
#12039=CARTESIAN_POINT ( 'NONE',  ( -22.37419622807756525, 26.07634736961676580, -31.02968219912407122 ) ) ;
#12047=EDGE_CURVE ( 'NONE', #54691, #22572, #4084, .T. ) ;
#12051=FILL_AREA_STYLE_COLOUR ( '', #60041 ) ;
#12068=VERTEX_POINT ( 'NONE', #7257 ) ;
#12072=( NAMED_UNIT ( * ) SI_UNIT ( $, .STERADIAN. ) SOLID_ANGLE_UNIT ( ) );
#12101=CARTESIAN_POINT ( 'NONE',  ( 0.6243278333291550908, 8.125659060767901565, 51.58699189189907486 ) ) ;
#12121=CARTESIAN_POINT ( 'NONE',  ( 30.80294602723973085, 13.24188206181652383, 41.41355684762679346 ) ) ;
#12132=MECHANICAL_DESIGN_GEOMETRIC_PRESENTATION_REPRESENTATION('',(#22498),#93150);
#12151=DIRECTION ( 'NONE',  ( 0.000000000000000000, 0.000000000000000000, 1.000000000000000000 ) ) ;
#12173=VERTEX_POINT ( 'NONE', #82211 ) ;
#12184=EDGE_LOOP ( 'NONE', ( #82754, #99960 ) ) ;
#12204=CARTESIAN_POINT ( 'NONE',  ( 0.000000000000000000, 36.79151656018385097, -22.55262289886175964 ) ) ;
#12208=CARTESIAN_POINT ( 'NONE',  ( 28.77725283099220732, 13.66028544304340464, -39.99080474963867715 ) ) ;
#12225=( NAMED_UNIT ( * ) PLANE_ANGLE_UNIT ( ) SI_UNIT ( $, .RADIAN. ) );
#12230=B_SPLINE_CURVE_WITH_KNOTS ( 'NONE', 3,
 ( #67866, #16655, #33392, #18277, #66264, #99152, #10152, #33938, #76474, #34479, #100224, #43066, #424, #84049, #1511, #25310, #49545, #99695, #67346, #51133, #98622, #59255 ),
 .UNSPECIFIED., .F., .F.,
 ( 4, 2, 2, 2, 2, 2, 2, 2, 2, 2, 4 ),
 ( 0.002801246442724396931, 0.003304316507003848043, 0.003555851539143575768, 0.003807386571283303059, 0.004310456635562755039, 0.004561991667702480595, 0.004813526699842207018, 0.005316596764121661600, 0.005819666828401116182, 0.006322736892680569896, 0.006825806956960025346 ),
 .UNSPECIFIED. ) ;
#12234=CARTESIAN_POINT ( 'NONE',  ( 9.958126073916819365, 43.33285415681326924, 15.37489409574949129 ) ) ;
#12252=CARTESIAN_POINT ( 'NONE',  ( 0.7782283554130018377, 36.39419318762584510, -29.48168008561355435 ) ) ;
#12257=CARTESIAN_POINT ( 'NONE',  ( 27.10511071441197117, -1.200000000000000030E-05, 8.806984339685705265 ) ) ;
#12264=FILL_AREA_STYLE_COLOUR ( '', #99699 ) ;
#12270=ORIENTED_EDGE ( 'NONE', *, *, #42121, .T. ) ;
#12294=( NAMED_UNIT ( * ) SI_UNIT ( $, .STERADIAN. ) SOLID_ANGLE_UNIT ( ) );
#12302=CARTESIAN_POINT ( 'NONE',  ( 55.00000000000000000, 0.000000000000000000, 0.000000000000000000 ) ) ;
#12324=AXIS2_PLACEMENT_3D ( 'NONE', #79733, #22602, #14448 ) ;
#12345=CARTESIAN_POINT ( 'NONE',  ( -48.60240570037294106, 10.21057620019135470, 14.48840219382793038 ) ) ;
#12385=DIRECTION ( 'NONE',  ( -0.000000000000000000, 1.000000000000000000, -0.000000000000000000 ) ) ;
#12387=CYLINDRICAL_SURFACE ( 'NONE', #16769, 1.250000000000001110 ) ;
#12396=ORIENTED_EDGE ( 'NONE', *, *, #91814, .F. ) ;
#12415=CARTESIAN_POINT ( 'NONE',  ( -1.249332996999305667, 51.75169767656670672, 8.836784652845731003 ) ) ;
#12427=( LENGTH_UNIT ( ) NAMED_UNIT ( * ) SI_UNIT ( .MILLI., .METRE. ) );
#12435=CARTESIAN_POINT ( 'NONE',  ( -1.131038375678608876, 45.55010860757282387, 18.03819305252759264 ) ) ;
#12439=VERTEX_POINT ( 'NONE', #83807 ) ;
#12447=LINE ( 'NONE', #102538, #28085 ) ;
#12460=SURFACE_STYLE_USAGE ( .BOTH. , #55038 ) ;
#12470=CARTESIAN_POINT ( 'NONE',  ( 17.86121324767568552, 34.21128550139528102, 23.65650543089517654 ) ) ;
#12474=CARTESIAN_POINT ( 'NONE',  ( -28.94895647869480726, 13.71030094619075967, -39.84075445247425051 ) ) ;
#12518=CYLINDRICAL_SURFACE ( 'NONE', #68059, 1.250000000000001110 ) ;
#12539=CARTESIAN_POINT ( 'NONE',  ( -11.53285117555248007, 45.44727734447007350, 14.28089210442085921 ) ) ;
#12543=CARTESIAN_POINT ( 'NONE',  ( 46.92395915124532024, 18.83177588379324163, -15.01493731818186816 ) ) ;
#12577=EDGE_CURVE ( 'NONE', #62895, #54301, #23357, .T. ) ;
#12579=VECTOR ( 'NONE', #75732, 1000.000000000000114 ) ;
#12585=CARTESIAN_POINT ( 'NONE',  ( 16.64348903516523848, -1.200000000000000030E-05, 5.407797401561420969 ) ) ;
#12614=DIRECTION ( 'NONE',  ( 0.000000000000000000, 1.000000000000000000, 0.000000000000000000 ) ) ;
#12615=CARTESIAN_POINT ( 'NONE',  ( 4.960693420635299056, 51.41875661953385190, 8.497939143228606440 ) ) ;
#12619=ORIENTED_EDGE ( 'NONE', *, *, #88842, .F. ) ;
#12629=ORIENTED_EDGE ( 'NONE', *, *, #90343, .T. ) ;
#12630=CARTESIAN_POINT ( 'NONE',  ( 0.000000000000000000, 0.000000000000000000, 0.000000000000000000 ) ) ;
#12673=CARTESIAN_POINT ( 'NONE',  ( 4.650896588451713498, 54.30650138372552505, -6.203625354536873360 ) ) ;
#12681=CARTESIAN_POINT ( 'NONE',  ( 27.10511071441198894, 36.88665068479745912, 7.556984339683237906 ) ) ;
#12684=CARTESIAN_POINT ( 'NONE',  ( 16.96105790261473345, 43.64123098144456492, -4.188549414824395356 ) ) ;
#12685=VERTEX_POINT ( 'NONE', #104240 ) ;
#12691=EDGE_CURVE ( 'NONE', #59308, #66067, #45160, .T. ) ;
#12720=LINE ( 'NONE', #14303, #51445 ) ;
#12722=CARTESIAN_POINT ( 'NONE',  ( 5.290067270632397012, 54.20842449845690680, 6.031152949374294359 ) ) ;
#12729=CARTESIAN_POINT ( 'NONE',  ( 6.337538409676599689E-15, 7.746009256456446224, 51.75000000000000711 ) ) ;
#12739=CARTESIAN_POINT ( 'NONE',  ( -9.180591118468083067, 51.37400502630696053, 3.869057452854628654 ) ) ;
#12747=EDGE_CURVE ( 'NONE', #36282, #24510, #74524, .T. ) ;
#12781=ORIENTED_EDGE ( 'NONE', *, *, #4254, .F. ) ;
#12785=CARTESIAN_POINT ( 'NONE',  ( -1.008312940004822522, 54.10577091759437707, -8.243645369945518553 ) ) ;
#12797=VERTEX_POINT ( 'NONE', #51847 ) ;
#12819=DIRECTION ( 'NONE',  ( 0.000000000000000000, 0.000000000000000000, 1.000000000000000000 ) ) ;
#12836=ADVANCED_FACE ( 'NONE', ( #69122 ), #28153, .F. ) ;
#12844=COLOUR_RGB ( '', 0.31764706, 0.68627451, 0.89019608) ;
#12851=MECHANICAL_DESIGN_GEOMETRIC_PRESENTATION_REPRESENTATION('',(#33589),#35299);
#12858=CARTESIAN_POINT ( 'NONE',  ( -26.78447284414440333, 36.99601554321866814, 7.587964289499315562 ) ) ;
#12874=EDGE_LOOP ( 'NONE', ( #64962, #153, #91078, #96720 ) ) ;
#12878=CARTESIAN_POINT ( 'NONE',  ( -30.92866670662964523, 8.704003156311230782, 40.98833526575327113 ) ) ;
#12888=CARTESIAN_POINT ( 'NONE',  ( -16.32725980561048829, 43.86428832234518183, -4.195806562069138046 ) ) ;
#12904=CARTESIAN_POINT ( 'NONE',  ( 30.29857313018901266, 7.759641293511155169, -41.94607130693972152 ) ) ;
#12935=CARTESIAN_POINT ( 'NONE',  ( -17.97938082339169341, 36.40366709787543442, -23.34517568653161490 ) ) ;
#12953=CARTESIAN_POINT ( 'NONE',  ( -9.059498534015210325, 43.97148598410754516, -13.86662515133364160 ) ) ;
#12961=CARTESIAN_POINT ( 'NONE',  ( -0.6243543237748914176, 8.125635866029588428, 51.58700165176743013 ) ) ;
#12962=EDGE_CURVE ( 'NONE', #87056, #63425, #2, .T. ) ;
#12969=CARTESIAN_POINT ( 'NONE',  ( 10.45102250067199812, 43.95277330377771108, 12.91605047380969218 ) ) ;
#12976=CARTESIAN_POINT ( 'NONE',  ( -15.64672812219209241, 34.65657699850147111, 23.72309513107661161 ) ) ;
#12986=( LENGTH_UNIT ( ) NAMED_UNIT ( * ) SI_UNIT ( .MILLI., .METRE. ) );
#12992=CARTESIAN_POINT ( 'NONE',  ( 30.59538916938560860, 12.96143355072255687, -41.71318167414167277 ) ) ;
#13001=CARTESIAN_POINT ( 'NONE',  ( -46.83368825529026225, 18.87956456981594755, 15.22947487994887616 ) ) ;
#13009=CARTESIAN_POINT ( 'NONE',  ( 37.88747170836497702, 25.37001114043394878, 13.42513980240604177 ) ) ;
#13012=CARTESIAN_POINT ( 'NONE',  ( -48.02835407290516656, -1.200000000000000030E-05, 14.35535821593516559 ) ) ;
#13026=ADVANCED_FACE ( 'NONE', ( #74392 ), #65788, .F. ) ;
#13030=CARTESIAN_POINT ( 'NONE',  ( -27.65271972678647927, 34.30554982303950595, 9.933614217763615528 ) ) ;
#13033=CARTESIAN_POINT ( 'NONE',  ( -16.83415698846535236, 37.10146012410931604, 21.80698433968611383 ) ) ;
#13037=DIRECTION ( 'NONE',  ( -0.000000000000000000, 1.000000000000000000, -0.000000000000000000 ) ) ;
#13062=ORIENTED_EDGE ( 'NONE', *, *, #48061, .T. ) ;
#13066=ORIENTED_EDGE ( 'NONE', *, *, #1677, .F. ) ;
#13084=CARTESIAN_POINT ( 'NONE',  ( -9.806112067865916160, 53.43729364773486168, -2.589978564625472046 ) ) ;
#13098=CARTESIAN_POINT ( 'NONE',  ( 27.10511071441197117, 36.60571256639528315, 10.05698433968570704 ) ) ;
#13103=CARTESIAN_POINT ( 'NONE',  ( 28.19275368886287580, 34.18006324415607367, -9.428753190584984623 ) ) ;
#13126=STYLED_ITEM ( 'NONE', ( #40085 ), #65896 ) ;
#13132=COLOUR_RGB ( '', 0.08235294, 0.09019608, 0.10196078) ;
#13138=CARTESIAN_POINT ( 'NONE',  ( -37.56673239365863282, -1.200000000000000030E-05, -12.20617127781024713 ) ) ;
#13143=CARTESIAN_POINT ( 'NONE',  ( -37.40742181597744320, 25.81285809103578543, 10.95617127781060418 ) ) ;
#13146=CARTESIAN_POINT ( 'NONE',  ( 4.036241782280404422, 52.01032325769635634, 7.154377370704869676 ) ) ;
#13152=CARTESIAN_POINT ( 'NONE',  ( 1.530808498934192310E-16, -1.200000000000000030E-05, 16.25000000000000000 ) ) ;
#13160=CARTESIAN_POINT ( 'NONE',  ( -25.89174952812846797, 37.21031890518617047, -8.494939486733640521 ) ) ;
#13166=CARTESIAN_POINT ( 'NONE',  ( 5.290067270632455632, 51.34639538792298197, 8.531152949374481764 ) ) ;
#13191=VERTEX_POINT ( 'NONE', #92991 ) ;
#13202=CARTESIAN_POINT ( 'NONE',  ( 4.205231606200393379, 53.86394433159298956, -7.921949934137936467 ) ) ;
#13204=CARTESIAN_POINT ( 'NONE',  ( -16.58710573300773561, 37.15623819652538629, 21.80698433968612449 ) ) ;
#13209=CARTESIAN_POINT ( 'NONE',  ( -16.72321626032217523, 45.57697876764352429, -6.657797401561673212 ) ) ;
#13215=MECHANICAL_DESIGN_GEOMETRIC_PRESENTATION_REPRESENTATION('',(#63205),#88993);
#13222=VERTEX_POINT ( 'NONE', #42308 ) ;
#13229=MECHANICAL_DESIGN_GEOMETRIC_PRESENTATION_REPRESENTATION('',(#33987),#47716);
#13266=CARTESIAN_POINT ( 'NONE',  ( -8.880609241544023646, 51.45519007158284808, 4.000283470555588750 ) ) ;
#13285=CARTESIAN_POINT ( 'NONE',  ( 29.68315524076926692, 13.47185074185900255, -42.10535821593530414 ) ) ;
#13314=CARTESIAN_POINT ( 'NONE',  ( -1.014206878838883386, 53.56122919495654600, -9.748765210281540305 ) ) ;
#13344=CARTESIAN_POINT ( 'NONE',  ( 0.9982104683319775740, 8.901057192202040724, -51.25567227449372609 ) ) ;
#13362=CARTESIAN_POINT ( 'NONE',  ( -27.26469077191609003, 36.55125769914398859, 10.05698433968617067 ) ) ;
#13364=CARTESIAN_POINT ( 'NONE',  ( -27.10511071441192144, -1.200000000000000030E-05, -7.556984339685890006 ) ) ;
#13380=( NAMED_UNIT ( * ) SI_UNIT ( $, .STERADIAN. ) SOLID_ANGLE_UNIT ( ) );
#13387=CARTESIAN_POINT ( 'NONE',  ( -25.89663754417259511, 37.12989468761069389, 9.165637236921460484 ) ) ;
#13396=EDGE_LOOP ( 'NONE', ( #102594, #18378 ) ) ;
#13398=CARTESIAN_POINT ( 'NONE',  ( -49.25933966097106520, 7.764757817614880153, 15.83577412118870242 ) ) ;
#13472=CARTESIAN_POINT ( 'NONE',  ( -0.4151059376575879090, 51.29107746579092719, 10.18202427744692073 ) ) ;
#13483=CARTESIAN_POINT ( 'NONE',  ( -10.20347334622529978, 43.27386994973568335, -15.40779740156156841 ) ) ;
#13485=CARTESIAN_POINT ( 'NONE',  ( -1.219945943888230522, 34.73238240055653847, 28.18370779043763008 ) ) ;
#13493=CARTESIAN_POINT ( 'NONE',  ( -1.235584394549037901, 10.15213688280110738, 50.72542580235119658 ) ) ;
#13502=SURFACE_STYLE_FILL_AREA ( #88480 ) ;
#13537=CARTESIAN_POINT ( 'NONE',  ( 17.16204799116226809, 34.18975596472709100, 24.24075866926950340 ) ) ;
#13556=CARTESIAN_POINT ( 'NONE',  ( 4.988960626530190971E-15, 27.29656849860388235, 40.75000000000000000 ) ) ;
#13563=DIRECTION ( 'NONE',  ( 0.000000000000000000, 1.000000000000000000, 0.000000000000000000 ) ) ;
#13569=DIRECTION ( 'NONE',  ( -0.000000000000000000, 1.000000000000000000, -0.000000000000000000 ) ) ;
#13603=ORIENTED_EDGE ( 'NONE', *, *, #48254, .F. ) ;
#13604=CARTESIAN_POINT ( 'NONE',  ( 11.53285117555237171, 45.44727734447008061, -14.28089210442093915 ) ) ;
#13622=ORIENTED_EDGE ( 'NONE', *, *, #67576, .T. ) ;
#13641=LINE ( 'NONE', #104249, #4716 ) ;
#13642=ORIENTED_EDGE ( 'NONE', *, *, #36687, .T. ) ;
#13647=FILL_AREA_STYLE_COLOUR ( '', #101999 ) ;
#13654=DIRECTION ( 'NONE',  ( 0.000000000000000000, 0.000000000000000000, 1.000000000000000000 ) ) ;
#13662=CARTESIAN_POINT ( 'NONE',  ( -38.56060268544248260, 27.32095725847138823, -12.96889906080386901 ) ) ;
#13673=DIRECTION ( 'NONE',  ( 0.000000000000000000, 0.000000000000000000, 1.000000000000000000 ) ) ;
#13679=MECHANICAL_DESIGN_GEOMETRIC_PRESENTATION_REPRESENTATION('',(#91169),#36068);
#13692=EDGE_CURVE ( 'NONE', #41831, #101431, #5220, .T. ) ;
#13743=CARTESIAN_POINT ( 'NONE',  ( 26.10600422010756105, 37.18654406599299023, 8.037532972182770408 ) ) ;
#13745=CARTESIAN_POINT ( 'NONE',  ( -23.38389609179523632, 28.08052868592283957, -30.70617127781034483 ) ) ;
#13755=FILL_AREA_STYLE_COLOUR ( '', #68119 ) ;
#13760=CARTESIAN_POINT ( 'NONE',  ( 0.2960616276314126383, 18.79208194970808776, -49.28345773665818541 ) ) ;
#13797=CARTESIAN_POINT ( 'NONE',  ( -9.773556239149636227, 51.26923793256161588, 3.090446767225991209 ) ) ;
#13801=CARTESIAN_POINT ( 'NONE',  ( 47.14764774813721715, 18.53760837137042472, 14.71662980465857906 ) ) ;
#13814=CARTESIAN_POINT ( 'NONE',  ( 27.10511071441176156, 34.47735702144343861, -10.05698433968637673 ) ) ;
#13821=CARTESIAN_POINT ( 'NONE',  ( -0.4145643374704980344, 25.19212045144282541, -40.68227741578153456 ) ) ;
#13822=ADVANCED_FACE ( 'NONE', ( #49627 ), #32418, .F. ) ;
#13863=( NAMED_UNIT ( * ) PLANE_ANGLE_UNIT ( ) SI_UNIT ( $, .RADIAN. ) );
#13877=CARTESIAN_POINT ( 'NONE',  ( 1.250982008297754300, 10.43118007883091103, -50.60792131318659415 ) ) ;
#13878=CARTESIAN_POINT ( 'NONE',  ( 16.75187969033571989, 37.11970326878314097, 21.80698433968582961 ) ) ;
#13892=CARTESIAN_POINT ( 'NONE',  ( -27.10511071441183262, 36.88665068479722464, 7.556984339686156460 ) ) ;
#13918=CARTESIAN_POINT ( 'NONE',  ( -25.85367364129496082, 37.19423504344951681, 8.748924795912675023 ) ) ;
#13939=COLOUR_RGB ( '', 0.08235294, 0.09019608, 0.10196078) ;
#13970=CARTESIAN_POINT ( 'NONE',  ( -8.559508646656389885, 53.96349637827586321, -1.531152949374502859 ) ) ;
#13984=FACE_OUTER_BOUND ( 'NONE', #91968, .T. ) ;
#14001=ORIENTED_EDGE ( 'NONE', *, *, #22258, .F. ) ;
#14007=VECTOR ( 'NONE', #71630, 1000.000000000000000 ) ;
#14020=CARTESIAN_POINT ( 'NONE',  ( -1.106297339054949314, 12.12138970700505958, 49.90201418493064267 ) ) ;
#14031=CARTESIAN_POINT ( 'NONE',  ( 29.68315524077034695, -1.200000000000000030E-05, 40.85535821593451544 ) ) ;
#14085=EDGE_CURVE ( 'NONE', #87776, #68832, #94020, .T. ) ;
#14086=CARTESIAN_POINT ( 'NONE',  ( -37.56673239365851913, 25.75719283951025673, 10.95617127780993449 ) ) ;
#14093=CARTESIAN_POINT ( 'NONE',  ( -1.150658033319299881E-13, -1.200000000000000030E-05, -51.75000000000000711 ) ) ;
#14098=CARTESIAN_POINT ( 'NONE',  ( 6.496772124874876653, 53.67412401770713615, -6.918302629204984733 ) ) ;
#14099=CARTESIAN_POINT ( 'NONE',  ( 17.37694393396142090, 34.80682117732449399, -21.96264255479069405 ) ) ;
#14129=CARTESIAN_POINT ( 'NONE',  ( -10.69637036727096557, 45.32132628290195697, 15.34161786853266740 ) ) ;
#14131=CARTESIAN_POINT ( 'NONE',  ( 10.69637036727085722, 45.32132628290193566, -15.34161786853273846 ) ) ;
#14145=VERTEX_POINT ( 'NONE', #1180 ) ;
#14155=CARTESIAN_POINT ( 'NONE',  ( 16.18722300313225304, 37.20509570188509230, 21.93860808728192779 ) ) ;
#14157=CARTESIAN_POINT ( 'NONE',  ( 0.1684601300089527409, 44.08548369317414029, -16.25000000000000000 ) ) ;
#14159=CARTESIAN_POINT ( 'NONE',  ( -48.26750065955930324, 16.22349350713446725, -14.37287707152977667 ) ) ;
#14191=CARTESIAN_POINT ( 'NONE',  ( 10.92801675053753918, 45.30201443972635644, 15.24347305256516449 ) ) ;
#14197=SURFACE_SIDE_STYLE ('',( #6646 ) ) ;
#14208=B_SPLINE_CURVE_WITH_KNOTS ( 'NONE', 3,
 ( #90525, #8534, #50058, #98606, #15568, #58150, #56543, #40911, #48983, #73800, #33919, #16637, #67330, #41441, #83491, #937, #66790, #1496, #74332, #407, #82968, #48457 ),
 .UNSPECIFIED., .F., .F.,
 ( 4, 2, 2, 2, 2, 2, 2, 2, 2, 2, 4 ),
 ( 0.002937870026032432698, 0.003442696458882132677, 0.003947522891731832656, 0.004199936108156682862, 0.004452349324581533069, 0.004957175757431232614, 0.005462002190280932160, 0.005714415406705783233, 0.005966828623130632572, 0.006471655055980334720, 0.006976481488830035133 ),
 .UNSPECIFIED. ) ;
#14227=CARTESIAN_POINT ( 'NONE',  ( -6.048905432935242743, 53.95601670924679638, 6.275204406079152086 ) ) ;
#14230=( NAMED_UNIT ( * ) PLANE_ANGLE_UNIT ( ) SI_UNIT ( $, .RADIAN. ) );
#14234=MECHANICAL_DESIGN_GEOMETRIC_PRESENTATION_REPRESENTATION('',(#69404),#22905);
#14237=VECTOR ( 'NONE', #71663, 1000.000000000000000 ) ;
#14281=CARTESIAN_POINT ( 'NONE',  ( 24.23707248033631245, 27.31414015027110764, -32.69896640055604564 ) ) ;
#14283=ORIENTED_EDGE ( 'NONE', *, *, #32974, .F. ) ;
#14290=CARTESIAN_POINT ( 'NONE',  ( 22.13522383661086934, 25.65748311883131905, -32.60130617687421761 ) ) ;
#14303=CARTESIAN_POINT ( 'NONE',  ( 7.681258945454893382E-14, -1.200000000000000030E-05, 40.75000000000000000 ) ) ;
#14311=CARTESIAN_POINT ( 'NONE',  ( 8.559508646656407649, 53.96349637827586321, 1.531152949374444239 ) ) ;
#14345=DIRECTION ( 'NONE',  ( -0.000000000000000000, 1.000000000000000000, 0.000000000000000000 ) ) ;
#14347=CARTESIAN_POINT ( 'NONE',  ( 9.657433074643469340, 43.43006688034495255, 15.25031001494009608 ) ) ;
#14350=CARTESIAN_POINT ( 'NONE',  ( 29.68315524076926337, -1.200000000000000030E-05, -40.85535821593530414 ) ) ;
#14369=CARTESIAN_POINT ( 'NONE',  ( -0.6456277288726508523, 53.45124240752763001, -10.08335398010373574 ) ) ;
#14391=CARTESIAN_POINT ( 'NONE',  ( 1.012061803676453042, 25.89207449483374290, -38.74815287735676606 ) ) ;
#14395=CARTESIAN_POINT ( 'NONE',  ( -7.799243123709609371, 52.08920511281555576, 1.774792398066115107 ) ) ;
#14401=( LENGTH_UNIT ( ) NAMED_UNIT ( * ) SI_UNIT ( .MILLI., .METRE. ) );
#14421=STYLED_ITEM ( 'NONE', ( #9282 ), #95420 ) ;
#14439=ORIENTED_EDGE ( 'NONE', *, *, #42504, .T. ) ;
#14448=DIRECTION ( 'NONE',  ( 0.000000000000000000, 0.000000000000000000, 1.000000000000000000 ) ) ;
#14454=ORIENTED_EDGE ( 'NONE', *, *, #100634, .F. ) ;
#14457=CARTESIAN_POINT ( 'NONE',  ( -48.91361122442935283, 8.059984797525034494, 16.48958644079295155 ) ) ;
#14462=CARTESIAN_POINT ( 'NONE',  ( 29.14573983020287784, 13.65694994997195444, 39.72476874530803315 ) ) ;
#14503=ORIENTED_EDGE ( 'NONE', *, *, #28365, .F. ) ;
#14520=VERTEX_POINT ( 'NONE', #32963 ) ;
#14539=CARTESIAN_POINT ( 'NONE',  ( -0.1696257032302785628, 34.17492106715072708, 29.74129072143946928 ) ) ;
#14555=SURFACE_STYLE_USAGE ( .BOTH. , #23226 ) ;
#14558=SURFACE_STYLE_FILL_AREA ( #55546 ) ;
#14584=CARTESIAN_POINT ( 'NONE',  ( 36.49133541866372354, 28.04549298931340928, 12.86447375659304804 ) ) ;
#14601=CARTESIAN_POINT ( 'NONE',  ( -28.77636872657267730, 18.82904586931651636, -39.99174360897771408 ) ) ;
#14603=SURFACE_STYLE_FILL_AREA ( #22751 ) ;
#14614=FACE_OUTER_BOUND ( 'NONE', #2484, .T. ) ;
#14627=ORIENTED_EDGE ( 'NONE', *, *, #98199, .F. ) ;
#14628=DIRECTION ( 'NONE',  ( 0.000000000000000000, 0.000000000000000000, 1.000000000000000000 ) ) ;
#14631=ORIENTED_EDGE ( 'NONE', *, *, #29544, .F. ) ;
#14667=AXIS2_PLACEMENT_3D ( 'NONE', #82638, #90199, #49190 ) ;
#14686=( GEOMETRIC_REPRESENTATION_CONTEXT ( 3 ) GLOBAL_UNCERTAINTY_ASSIGNED_CONTEXT ( ( #85909 ) ) GLOBAL_UNIT_ASSIGNED_CONTEXT ( ( #28104, #85241, #58851 ) ) REPRESENTATION_CONTEXT ( 'NONE', 'WORKASPACE' ) );
#14690=CARTESIAN_POINT ( 'NONE',  ( -48.69590189480585707, 13.58600142653171972, -16.66526863408559578 ) ) ;
#14696=CARTESIAN_POINT ( 'NONE',  ( 0.000000000000000000, 34.08768991669519721, 0.000000000000000000 ) ) ;
#14706=LINE ( 'NONE', #72426, #34627 ) ;
#14714=EDGE_LOOP ( 'NONE', ( #29885, #38289, #77312, #3784 ) ) ;
#14717=CARTESIAN_POINT ( 'NONE',  ( -38.32973030926034141, 27.37225254236124528, -13.21033226210355416 ) ) ;
#14720=CARTESIAN_POINT ( 'NONE',  ( -1.235501149773866825, 15.31955389872309858, -50.72623786250530742 ) ) ;
#14723=VECTOR ( 'NONE', #67033, 1000.000000000000000 ) ;
#14732=CARTESIAN_POINT ( 'NONE',  ( 48.15175547875055173, 14.66334354488943426, -16.85535821593556349 ) ) ;
#14738=B_SPLINE_CURVE_WITH_KNOTS ( 'NONE', 3,
 ( #46909, #31298, #64184, #20592, #21102, #70671, #86350, #95472, #12415, #5406, #4340, #37811, #62588, #54447, #87400, #13472, #90029, #73294, #57115, #25327 ),
 .UNSPECIFIED., .F., .F.,
 ( 4, 2, 2, 2, 2, 2, 2, 2, 2, 4 ),
 ( 0.007172846040326944991, 0.007676791773118825553, 0.008180737505910706114, 0.008684683238702585809, 0.009188628971494467237, 0.009692574704286346932, 0.01019652043707822836, 0.01070046616987010805, 0.01095243903626605050, 0.01120441190266199122 ),
 .UNSPECIFIED. ) ;
#14744=ORIENTED_EDGE ( 'NONE', *, *, #82117, .F. ) ;
#14779=CIRCLE ( 'NONE', #2780, 11.27631144943088337 ) ;
#14800=CARTESIAN_POINT ( 'NONE',  ( -15.50702112914504838, 36.95515616017750204, 23.25462944313558111 ) ) ;
#14806=CARTESIAN_POINT ( 'NONE',  ( -17.71951158999537057, 45.45134770963998960, -4.750929343604651578 ) ) ;
#14812=CARTESIAN_POINT ( 'NONE',  ( 23.61948937802333504, 28.00997096501933825, -30.76980700055193552 ) ) ;
#14826=CARTESIAN_POINT ( 'NONE',  ( 22.45260625274932664, 25.48533499626559262, -32.95744641864007463 ) ) ;
#14829=CARTESIAN_POINT ( 'NONE',  ( -47.77471032523668981, 17.34854710534463251, -14.37330285161499255 ) ) ;
#14852=AXIS2_PLACEMENT_3D ( 'NONE', #7884, #89361, #54842 ) ;
#14862=CARTESIAN_POINT ( 'NONE',  ( 47.07350275986915733, 18.64911821952824056, 14.79681583022511404 ) ) ;
#14908=ORIENTED_EDGE ( 'NONE', *, *, #81112, .T. ) ;
#14914=FILL_AREA_STYLE ('',( #7354 ) ) ;
#14935=CARTESIAN_POINT ( 'NONE',  ( 5.708216051535447754E-15, 25.16329480281783759, 46.61112130868859538 ) ) ;
#14938=CARTESIAN_POINT ( 'NONE',  ( -0.3343981592458916130, 35.06559523944065404, -27.29262800599611438 ) ) ;
#14947=VERTEX_POINT ( 'NONE', #98599 ) ;
#14957=ORIENTED_EDGE ( 'NONE', *, *, #66370, .T. ) ;
#14975=( NAMED_UNIT ( * ) PLANE_ANGLE_UNIT ( ) SI_UNIT ( $, .RADIAN. ) );
#14983=CARTESIAN_POINT ( 'NONE',  ( 0.000000000000000000, 0.000000000000000000, 0.000000000000000000 ) ) ;
#15020=ORIENTED_EDGE ( 'NONE', *, *, #8758, .T. ) ;
#15022=DIRECTION ( 'NONE',  ( -0.000000000000000000, 1.000000000000000000, -0.000000000000000000 ) ) ;
#15033=CARTESIAN_POINT ( 'NONE',  ( 10.45208520439346422, 43.95501981190459162, -12.90779740156171584 ) ) ;
#15038=DIRECTION ( 'NONE',  ( 0.000000000000000000, 0.000000000000000000, 1.000000000000000000 ) ) ;
#15044=( GEOMETRIC_REPRESENTATION_CONTEXT ( 3 ) GLOBAL_UNCERTAINTY_ASSIGNED_CONTEXT ( ( #106590 ) ) GLOBAL_UNIT_ASSIGNED_CONTEXT ( ( #18472, #100954, #43784 ) ) REPRESENTATION_CONTEXT ( 'NONE', 'WORKASPACE' ) );
#15047=VERTEX_POINT ( 'NONE', #103266 ) ;
#15050=PRESENTATION_STYLE_ASSIGNMENT (( #23712 ) ) ;
#15069=MECHANICAL_DESIGN_GEOMETRIC_PRESENTATION_REPRESENTATION('',(#61615),#42633);
#15071=STYLED_ITEM ( 'NONE', ( #51245 ), #3886 ) ;
#15085=CARTESIAN_POINT ( 'NONE',  ( -1.126885523087953089, 34.38870459337674390, 29.13346846296686721 ) ) ;
#15101=( NAMED_UNIT ( * ) PLANE_ANGLE_UNIT ( ) SI_UNIT ( $, .RADIAN. ) );
#15104=CARTESIAN_POINT ( 'NONE',  ( 0.000000000000000000, -1.200000000000000030E-05, 17.50000000000000000 ) ) ;
#15108=CARTESIAN_POINT ( 'NONE',  ( -16.75187969033532553, 34.25544727262118982, 24.30698433968612449 ) ) ;
#15135=EDGE_CURVE ( 'NONE', #79036, #54576, #21830, .T. ) ;
#15137=CARTESIAN_POINT ( 'NONE',  ( 26.78714902951895382, 34.58969031657304072, -10.02637816120943270 ) ) ;
#15140=CARTESIAN_POINT ( 'NONE',  ( -28.72976249129343884, 13.62251309882729267, -40.04442010369706395 ) ) ;
#15146=CARTESIAN_POINT ( 'NONE',  ( 0.6414297221551786832, 26.01290138943593888, 38.42394282347074608 ) ) ;
#15150=CARTESIAN_POINT ( 'NONE',  ( -28.46814188645407739, 18.16755603797500029, -40.55128649371884109 ) ) ;
#15152=CYLINDRICAL_SURFACE ( 'NONE', #6969, 1.250000000000001110 ) ;
#15154=CARTESIAN_POINT ( 'NONE',  ( 23.76770941297787587, 25.83109853082994789, 30.83089620004140130 ) ) ;
#15169=CARTESIAN_POINT ( 'NONE',  ( 28.71513376685288321, 15.67191133428134542, -41.65496614056306868 ) ) ;
#15178=DIRECTION ( 'NONE',  ( 0.000000000000000000, 1.000000000000000000, -0.000000000000000000 ) ) ;
#15196=AXIS2_PLACEMENT_3D ( 'NONE', #47545, #63759, #96121 ) ;
#15234=CARTESIAN_POINT ( 'NONE',  ( 0.5677053942435199563, 44.03347157068819939, -16.38324328692960563 ) ) ;
#15235=CARTESIAN_POINT ( 'NONE',  ( -38.81019369337919045, 25.23140533547475073, 11.84541638487588067 ) ) ;
#15254=SURFACE_SIDE_STYLE ('',( #23377 ) ) ;
#15258=ORIENTED_EDGE ( 'NONE', *, *, #65031, .T. ) ;
#15279=VERTEX_POINT ( 'NONE', #58429 ) ;
#15340=CARTESIAN_POINT ( 'NONE',  ( -16.42257055868371651, 36.46149248629888007, 24.27355254955521247 ) ) ;
#15343=CYLINDRICAL_SURFACE ( 'NONE', #91116, 1.250000000000001110 ) ;
#15344=CARTESIAN_POINT ( 'NONE',  ( 1.249506209833404657, 34.67599045332981689, 28.33744947526314206 ) ) ;
#15351=CARTESIAN_POINT ( 'NONE',  ( -24.22978927791485404, 25.18864859774202714, 32.69423595551459982 ) ) ;
#15369=ORIENTED_EDGE ( 'NONE', *, *, #78781, .F. ) ;
#15383=CARTESIAN_POINT ( 'NONE',  ( -9.643763425038864412, 44.08769799646883314, 13.07246033778566918 ) ) ;
#15417=LINE ( 'NONE', #48304, #103742 ) ;
#15419=CARTESIAN_POINT ( 'NONE',  ( -0.8392880725949716236, 25.95834017491164403, -38.57005309225670686 ) ) ;
#15424=DIRECTION ( 'NONE',  ( -0.000000000000000000, 1.000000000000000000, -0.000000000000000000 ) ) ;
#15428=CARTESIAN_POINT ( 'NONE',  ( 1.099023582544892408, 45.97038027629827184, -16.88323843016358694 ) ) ;
#15440=CARTESIAN_POINT ( 'NONE',  ( -29.77450884433714151, 8.177050405881796991, -42.10535821593515493 ) ) ;
#15441=AXIS2_PLACEMENT_3D ( 'NONE', #68220, #33745, #10501 ) ;
#15478=B_SPLINE_CURVE_WITH_KNOTS ( 'NONE', 3,
 ( #66098, #57995, #50960, #93037, #90916, #17568, #17030, #49906, #74706, #100587, #34835, #9984, #8914, #41818, #19198, #67705, #42888, #10512, #83873, #50428 ),
 .UNSPECIFIED., .F., .F.,
 ( 4, 2, 2, 2, 2, 2, 2, 2, 2, 4 ),
 ( 0.003775051291532607704, 0.004278405665375015383, 0.004781760039217423930, 0.005285114413059831609, 0.005788468786902239288, 0.006040145973823445730, 0.006291823160744653039, 0.006795177534587053779, 0.007298531908429453652, 0.007801886282271855259 ),
 .UNSPECIFIED. ) ;
#15487=FILL_AREA_STYLE_COLOUR ( '', #1703 ) ;
#15529=SURFACE_STYLE_FILL_AREA ( #98569 ) ;
#15541=CARTESIAN_POINT ( 'NONE',  ( 29.07939586085803185, 18.85565742903570552, 39.75811902752973737 ) ) ;
#15549=( NAMED_UNIT ( * ) SI_UNIT ( $, .STERADIAN. ) SOLID_ANGLE_UNIT ( ) );
#15568=CARTESIAN_POINT ( 'NONE',  ( -26.35538756233841085, 34.76322194132067267, 9.819931615225865329 ) ) ;
#15569=CARTESIAN_POINT ( 'NONE',  ( 11.27275010301936753, 43.63375202082728777, -13.37403123923981951 ) ) ;
#15578=CARTESIAN_POINT ( 'NONE',  ( -16.96468291457300026, 45.49948827470975488, 6.626685320826292802 ) ) ;
#15603=ORIENTED_EDGE ( 'NONE', *, *, #710, .T. ) ;
#15614=CARTESIAN_POINT ( 'NONE',  ( -29.33080127677455096, 13.52978328598925906, 39.65469037846435896 ) ) ;
#15622=CARTESIAN_POINT ( 'NONE',  ( 36.45652548590511799, 28.06682613793154957, -12.78635007879563190 ) ) ;
#15631=CARTESIAN_POINT ( 'NONE',  ( 22.19982010036187603, 28.18804608458829719, 31.21118039878576411 ) ) ;
#15641=ADVANCED_FACE ( 'NONE', ( #95061 ), #96107, .F. ) ;
#15662=CARTESIAN_POINT ( 'NONE',  ( 25.89149878171548380, 35.08194043918889804, -8.495905954776644009 ) ) ;
#15664=PRESENTATION_STYLE_ASSIGNMENT (( #16735 ) ) ;
#15666=EDGE_CURVE ( 'NONE', #104078, #41373, #19194, .T. ) ;
#15671=LINE ( 'NONE', #89041, #16917 ) ;
#15678=DIRECTION ( 'NONE',  ( -0.000000000000000000, 1.000000000000000000, 0.000000000000000000 ) ) ;
#15697=CARTESIAN_POINT ( 'NONE',  ( 28.73029465396662374, 18.79238081053093623, -40.04376963015472057 ) ) ;
#15733=CARTESIAN_POINT ( 'NONE',  ( -5.621309607737247305, 52.00056912798299180, 6.031152949374553707 ) ) ;
#15734=ORIENTED_EDGE ( 'NONE', *, *, #86746, .T. ) ;
#15744=CARTESIAN_POINT ( 'NONE',  ( -6.273349488839427224, 53.84215621584975509, -6.493349957603958167 ) ) ;
#15755=DIRECTION ( 'NONE',  ( -0.000000000000000000, 1.000000000000000000, -0.000000000000000000 ) ) ;
#15763=FACE_BOUND ( 'NONE', #39524, .T. ) ;
#15765=CARTESIAN_POINT ( 'NONE',  ( 1.006201139504063979, 43.34891076668851184, -18.24605675915023184 ) ) ;
#15770=B_SPLINE_CURVE_WITH_KNOTS ( 'NONE', 3,
 ( #30384, #63273, #96171, #55147, #88077, #14155, #47059, #79959, #6071, #55663, #88600, #47588, #90189, #599, #43237, #34117, #82629, #58901, #58351, #41639, #9253, #33564, #49721, #75595, #16291, #99320 ),
 .UNSPECIFIED., .F., .F.,
 ( 4, 2, 2, 2, 2, 2, 2, 2, 2, 2, 2, 2, 4 ),
 ( 0.003090333073482953025, 0.003342552850341273894, 0.003594772627199594763, 0.003846992404057915631, 0.004099212180916236500, 0.004603651734632870432, 0.004855871511491187398, 0.005108091288349503496, 0.006116970395782786105, 0.006369190172641096999, 0.006621409949499407893, 0.006873629726357717920, 0.007125849503216027947 ),
 .UNSPECIFIED. ) ;
#15782=CARTESIAN_POINT ( 'NONE',  ( -22.46054152223504019, 27.61307239794276924, -32.95409374511062595 ) ) ;
#15794=CARTESIAN_POINT ( 'NONE',  ( -38.64252647164300924, 27.44902043786143153, -11.54866764408293811 ) ) ;
#15810=EDGE_LOOP ( 'NONE', ( #4627, #61421, #45617, #56824 ) ) ;
#15814=CARTESIAN_POINT ( 'NONE',  ( 1.122371673248518720, 51.93028698896991813, -8.361323773265381121 ) ) ;
#15821=CARTESIAN_POINT ( 'NONE',  ( 10.92528302346674351, 43.17643060797472998, 15.23541717086651559 ) ) ;
#15833=CARTESIAN_POINT ( 'NONE',  ( -5.453871017069856997, 54.16911077613673342, 6.031152949374326333 ) ) ;
#15839=VERTEX_POINT ( 'NONE', #64791 ) ;
#15855=CARTESIAN_POINT ( 'NONE',  ( 23.21751746555220564, 25.25267828308493634, -33.20617127781077471 ) ) ;
#15868=CYLINDRICAL_SURFACE ( 'NONE', #88951, 1.250000000000001110 ) ;
#15880=SURFACE_SIDE_STYLE ('',( #31565 ) ) ;
#15886=ORIENTED_EDGE ( 'NONE', *, *, #17544, .F. ) ;
#15894=CARTESIAN_POINT ( 'NONE',  ( 1.098080042019399905, 45.97102111612958453, 16.88153618267994815 ) ) ;
#15897=CARTESIAN_POINT ( 'NONE',  ( 0.000000000000000000, 0.000000000000000000, 0.000000000000000000 ) ) ;
#15901=CARTESIAN_POINT ( 'NONE',  ( 46.89572507581423366, 12.86406951795954434, -16.16260000396544783 ) ) ;
#15906=CARTESIAN_POINT ( 'NONE',  ( 0.7851006235064621475, 53.48263589571089227, 9.986492805000406037 ) ) ;
#15908=CARTESIAN_POINT ( 'NONE',  ( -37.40775402191688670, 27.94109755877887125, 10.95617127781058642 ) ) ;
#15916=CARTESIAN_POINT ( 'NONE',  ( 30.55414771718632494, 11.21328959333584230, 39.95065846501993434 ) ) ;
#15920=CARTESIAN_POINT ( 'NONE',  ( -7.681258945454893382E-14, -1.200000000000000030E-05, -39.50000000000000000 ) ) ;
#15935=B_SPLINE_CURVE_WITH_KNOTS ( 'NONE', 3,
 ( #24781, #39885, #32344, #97561, #90020, #57629, #56032, #8026, #80316, #81377, #7487, #23185, #89499, #96532, #6967, #65750, #39366, #98630, #90554, #16663, #65214, #72244 ),
 .UNSPECIFIED., .F., .F.,
 ( 4, 2, 2, 2, 2, 2, 2, 2, 2, 2, 4 ),
 ( 0.006438828156869064352, 0.006690637486827953097, 0.006942446816786841841, 0.007446065476704619331, 0.007949684136622395952, 0.008453302796540173442, 0.008956921456457950931, 0.009460540116375728420, 0.009964158776293505909, 0.01021596810625239465, 0.01046777743621128340 ),
 .UNSPECIFIED. ) ;
#15946=( NAMED_UNIT ( * ) SI_UNIT ( $, .STERADIAN. ) SOLID_ANGLE_UNIT ( ) );
#15955=CARTESIAN_POINT ( 'NONE',  ( -0.5676227808506075778, 26.02816272619953608, -38.38318647011021767 ) ) ;
#15956=CARTESIAN_POINT ( 'NONE',  ( -9.768722988854461775, 53.46525899633061130, 2.424613394572812997 ) ) ;
#15958=CARTESIAN_POINT ( 'NONE',  ( -1.219825599638223235, 43.50030555992006498, 17.81618553082049061 ) ) ;
#15994=UNCERTAINTY_MEASURE_WITH_UNIT (LENGTH_MEASURE( 1.000000000000000082E-05 ), #104552, 'distance_accuracy_value', 'NONE');
#16024=COLOUR_RGB ( '', 0.40784314, 0.44705882, 0.49803922) ;
#16025=CARTESIAN_POINT ( 'NONE',  ( 24.20495127240709721, 25.63507095802091129, -31.17354648878573897 ) ) ;
#16027=( GEOMETRIC_REPRESENTATION_CONTEXT ( 3 ) GLOBAL_UNCERTAINTY_ASSIGNED_CONTEXT ( ( #45961 ) ) GLOBAL_UNIT_ASSIGNED_CONTEXT ( ( #67594, #34720, #58973 ) ) REPRESENTATION_CONTEXT ( 'NONE', 'WORKASPACE' ) );
#16029=ORIENTED_EDGE ( 'NONE', *, *, #34009, .F. ) ;
#16035=SURFACE_STYLE_FILL_AREA ( #64601 ) ;
#16046=CARTESIAN_POINT ( 'NONE',  ( -27.26381482557892255, 34.42320106084914499, -10.05698433968609606 ) ) ;
#16049=EDGE_CURVE ( 'NONE', #93186, #36646, #31959, .T. ) ;
#16073=CARTESIAN_POINT ( 'NONE',  ( 28.71655383515135185, 10.49725697686260872, 41.65669210871947570 ) ) ;
#16108=CARTESIAN_POINT ( 'NONE',  ( -47.78440564129563484, 10.33446651290970486, 16.83708170412465677 ) ) ;
#16110=COLOUR_RGB ( '', 0.31764706, 0.68627451, 0.89019608) ;
#16116=ORIENTED_EDGE ( 'NONE', *, *, #95044, .T. ) ;
#16118=CARTESIAN_POINT ( 'NONE',  ( 16.64348903516512834, 45.88445698070336931, -4.157797401561768247 ) ) ;
#16137=CARTESIAN_POINT ( 'NONE',  ( -17.40116869051068704, 43.25107240467212932, 6.405389961558260126 ) ) ;
#16140=CARTESIAN_POINT ( 'NONE',  ( -6.045900698167796072, 51.82901340926924405, -6.272940833958317697 ) ) ;
#16146=CARTESIAN_POINT ( 'NONE',  ( -10.61502689374716191, 43.20235065847915479, -15.36667125108853327 ) ) ;
#16158=CARTESIAN_POINT ( 'NONE',  ( 28.28051920154564769, 34.26500913490271216, -8.373811989914575094 ) ) ;
#16163=CARTESIAN_POINT ( 'NONE',  ( -17.25498915691571966, 43.52709508488109691, -4.306061980902978981 ) ) ;
#16186=CARTESIAN_POINT ( 'NONE',  ( 29.68315524076926337, -1.200000000000000030E-05, -39.60535821593530414 ) ) ;
#16191=ORIENTED_EDGE ( 'NONE', *, *, #49809, .T. ) ;
#16203=DIRECTION ( 'NONE',  ( -0.000000000000000000, 1.000000000000000000, 0.000000000000000000 ) ) ;
#16209=CARTESIAN_POINT ( 'NONE',  ( -28.94897463965919471, 18.87963818668123395, -39.84074594005996772 ) ) ;
#16213=CARTESIAN_POINT ( 'NONE',  ( 23.97256388385797266, 25.74924427912474911, 30.95680134856036148 ) ) ;
#16217=COLOUR_RGB ( '', 0.08235294, 0.09019608, 0.10196078) ;
#16220=CARTESIAN_POINT ( 'NONE',  ( -4.962805741472906540, 51.42064187080856641, 8.490339940873784741 ) ) ;
#16240=FACE_BOUND ( 'NONE', #65381, .T. ) ;
#16246=( NAMED_UNIT ( * ) SI_UNIT ( $, .STERADIAN. ) SOLID_ANGLE_UNIT ( ) );
#16251=MANIFOLD_SOLID_BREP ( 'CirPattern1', #99654 ) ;
#16271=CARTESIAN_POINT ( 'NONE',  ( -23.54393690455800936, 28.03570273098069876, -30.73873073986574411 ) ) ;
#16277=ADVANCED_FACE ( 'NONE', ( #26583 ), #87443, .F. ) ;
#16291=CARTESIAN_POINT ( 'NONE',  ( 16.66949223230267307, 36.40081923159284116, 24.30698433968582606 ) ) ;
#16294=CARTESIAN_POINT ( 'NONE',  ( -37.56673239365851913, 25.75719283951025673, 10.95617127780993449 ) ) ;
#16301=AXIS2_PLACEMENT_3D ( 'NONE', #14696, #47068, #63815 ) ;
#16320=SURFACE_STYLE_FILL_AREA ( #91297 ) ;
#16321=ORIENTED_EDGE ( 'NONE', *, *, #36108, .T. ) ;
#16331=VERTEX_POINT ( 'NONE', #55562 ) ;
#16345=CARTESIAN_POINT ( 'NONE',  ( 48.55396075288199853, 8.676907163023365399, 16.74236275264500051 ) ) ;
#16352=LINE ( 'NONE', #56260, #58323 ) ;
#16418=CARTESIAN_POINT ( 'NONE',  ( 0.7814291517363842754, 52.07069370489680438, 8.010806432753755146 ) ) ;
#16423=CARTESIAN_POINT ( 'NONE',  ( 1.106266637551095000, 17.29082734553924539, -49.90197654099129920 ) ) ;
#16426=CARTESIAN_POINT ( 'NONE',  ( 23.21751746555220564, 25.98869614573808917, -30.70617127781077116 ) ) ;
#16444=CARTESIAN_POINT ( 'NONE',  ( -10.20315579733895639, 44.01148501590944306, 12.90779740156163768 ) ) ;
#16445=ORIENTED_EDGE ( 'NONE', *, *, #53077, .F. ) ;
#16465=EDGE_CURVE ( 'NONE', #4091, #90588, #79873, .T. ) ;
#16478=CYLINDRICAL_SURFACE ( 'NONE', #3945, 1.250000000000001110 ) ;
#16484=CARTESIAN_POINT ( 'NONE',  ( -10.28624191511830155, -1.200000000000000030E-05, -15.40779740156157196 ) ) ;
#16488=CARTESIAN_POINT ( 'NONE',  ( -1.094645143735793358, 25.39612329712696948, -40.10891261621117110 ) ) ;
#16489=CARTESIAN_POINT ( 'NONE',  ( -9.500381993471846087, 53.42959890879150464, 3.608304243553658974 ) ) ;
#16491=CARTESIAN_POINT ( 'NONE',  ( -0.7776801151804421108, 43.26715133920247780, 18.48212775743904501 ) ) ;
#16517=CARTESIAN_POINT ( 'NONE',  ( -8.559508646656370345, 53.68473964988125857, 4.031152949374564365 ) ) ;
#16560=CARTESIAN_POINT ( 'NONE',  ( 46.77752740700951506, 13.53072847091734054, 15.64014710929875740 ) ) ;
#16562=DIRECTION ( 'NONE',  ( 0.000000000000000000, 1.000000000000000000, 0.000000000000000000 ) ) ;
#16564=CARTESIAN_POINT ( 'NONE',  ( 16.75187969033571989, -1.200000000000000030E-05, 24.30698433968583316 ) ) ;
#16575=ORIENTED_EDGE ( 'NONE', *, *, #48575, .F. ) ;
#16588=ORIENTED_EDGE ( 'NONE', *, *, #38880, .T. ) ;
#16609=CARTESIAN_POINT ( 'NONE',  ( 28.72976249129374082, 13.62251309882733175, 40.04442010369683658 ) ) ;
#16611=AXIS2_PLACEMENT_3D ( 'NONE', #91576, #2006, #35487 ) ;
#16612=CARTESIAN_POINT ( 'NONE',  ( 28.94897463965949314, 18.87963818668124105, 39.84074594005971903 ) ) ;
#16622=AXIS2_PLACEMENT_3D ( 'NONE', #75325, #1425, #52645 ) ;
#16637=CARTESIAN_POINT ( 'NONE',  ( -25.85202045074685984, 35.07630312271587769, 8.665166400306999250 ) ) ;
#16639=CARTESIAN_POINT ( 'NONE',  ( 10.61390424674485899, 43.90835935462011008, -12.94086579116563485 ) ) ;
#16646=( LENGTH_UNIT ( ) NAMED_UNIT ( * ) SI_UNIT ( .MILLI., .METRE. ) );
#16650=ORIENTED_EDGE ( 'NONE', *, *, #81112, .F. ) ;
#16655=CARTESIAN_POINT ( 'NONE',  ( 8.718677345792714917, 53.63232851853486238, 4.031152949374446237 ) ) ;
#16663=CARTESIAN_POINT ( 'NONE',  ( -0.1698250053810657911, 25.17129873335319346, 40.74125109472547024 ) ) ;
#16669=VERTEX_POINT ( 'NONE', #100287 ) ;
#16676=CARTESIAN_POINT ( 'NONE',  ( -17.19159652742020228, 43.30607723763039019, 6.534202769278905976 ) ) ;
#16680=CARTESIAN_POINT ( 'NONE',  ( -6.542072687172704626, 51.42643242773939249, -7.321406361055552203 ) ) ;
#16694=CARTESIAN_POINT ( 'NONE',  ( 37.24829029260226321, 27.71736929400079319, -13.42529695738276629 ) ) ;
#16702=CARTESIAN_POINT ( 'NONE',  ( -17.63776521792187069, 43.19898629042302929, -6.169977679521857716 ) ) ;
#16708=B_SPLINE_CURVE_WITH_KNOTS ( 'NONE', 3,
 ( #9815, #42732, #19036, #43267, #76150, #2250, #41667, #74555, #68071, #100962, #629, #66471, #25529, #69670, #54512, #93949, #93419, #13001, #53989, #78806, #20646, #4937, #29253, #4398, #62134, #95024, #45927, #52403, #85322, #102569 ),
 .UNSPECIFIED., .F., .F.,
 ( 4, 2, 2, 2, 2, 2, 2, 2, 2, 2, 2, 2, 2, 2, 4 ),
 ( 0.002924093377768991441, 0.003854458377717581014, 0.004784823377666175791, 0.005715188377614770568, 0.006180370877589073594, 0.006645553377563376621, 0.007110735877537680515, 0.007343327127524836365, 0.007575918377511992215, 0.007808509627499148065, 0.008041100877486304782, 0.008506283377460621686, 0.008971465877434938591, 0.009436648377409257230, 0.01036701337735790318 ),
 .UNSPECIFIED. ) ;
#16725=B_SPLINE_CURVE_WITH_KNOTS ( 'NONE', 3,
 ( #75868, #35446, #44038, #3041, #35989, #9521, #18733, #51043, #34386, #85577, #42433, #34915, #68862, #51584, #42978, #67262, #44581, #75324, #77472, #33847, #2500, #58636, #83959, #10068, #91535, #84502, #92579, #17649, #26306, #26830 ),
 .UNSPECIFIED., .F., .F.,
 ( 4, 2, 2, 2, 2, 2, 2, 2, 2, 2, 2, 2, 2, 2, 4 ),
 ( 0.004754800762794661635, 0.005690253947496225727, 0.006157980539847006905, 0.006625707132197788951, 0.006859570428373176071, 0.007093433724548564925, 0.007327297020723952913, 0.007561160316899340900, 0.007795023613074728887, 0.008028886909250116874, 0.008496613501600898052, 0.009432066686302465613, 0.01036751987100403144, 0.01130297305570559900, 0.01223842624040716656 ),
 .UNSPECIFIED. ) ;
#16735=SURFACE_STYLE_USAGE ( .BOTH. , #90630 ) ;
#16737=SURFACE_SIDE_STYLE ('',( #57702 ) ) ;
#16741=CARTESIAN_POINT ( 'NONE',  ( 0.1685831701706822228, 25.16821295365200228, 40.75000000000013500 ) ) ;
#16748=MECHANICAL_DESIGN_GEOMETRIC_PRESENTATION_REPRESENTATION('',(#11577),#2959);
#16750=AXIS2_PLACEMENT_3D ( 'NONE', #44324, #21670, #87448 ) ;
#16752=CARTESIAN_POINT ( 'NONE',  ( 24.03417899433058835, 25.72120757053723494, 31.00649972266041132 ) ) ;
#16758=CARTESIAN_POINT ( 'NONE',  ( -4.151814662913274390, 52.11326435471435303, 6.758048296790627241 ) ) ;
#16769=AXIS2_PLACEMENT_3D ( 'NONE', #20016, #94402, #93858 ) ;
#16777=B_SPLINE_CURVE_WITH_KNOTS ( 'NONE', 3,
 ( #38265, #54382, #104017, #30160, #90498, #14462, #39312, #72194, #80265, #57050, #16609, #72711, #49499, #89967, #65694, #105098, #57576, #105612, #71643, #63591, #40351, #16073, #47374, #23136, #31237, #82405, #81849, #24202 ),
 .UNSPECIFIED., .F., .F.,
 ( 4, 2, 2, 2, 2, 2, 2, 2, 2, 2, 2, 2, 2, 4 ),
 ( 0.007040904414468415924, 0.007507994684082267001, 0.007741539818889188636, 0.007975084953696110271, 0.008208630088503032773, 0.008442175223309953541, 0.008909265492923810689, 0.009376355762537667837, 0.009843446032151523251, 0.01077762657137924275, 0.01171180711060696052, 0.01264598764983468002, 0.01358016818906239778, 0.01451434872829011555 ),
 .UNSPECIFIED. ) ;
#16817=CARTESIAN_POINT ( 'NONE',  ( 37.56673239365873940, 27.88554838446218653, 10.95617127780822564 ) ) ;
#16828=( LENGTH_UNIT ( ) NAMED_UNIT ( * ) SI_UNIT ( .MILLI., .METRE. ) );
#16834=B_SPLINE_CURVE_WITH_KNOTS ( 'NONE', 3,
 ( #105101, #65699, #98584, #72713, #89449, #24206, #15541, #16612, #82410, #8510, #7436, #23138, #40353, #48956, #106131, #32289, #39316, #47378, #81853, #74306, #57055, #40888, #383, #97000, #88389, #65159, #80268, #6381, #72196, #64131 ),
 .UNSPECIFIED., .F., .F.,
 ( 4, 2, 2, 2, 2, 2, 2, 2, 2, 2, 2, 2, 2, 2, 4 ),
 ( 0.006732386592399308353, 0.007201418480221453110, 0.007435934424132525054, 0.007670450368043596999, 0.007904966311954668076, 0.008139482255865740021, 0.008373998199776811965, 0.008608514143687885645, 0.009077546031510029534, 0.009546577919332173423, 0.01048464169497645079, 0.01142270547062072990, 0.01236076924626500900, 0.01329883302190928637, 0.01423689679755356548 ),
 .UNSPECIFIED. ) ;
#16839=CARTESIAN_POINT ( 'NONE',  ( -48.87836615495903914, 8.113987396617073244, -16.52312645342838238 ) ) ;
#16846=CARTESIAN_POINT ( 'NONE',  ( 17.89001738438794931, 45.34603189753767083, 5.216234635019720400 ) ) ;
#16860=CARTESIAN_POINT ( 'NONE',  ( -21.97741296367594543, 27.90380497738007293, -32.31715157276733663 ) ) ;
#16875=CARTESIAN_POINT ( 'NONE',  ( 38.75747312663246902, 27.29554786619022622, -12.59589368416849453 ) ) ;
#16888=STYLED_ITEM ( 'NONE', ( #100385 ), #42426 ) ;
#16895=CARTESIAN_POINT ( 'NONE',  ( 48.87836615495911730, 8.113987396617103443, 16.52312645342804842 ) ) ;
#16897=CARTESIAN_POINT ( 'NONE',  ( 1.249445774276175536, 43.67355798807202660, 17.33679506162915374 ) ) ;
#16917=VECTOR ( 'NONE', #16203, 1000.000000000000000 ) ;
#16946=( NAMED_UNIT ( * ) SI_UNIT ( $, .STERADIAN. ) SOLID_ANGLE_UNIT ( ) );
#16948=CARTESIAN_POINT ( 'NONE',  ( 16.32461263189640377, 43.58742806653211943, 6.626833409472919989 ) ) ;
#16963=CARTESIAN_POINT ( 'NONE',  ( -1.249013534494713751, 16.16290615548213694, 50.37193964746203534 ) ) ;
#16967=CARTESIAN_POINT ( 'NONE',  ( -0.3342755987430475195, 44.06880435339610358, -16.29260335467761323 ) ) ;
#16975=CARTESIAN_POINT ( 'NONE',  ( -9.267538580112278268, 46.19448214903181338, 13.41394971794136559 ) ) ;
#16980=CARTESIAN_POINT ( 'NONE',  ( -36.31529515053280477, 28.19075680830513875, 12.14815066672548305 ) ) ;
#16992=AXIS2_PLACEMENT_3D ( 'NONE', #35848, #43370, #92977 ) ;
#16994=CARTESIAN_POINT ( 'NONE',  ( 0.000000000000000000, 45.89575828009193259, -11.27631144943088337 ) ) ;
#17030=CARTESIAN_POINT ( 'NONE',  ( 38.64176212055058812, 25.32107803816180791, -11.54726517548278686 ) ) ;
#17033=CARTESIAN_POINT ( 'NONE',  ( -9.810861164843071691, 53.41087315403468239, 2.841314465358082852 ) ) ;
#17037=CARTESIAN_POINT ( 'NONE',  ( -0.4150371643087381601, 43.19867153370302759, 18.68204839779363624 ) ) ;
#17064=( NAMED_UNIT ( * ) SI_UNIT ( $, .STERADIAN. ) SOLID_ANGLE_UNIT ( ) );
#17082=ORIENTED_EDGE ( 'NONE', *, *, #57053, .F. ) ;
#17104=CARTESIAN_POINT ( 'NONE',  ( 47.55322331356174459, 10.90908589463668754, 16.76771630193798046 ) ) ;
#17112=MECHANICAL_DESIGN_GEOMETRIC_PRESENTATION_REPRESENTATION('',(#32597),#82535);
#17129=DIRECTION ( 'NONE',  ( 1.150791560227848051E-16, -0.3420201433256733758, 0.9396926207859066515 ) ) ;
#17132=CARTESIAN_POINT ( 'NONE',  ( -27.10511071441192144, 34.47735702144345282, -10.05698433968589178 ) ) ;
#17163=CARTESIAN_POINT ( 'NONE',  ( 22.13642162920427126, 27.78492472323462792, -32.60352800065684420 ) ) ;
#17168=CARTESIAN_POINT ( 'NONE',  ( -28.61312531052638519, 18.65874454358749190, 40.19656138064493689 ) ) ;
#17169=CARTESIAN_POINT ( 'NONE',  ( -15.89325899475126391, 43.76119630618126877, -6.420346730828080162 ) ) ;
#17196=CARTESIAN_POINT ( 'NONE',  ( -46.92658635379587651, 13.66002169525844145, 15.01004073971070341 ) ) ;
#17208=CARTESIAN_POINT ( 'NONE',  ( -5.290067270632215823, 53.47475093287481229, 8.531152949374556371 ) ) ;
#17229=CARTESIAN_POINT ( 'NONE',  ( -17.07866832072232910, 34.90909537143385677, -21.83975874131578720 ) ) ;
#17239=CARTESIAN_POINT ( 'NONE',  ( -29.27148335582101879, 13.57837266936924614, 39.67318301868861852 ) ) ;
#17296=VECTOR ( 'NONE', #99676, 1000.000000000000114 ) ;
#17303=COLOUR_RGB ( '', 0.40784314, 0.44705882, 0.49803922) ;
#17310=CARTESIAN_POINT ( 'NONE',  ( -4.504790317111235787, 52.18342994161649528, 6.294253490234988924 ) ) ;
#17338=CARTESIAN_POINT ( 'NONE',  ( 6.735557395310442615E-15, 0.000000000000000000, 55.00000000000000000 ) ) ;
#17360=FACE_BOUND ( 'NONE', #3771, .T. ) ;
#17374=VERTEX_POINT ( 'NONE', #94214 ) ;
#17394=CARTESIAN_POINT ( 'NONE',  ( 26.78521724860346254, 36.99578157268295797, -7.587698921419404385 ) ) ;
#17397=CARTESIAN_POINT ( 'NONE',  ( -22.01999690012023692, 28.11337147615393306, -31.58836928537003175 ) ) ;
#17405=ORIENTED_EDGE ( 'NONE', *, *, #96581, .F. ) ;
#17415=( NAMED_UNIT ( * ) PLANE_ANGLE_UNIT ( ) SI_UNIT ( $, .RADIAN. ) );
#17424=DIRECTION ( 'NONE',  ( 0.000000000000000000, 1.000000000000000000, 0.000000000000000000 ) ) ;
#17431=( GEOMETRIC_REPRESENTATION_CONTEXT ( 3 ) GLOBAL_UNCERTAINTY_ASSIGNED_CONTEXT ( ( #1399 ) ) GLOBAL_UNIT_ASSIGNED_CONTEXT ( ( #35187, #27106, #84774 ) ) REPRESENTATION_CONTEXT ( 'NONE', 'WORKASPACE' ) );
#17439=VECTOR ( 'NONE', #82962, 1000.000000000000000 ) ;
#17444=( GEOMETRIC_REPRESENTATION_CONTEXT ( 3 ) GLOBAL_UNCERTAINTY_ASSIGNED_CONTEXT ( ( #44029 ) ) GLOBAL_UNIT_ASSIGNED_CONTEXT ( ( #72237, #64166, #32335 ) ) REPRESENTATION_CONTEXT ( 'NONE', 'WORKASPACE' ) );
#17449=FACE_OUTER_BOUND ( 'NONE', #90083, .T. ) ;
#17450=SURFACE_SIDE_STYLE ('',( #75654 ) ) ;
#17464=CARTESIAN_POINT ( 'NONE',  ( -15.70312386038158792, 44.04645639395336332, 4.579973510850313900 ) ) ;
#17469=CARTESIAN_POINT ( 'NONE',  ( -21.97272370781284323, 27.95363515319932191, 32.15429476236987938 ) ) ;
#17484=CARTESIAN_POINT ( 'NONE',  ( 15.51790693666056065, 44.08177281019668925, 4.857540322262676291 ) ) ;
#17490=EDGE_CURVE ( 'NONE', #30746, #103131, #71453, .T. ) ;
#17499=CARTESIAN_POINT ( 'NONE',  ( -4.278756001540764409, 52.15505427271036609, -6.541747321572864315 ) ) ;
#17508=CARTESIAN_POINT ( 'NONE',  ( 1.101584607545897043, 45.52388203129090982, 18.11230536840457361 ) ) ;
#17509=CARTESIAN_POINT ( 'NONE',  ( 1.251018392637836651, 15.60415866083139136, -50.60639602862229935 ) ) ;
#17515=CARTESIAN_POINT ( 'NONE',  ( -47.03591514779362370, 18.70176887044695846, -14.84266952052386124 ) ) ;
#17536=CARTESIAN_POINT ( 'NONE',  ( 6.399925260777681757, 51.30561996063480024, 7.879653260259286363 ) ) ;
#17544=EDGE_CURVE ( 'NONE', #106075, #62805, #34274, .T. ) ;
#17551=( GEOMETRIC_REPRESENTATION_CONTEXT ( 3 ) GLOBAL_UNCERTAINTY_ASSIGNED_CONTEXT ( ( #97938 ) ) GLOBAL_UNIT_ASSIGNED_CONTEXT ( ( #4038, #14230, #4570 ) ) REPRESENTATION_CONTEXT ( 'NONE', 'WORKASPACE' ) );
#17555=CARTESIAN_POINT ( 'NONE',  ( -36.36519827644053038, 25.99686924827267731, 12.56069422975649630 ) ) ;
#17561=ORIENTED_EDGE ( 'NONE', *, *, #104872, .F. ) ;
#17567=VERTEX_POINT ( 'NONE', #58530 ) ;
#17568=CARTESIAN_POINT ( 'NONE',  ( 38.54716475372293871, 25.36783991978645147, -11.41422472833605006 ) ) ;
#17571=CARTESIAN_POINT ( 'NONE',  ( -9.749942471036476377, 53.39674074574894291, 3.171770270685806636 ) ) ;
#17590=CARTESIAN_POINT ( 'NONE',  ( 26.49164619350623440, 34.70556741407747126, 9.907652308642946437 ) ) ;
#17600=EDGE_LOOP ( 'NONE', ( #69826, #70623 ) ) ;
#17616=CARTESIAN_POINT ( 'NONE',  ( 0.000000000000000000, 23.58303312036771615, 0.000000000000000000 ) ) ;
#17623=CARTESIAN_POINT ( 'NONE',  ( 0.08413355536092814724, 53.39766064372320642, -10.25000000000000000 ) ) ;
#17637=CARTESIAN_POINT ( 'NONE',  ( -15.93287854420827721, 36.64197083639891872, -24.00465449142953744 ) ) ;
#17640=CARTESIAN_POINT ( 'NONE',  ( 47.44481056709881273, 11.19259812317959124, 16.71748578406432273 ) ) ;
#17648=ORIENTED_EDGE ( 'NONE', *, *, #8900, .F. ) ;
#17649=CARTESIAN_POINT ( 'NONE',  ( -47.78242936231056603, 10.33916499670815270, -16.83675847388958147 ) ) ;
#17653=VERTEX_POINT ( 'NONE', #74157 ) ;
#17666=( NAMED_UNIT ( * ) SI_UNIT ( $, .STERADIAN. ) SOLID_ANGLE_UNIT ( ) );
#17678=CARTESIAN_POINT ( 'NONE',  ( 17.94999111897404731, 36.38767359518976718, -23.42285042635058900 ) ) ;
#17695=CARTESIAN_POINT ( 'NONE',  ( -28.71513376685318164, 15.67191133428136673, 41.65496614056284841 ) ) ;
#17700=( GEOMETRIC_REPRESENTATION_CONTEXT ( 3 ) GLOBAL_UNCERTAINTY_ASSIGNED_CONTEXT ( ( #20058 ) ) GLOBAL_UNIT_ASSIGNED_CONTEXT ( ( #69265, #5564, #28291 ) ) REPRESENTATION_CONTEXT ( 'NONE', 'WORKASPACE' ) );
#17712=ORIENTED_EDGE ( 'NONE', *, *, #69849, .F. ) ;
#17722=CARTESIAN_POINT ( 'NONE',  ( -47.24160628166287523, 11.75468494072141112, 16.58444347056430956 ) ) ;
#17739=CARTESIAN_POINT ( 'NONE',  ( -29.85155995213069247, 18.03343143632516643, 39.61445771744197231 ) ) ;
#17746=EDGE_CURVE ( 'NONE', #7616, #20102, #82253, .T. ) ;
#17757=CARTESIAN_POINT ( 'NONE',  ( -6.133251129394694523, 51.27079673972909291, -8.207848847617324139 ) ) ;
#17764=CARTESIAN_POINT ( 'NONE',  ( -29.59213159313646457, 8.427504962981458903, 42.10535821593508388 ) ) ;
#17781=CARTESIAN_POINT ( 'NONE',  ( -17.89009921150046623, 43.21754357103051092, -5.217241991157013814 ) ) ;
#17782=CARTESIAN_POINT ( 'NONE',  ( -1.098564211878685359, 45.97059960990146266, -16.88266418162399063 ) ) ;
#17793=B_SPLINE_CURVE_WITH_KNOTS ( 'NONE', 3,
 ( #18305, #10180, #35032, #68439, #91463, #41829, #15428, #65580, #7325, #25704, #57465, #89856, #65046, #74187, #66642, #41300, #83351, #25148, #33233, #90388 ),
 .UNSPECIFIED., .F., .F.,
 ( 4, 2, 2, 2, 2, 2, 2, 2, 2, 4 ),
 ( 0.003226290335689578279, 0.003730299423990245979, 0.004234308512290913679, 0.004738317600591582246, 0.005242326688892249079, 0.005746335777192917646, 0.006250344865493585346, 0.006502349409643918762, 0.006754353953794253046, 0.007258363042094923348 ),
 .UNSPECIFIED. ) ;
#17804=CARTESIAN_POINT ( 'NONE',  ( 2.607260012660386551E-19, 12.91535575337012354, -51.75000000000000711 ) ) ;
#17814=DIRECTION ( 'NONE',  ( -0.000000000000000000, 1.000000000000000000, -0.000000000000000000 ) ) ;
#17835=ADVANCED_FACE ( 'NONE', ( #91179 ), #105735, .F. ) ;
#17838=CARTESIAN_POINT ( 'NONE',  ( 5.125111398410182595, 53.50866886000678591, 8.522916231725279346 ) ) ;
#17846=CARTESIAN_POINT ( 'NONE',  ( 30.92866670662933615, 8.704003156311262757, -40.98833526575349140 ) ) ;
#17869=CARTESIAN_POINT ( 'NONE',  ( -0.6450442877596542779, 54.23802003939768923, 7.916300680330227379 ) ) ;
#17884=EDGE_CURVE ( 'NONE', #63425, #83087, #58803, .T. ) ;
#17885=CARTESIAN_POINT ( 'NONE',  ( 37.56673239365870387, 25.47613764497372557, 13.45617127780999134 ) ) ;
#17887=DIRECTION ( 'NONE',  ( 0.000000000000000000, 1.000000000000000000, 0.000000000000000000 ) ) ;
#17904=FILL_AREA_STYLE ('',( #83664 ) ) ;
#17924=( GEOMETRIC_REPRESENTATION_CONTEXT ( 3 ) GLOBAL_UNCERTAINTY_ASSIGNED_CONTEXT ( ( #51293 ) ) GLOBAL_UNIT_ASSIGNED_CONTEXT ( ( #29240, #86916, #38371 ) ) REPRESENTATION_CONTEXT ( 'NONE', 'WORKASPACE' ) );
#17927=CARTESIAN_POINT ( 'NONE',  ( 25.88357335569430262, 37.21352753314932471, -8.492829661866421631 ) ) ;
#17939=ORIENTED_EDGE ( 'NONE', *, *, #84944, .F. ) ;
#17941=CYLINDRICAL_SURFACE ( 'NONE', #26976, 1.250000000000001110 ) ;
#17953=CARTESIAN_POINT ( 'NONE',  ( 1.219574468913127818, 34.50199799138920298, -28.81730245403649704 ) ) ;
#17957=CARTESIAN_POINT ( 'NONE',  ( 8.239141761615604409, 51.66651536930677935, 3.999746327760523634 ) ) ;
#17973=CARTESIAN_POINT ( 'NONE',  ( -8.559508646656381003, 51.83514083332404709, -1.531152949374265049 ) ) ;
#17974=FACE_BOUND ( 'NONE', #137, .T. ) ;
#17975=CARTESIAN_POINT ( 'NONE',  ( 36.48155966215278312, 26.06893451358279279, 11.58015166401925455 ) ) ;
#17977=CARTESIAN_POINT ( 'NONE',  ( 9.089024885614422899, 43.98902913643783563, -13.78910996109302189 ) ) ;
#17982=ORIENTED_EDGE ( 'NONE', *, *, #48061, .F. ) ;
#17994=CARTESIAN_POINT ( 'NONE',  ( 28.31356611659730760, 36.37420247609845347, -8.448101363750753379 ) ) ;
#17996=CARTESIAN_POINT ( 'NONE',  ( -22.88454736421212488, 28.18015032983888801, 30.73969532942450300 ) ) ;
#17998=CARTESIAN_POINT ( 'NONE',  ( -3.840629472727446691E-14, -1.200000000000000030E-05, -28.50000000000000000 ) ) ;
#18014=CARTESIAN_POINT ( 'NONE',  ( -49.18736646279123903, 13.60337276043701671, 15.12866845614360223 ) ) ;
#18016=SURFACE_STYLE_FILL_AREA ( #91890 ) ;
#18017=CARTESIAN_POINT ( 'NONE',  ( 8.377077475354079672E-17, 56.87938524157181774, 0.6840402866513453084 ) ) ;
#18018=EDGE_CURVE ( 'NONE', #3192, #74150, #30422, .T. ) ;
#18032=CARTESIAN_POINT ( 'NONE',  ( 2.099928008175702901E-23, 44.08548369317413318, -16.25000000000000000 ) ) ;
#18040=CARTESIAN_POINT ( 'NONE',  ( 1.235826360310026795, 15.32379192987240657, -50.72445113533566285 ) ) ;
#18044=CARTESIAN_POINT ( 'NONE',  ( -9.177423055815456365, 46.16989776044872684, 13.55706802408392164 ) ) ;
#18056=CARTESIAN_POINT ( 'NONE',  ( -16.58625408824827119, 35.02807148468932752, -21.80698433968594685 ) ) ;
#18068=CARTESIAN_POINT ( 'NONE',  ( 6.536739755986783251, 51.40531100843265477, 7.403841948493273151 ) ) ;
#18080=CARTESIAN_POINT ( 'NONE',  ( 5.290067270632158980, 51.34639538792298197, -8.531152949374604333 ) ) ;
#18083=DIRECTION ( 'NONE',  ( 0.000000000000000000, 0.000000000000000000, -1.000000000000000000 ) ) ;
#18098=B_SPLINE_CURVE_WITH_KNOTS ( 'NONE', 3,
 ( #68191, #11530, #76275, #60657, #2383, #36408, #35329, #44457, #18607, #51469, #84384, #84914, #85999, #35870, #77352, #3998, #3465, #28302, #10999, #77886, #43917, #19161, #94063, #20228, #60135, #53078, #45001, #69793, #10473, #102688 ),
 .UNSPECIFIED., .F., .F.,
 ( 4, 2, 2, 2, 2, 2, 2, 2, 2, 2, 2, 2, 2, 2, 4 ),
 ( 0.01009607051181166983, 0.01101525429224240425, 0.01193443807267314041, 0.01285362185310387484, 0.01377280563353460927, 0.01423239752374997821, 0.01446219346885766269, 0.01469198941396534716, 0.01492178535907303163, 0.01515158130418071611, 0.01538137724928840058, 0.01561117319439608506, 0.01607076508461143666, 0.01653035697482678826, 0.01744954075525749146 ),
 .UNSPECIFIED. ) ;
#18119=MECHANICAL_DESIGN_GEOMETRIC_PRESENTATION_REPRESENTATION('',(#74972),#97317);
#18126=CARTESIAN_POINT ( 'NONE',  ( 1.101047506738523696, 27.52289228718336034, 40.11312307701721380 ) ) ;
#18143=UNCERTAINTY_MEASURE_WITH_UNIT (LENGTH_MEASURE( 1.000000000000000082E-05 ), #43549, 'distance_accuracy_value', 'NONE');
#18144=VERTEX_POINT ( 'NONE', #40882 ) ;
#18145=( NAMED_UNIT ( * ) PLANE_ANGLE_UNIT ( ) SI_UNIT ( $, .RADIAN. ) );
#18162=ORIENTED_EDGE ( 'NONE', *, *, #58820, .F. ) ;
#18173=CARTESIAN_POINT ( 'NONE',  ( 47.24099558602568294, 11.75653836616716141, 16.58383527959104242 ) ) ;
#18185=CARTESIAN_POINT ( 'NONE',  ( -36.81189781133993932, 25.99449293029668340, -11.20643870584772550 ) ) ;
#18197=( GEOMETRIC_REPRESENTATION_CONTEXT ( 3 ) GLOBAL_UNCERTAINTY_ASSIGNED_CONTEXT ( ( #19654 ) ) GLOBAL_UNIT_ASSIGNED_CONTEXT ( ( #16646, #41449, #101295 ) ) REPRESENTATION_CONTEXT ( 'NONE', 'WORKASPACE' ) );
#18199=STYLED_ITEM ( 'NONE', ( #39130 ), #22488 ) ;
#18207=CARTESIAN_POINT ( 'NONE',  ( 17.64253364725055206, 45.32498240469067952, -6.177274125185148179 ) ) ;
#18215=UNCERTAINTY_MEASURE_WITH_UNIT (LENGTH_MEASURE( 1.000000000000000082E-05 ), #20619, 'distance_accuracy_value', 'NONE');
#18226=CARTESIAN_POINT ( 'NONE',  ( 15.64225497181437419, 35.03862301904531762, -22.45844242034788962 ) ) ;
#18236=CARTESIAN_POINT ( 'NONE',  ( -29.50962187807867210, 13.72866526111396546, 42.09567151085925474 ) ) ;
#18240=CARTESIAN_POINT ( 'NONE',  ( -22.88866733252017482, 25.33094138452381827, 33.17289542880824627 ) ) ;
#18250=CARTESIAN_POINT ( 'NONE',  ( -0.7772950121166072313, 27.39127224023426166, 40.48240021764166130 ) ) ;
#18277=CARTESIAN_POINT ( 'NONE',  ( 9.106558737793045921, 53.52158284938358435, 3.908029755355241441 ) ) ;
#18284=CARTESIAN_POINT ( 'NONE',  ( -37.56673239365849781, 27.88554838446201600, 10.95617127781066102 ) ) ;
#18300=CARTESIAN_POINT ( 'NONE',  ( -5.290067270634260410, 52.08006895350597176, -6.031152949369843697 ) ) ;
#18305=CARTESIAN_POINT ( 'NONE',  ( -3.381870600466846067E-15, 46.21383923812598482, -16.24999999999995026 ) ) ;
#18332=MECHANICAL_DESIGN_GEOMETRIC_PRESENTATION_REPRESENTATION('',(#51005),#33888);
#18345=AXIS2_PLACEMENT_3D ( 'NONE', #38436, #62699, #95591 ) ;
#18373=UNCERTAINTY_MEASURE_WITH_UNIT (LENGTH_MEASURE( 1.000000000000000082E-05 ), #3066, 'distance_accuracy_value', 'NONE');
#18378=ORIENTED_EDGE ( 'NONE', *, *, #93016, .T. ) ;
#18392=( NAMED_UNIT ( * ) PLANE_ANGLE_UNIT ( ) SI_UNIT ( $, .RADIAN. ) );
#18408=CARTESIAN_POINT ( 'NONE',  ( -0.7842673370667302413, 54.19802454029581895, 8.013341487591407741 ) ) ;
#18422=CARTESIAN_POINT ( 'NONE',  ( -5.930617632350569934, 51.27007761046171908, 8.357863051050422598 ) ) ;
#18428=CARTESIAN_POINT ( 'NONE',  ( 36.36462878256535447, 25.99729457938612143, -12.55876404825913362 ) ) ;
#18430=CARTESIAN_POINT ( 'NONE',  ( -1.010844465928027569, 37.02277097779673909, -27.74667697905033492 ) ) ;
#18436=CARTESIAN_POINT ( 'NONE',  ( -16.64348903516521005, 45.88445698070336221, -4.157797401561533768 ) ) ;
#18459=EDGE_CURVE ( 'NONE', #38799, #17374, #35388, .T. ) ;
#18461=FILL_AREA_STYLE ('',( #66452 ) ) ;
#18472=( LENGTH_UNIT ( ) NAMED_UNIT ( * ) SI_UNIT ( .MILLI., .METRE. ) );
#18477=SURFACE_SIDE_STYLE ('',( #16320 ) ) ;
#18480=PRESENTATION_STYLE_ASSIGNMENT (( #83185 ) ) ;
#18495=COLOUR_RGB ( '', 0.09019608, 0.27058824, 0.51372549) ;
#18518=CARTESIAN_POINT ( 'NONE',  ( 9.520703147840279712, 43.48472836740506153, -15.15874889920861968 ) ) ;
#18524=AXIS2_PLACEMENT_3D ( 'NONE', #29449, #36483, #11072 ) ;
#18530=MECHANICAL_DESIGN_GEOMETRIC_PRESENTATION_REPRESENTATION('',(#1534),#83958);
#18531=ORIENTED_EDGE ( 'NONE', *, *, #64773, .T. ) ;
#18554=CARTESIAN_POINT ( 'NONE',  ( 46.97732051764557326, 17.75298140206541220, -16.28617214199182328 ) ) ;
#18555=CARTESIAN_POINT ( 'NONE',  ( -11.06541635813348101, 43.17498430620472760, 15.13886682000006800 ) ) ;
#18568=SURFACE_STYLE_FILL_AREA ( #66025 ) ;
#18580=MECHANICAL_DESIGN_GEOMETRIC_PRESENTATION_REPRESENTATION('',(#47782),#68457);
#18589=COLOUR_RGB ( '', 0.08235294, 0.09019608, 0.10196078) ;
#18590=CARTESIAN_POINT ( 'NONE',  ( -47.78256487607072245, 15.50824688151216257, -16.83670797542569986 ) ) ;
#18598=CARTESIAN_POINT ( 'NONE',  ( -15.67130090876874604, 34.65698101724829172, -23.70546282029701857 ) ) ;
#18607=CARTESIAN_POINT ( 'NONE',  ( 49.15776748649641092, 8.563726824893073797, -15.04013919214091466 ) ) ;
#18609=COLOUR_RGB ( '', 0.08235294, 0.09019608, 0.10196078) ;
#18624=CARTESIAN_POINT ( 'NONE',  ( 6.303135229827225849, 51.28796181275954069, -8.018170099117096328 ) ) ;
#18652=FILL_AREA_STYLE_COLOUR ( '', #106286 ) ;
#18658=FILL_AREA_STYLE_COLOUR ( '', #93383 ) ;
#18673=CARTESIAN_POINT ( 'NONE',  ( -30.88008372391045242, 8.315965929874618467, -41.22858563418540712 ) ) ;
#18696=B_SPLINE_CURVE_WITH_KNOTS ( 'NONE', 3,
 ( #72542, #104930, #24561, #56339, #7265, #55801, #8333, #89803, #15901, #48255, #81156, #88737, #31071, #57406, #32650, #40176, #33174, #73051, #80624, #105962, #24035, #90322, #7794, #98410, #39667, #41237, #63949, #211 ),
 .UNSPECIFIED., .F., .F.,
 ( 4, 2, 2, 2, 2, 2, 2, 2, 2, 2, 2, 2, 2, 4 ),
 ( 0.002626378601955864887, 0.003560090090687840179, 0.004493801579419815471, 0.005427513068151789896, 0.006361224556883765188, 0.006828080301249753702, 0.007061508173432749259, 0.007294936045615743950, 0.007528363917798739507, 0.007761791789981735065, 0.008228647534347722711, 0.008695503278713710357, 0.009162359023079696269, 0.01009607051181166983 ),
 .UNSPECIFIED. ) ;
#18705=( GEOMETRIC_REPRESENTATION_CONTEXT ( 3 ) GLOBAL_UNCERTAINTY_ASSIGNED_CONTEXT ( ( #26548 ) ) GLOBAL_UNIT_ASSIGNED_CONTEXT ( ( #51975, #67651, #76785 ) ) REPRESENTATION_CONTEXT ( 'NONE', 'WORKASPACE' ) );
#18718=CARTESIAN_POINT ( 'NONE',  ( -15.50007054317033628, 37.03005157377465650, -23.01145510268015926 ) ) ;
#18733=CARTESIAN_POINT ( 'NONE',  ( -47.29503607946688248, 13.12332669628135484, -14.58854632476132629 ) ) ;
#18736=CARTESIAN_POINT ( 'NONE',  ( -36.94914368061458987, 25.95618448055659755, -11.11629759539213502 ) ) ;
#18771=AXIS2_PLACEMENT_3D ( 'NONE', #75871, #51045, #51587 ) ;
#18777=CARTESIAN_POINT ( 'NONE',  ( 15.66935158561425290, 34.65848964118274012, -23.70178274125795070 ) ) ;
#18778=PRESENTATION_STYLE_ASSIGNMENT (( #68364 ) ) ;
#18803=CARTESIAN_POINT ( 'NONE',  ( -0.1698221021441387313, 27.29656849860388235, 40.74999999999998579 ) ) ;
#18805=ORIENTED_EDGE ( 'NONE', *, *, #19305, .T. ) ;
#18815=CARTESIAN_POINT ( 'NONE',  ( -8.239065070776058874, 53.79488990884892274, -3.999784715952824143 ) ) ;
#18826=CARTESIAN_POINT ( 'NONE',  ( 15.70492864000501143, 46.17438344839472819, 4.577980962366692275 ) ) ;
#18829=DIRECTION ( 'NONE',  ( -0.000000000000000000, 1.000000000000000000, -0.000000000000000000 ) ) ;
#18832=DIRECTION ( 'NONE',  ( -0.000000000000000000, -1.000000000000000000, -0.000000000000000000 ) ) ;
#18882=CARTESIAN_POINT ( 'NONE',  ( 0.6452391198540656791, 36.35841920418370421, 29.58352460202021206 ) ) ;
#18884=ORIENTED_EDGE ( 'NONE', *, *, #106116, .F. ) ;
#18885=CARTESIAN_POINT ( 'NONE',  ( -4.205728106920963327, 53.86358984174591313, 7.922788842214678162 ) ) ;
#18897=CARTESIAN_POINT ( 'NONE',  ( -15.45347762069378383, 46.21495662470459820, 5.015962831654086074 ) ) ;
#18937=CONICAL_SURFACE ( 'NONE', #96445, 45.10524579772351217, 0.3972631705159501148 ) ;
#18938=LINE ( 'NONE', #51236, #39036 ) ;
#18945=STYLED_ITEM ( 'NONE', ( #35515 ), #69567 ) ;
#18948=SURFACE_STYLE_FILL_AREA ( #100873 ) ;
#18949=EDGE_CURVE ( 'NONE', #12439, #17653, #44340, .T. ) ;
#18967=CYLINDRICAL_SURFACE ( 'NONE', #2392, 1.250000000000001110 ) ;
#18977=CARTESIAN_POINT ( 'NONE',  ( -0.7864879193441504102, 36.39291929247367818, -29.48511154656912936 ) ) ;
#18978=CYLINDRICAL_SURFACE ( 'NONE', #94289, 1.250000000000001110 ) ;
#18982=CARTESIAN_POINT ( 'NONE',  ( -16.48315964343910167, 45.94107222901597964, -4.157797401561528439 ) ) ;
#18994=CARTESIAN_POINT ( 'NONE',  ( -1.093451710897897389, 45.52449153923928549, 18.11105145254594007 ) ) ;
#18995=VECTOR ( 'NONE', #81330, 1000.000000000000000 ) ;
#18999=CARTESIAN_POINT ( 'NONE',  ( -28.35333406767821884, 36.33371803105157483, 8.700175216043216864 ) ) ;
#19001=CARTESIAN_POINT ( 'NONE',  ( -48.15042790184227073, 11.33351092753205336, -14.35535821593460071 ) ) ;
#19027=CARTESIAN_POINT ( 'NONE',  ( 30.93146042459050804, 14.42085588385340778, -40.69811146320466833 ) ) ;
#19028=SURFACE_SIDE_STYLE ('',( #91815 ) ) ;
#19036=CARTESIAN_POINT ( 'NONE',  ( -47.78396355473400803, 15.50490861890658323, 16.83695313132053428 ) ) ;
#19040=CARTESIAN_POINT ( 'NONE',  ( 1.107728337459903178, 17.28511502408344214, 49.90434249749426954 ) ) ;
#19068=CARTESIAN_POINT ( 'NONE',  ( -0.9537700198956184927, 8.769399064309570946, -51.31178202143230749 ) ) ;
#19070=CARTESIAN_POINT ( 'NONE',  ( -17.08200492518427183, 36.32755554593312297, 24.26548702208081565 ) ) ;
#19083=AXIS2_PLACEMENT_3D ( 'NONE', #7979, #40891, #73777 ) ;
#19105=ORIENTED_EDGE ( 'NONE', *, *, #59012, .F. ) ;
#19113=PRESENTATION_STYLE_ASSIGNMENT (( #35823 ) ) ;
#19118=EDGE_LOOP ( 'NONE', ( #84459, #65015, #48206, #56433 ) ) ;
#19142=ADVANCED_FACE ( 'NONE', ( #13984 ), #105656, .F. ) ;
#19158=ADVANCED_FACE ( 'NONE', ( #64680 ), #81902, .F. ) ;
#19161=CARTESIAN_POINT ( 'NONE',  ( 48.91361122442920362, 8.059984797525084232, -16.48958644079329972 ) ) ;
#19191=CARTESIAN_POINT ( 'NONE',  ( 0.8433902809040685344, 8.501990100278735696, 51.42592703772288587 ) ) ;
#19193=EDGE_CURVE ( 'NONE', #41746, #9858, #105208, .T. ) ;
#19194=B_SPLINE_CURVE_WITH_KNOTS ( 'NONE', 3,
 ( #55090, #45969, #45442, #61640, #47005, #14098, #6013, #38937, #30869, #86450, #63749, #96636, #85912, #11987, #44917, #77801, #94532, #69712, #102605, #20683 ),
 .UNSPECIFIED., .F., .F.,
 ( 4, 2, 2, 2, 2, 2, 2, 2, 2, 4 ),
 ( 0.003623855290150441045, 0.004630762948664648646, 0.005134216777921752663, 0.005637670607178856680, 0.005889397521807407387, 0.006141124436435958095, 0.006644578265693064714, 0.006896305180321615422, 0.007148032094950166129, 0.007651485924207265810 ),
 .UNSPECIFIED. ) ;
#19198=CARTESIAN_POINT ( 'NONE',  ( 38.56636269275068685, 25.18999535537753331, -12.97483823376252410 ) ) ;
#19208=( LENGTH_UNIT ( ) NAMED_UNIT ( * ) SI_UNIT ( .MILLI., .METRE. ) );
#19233=CARTESIAN_POINT ( 'NONE',  ( 9.533652678419262116, 53.58338683237839462, -1.993657782990515992 ) ) ;
#19258=( NAMED_UNIT ( * ) SI_UNIT ( $, .STERADIAN. ) SOLID_ANGLE_UNIT ( ) );
#19268=CIRCLE ( 'NONE', #50217, 35.82893434829263413 ) ;
#19273=CARTESIAN_POINT ( 'NONE',  ( -48.02835407290516656, 11.61227450977240494, 14.35535821593516559 ) ) ;
#19278=EDGE_CURVE ( 'NONE', #20459, #103579, #12230, .T. ) ;
#19279=CARTESIAN_POINT ( 'NONE',  ( -15.73424097804746324, 37.19149822104526493, -22.31191215652655657 ) ) ;
#19305=EDGE_CURVE ( 'NONE', #22672, #83885, #98387, .T. ) ;
#19318=FACE_OUTER_BOUND ( 'NONE', #15810, .T. ) ;
#19323=CARTESIAN_POINT ( 'NONE',  ( 17.77146113466383426, 36.31761464240111081, -23.79974184213102362 ) ) ;
#19326=PRESENTATION_STYLE_ASSIGNMENT (( #93159 ) ) ;
#19337=DIRECTION ( 'NONE',  ( -0.000000000000000000, -1.000000000000000000, -0.000000000000000000 ) ) ;
#19364=LINE ( 'NONE', #100744, #22040 ) ;
#19415=CARTESIAN_POINT ( 'NONE',  ( -0.6457278711330333154, 45.36073317496411050, -18.58332603715044584 ) ) ;
#19419=CARTESIAN_POINT ( 'NONE',  ( -24.44510943275183124, 25.27280235212049675, -32.24409512226776542 ) ) ;
#19426=CARTESIAN_POINT ( 'NONE',  ( 15.73298926836839229, 37.19132885152138357, -22.31337215277972419 ) ) ;
#19447=CARTESIAN_POINT ( 'NONE',  ( -16.64348903516521005, -1.200000000000000030E-05, -4.157797401561533768 ) ) ;
#19460=MECHANICAL_DESIGN_GEOMETRIC_PRESENTATION_REPRESENTATION('',(#98616),#93496);
#19462=ORIENTED_EDGE ( 'NONE', *, *, #106511, .T. ) ;
#19484=CARTESIAN_POINT ( 'NONE',  ( 8.559508646656407649, -1.200000000000000030E-05, 2.781152949374444461 ) ) ;
#19490=SURFACE_STYLE_FILL_AREA ( #100879 ) ;
#19499=CARTESIAN_POINT ( 'NONE',  ( 24.46190898409538406, 27.53854914924986730, 31.75601090834086904 ) ) ;
#19508=FILL_AREA_STYLE ('',( #28120 ) ) ;
#19520=CARTESIAN_POINT ( 'NONE',  ( 0.000000000000000000, 29.56666008184760130, -34.51297463494397988 ) ) ;
#19537=CARTESIAN_POINT ( 'NONE',  ( -49.03380706566419889, 8.971284072415123489, -14.85953237006457783 ) ) ;
#19573=CARTESIAN_POINT ( 'NONE',  ( 17.51155336591212830, 34.75093603301226608, 22.05173959547846252 ) ) ;
#19578=CARTESIAN_POINT ( 'NONE',  ( 0.8348441572799575328, 18.10288867187672324, 49.56646071010256094 ) ) ;
#19591=SURFACE_STYLE_USAGE ( .BOTH. , #101523 ) ;
#19600=CARTESIAN_POINT ( 'NONE',  ( -7.346560218009842380, 52.17944658692381665, -2.467458042133138907 ) ) ;
#19606=CARTESIAN_POINT ( 'NONE',  ( -17.77146113466401545, 36.31761464240112502, 23.79974184213090638 ) ) ;
#19615=STYLED_ITEM ( 'NONE', ( #30192 ), #84617 ) ;
#19644=CARTESIAN_POINT ( 'NONE',  ( 46.86921974295913884, 18.15560460139400689, -16.08157171274295649 ) ) ;
#19648=CARTESIAN_POINT ( 'NONE',  ( -49.27995299967503939, 13.03636147101657983, 15.63012893016903249 ) ) ;
#19653=SURFACE_SIDE_STYLE ('',( #87010 ) ) ;
#19654=UNCERTAINTY_MEASURE_WITH_UNIT (LENGTH_MEASURE( 1.000000000000000082E-05 ), #16646, 'distance_accuracy_value', 'NONE');
#19674=CARTESIAN_POINT ( 'NONE',  ( -47.29386731606042815, 18.29473622529003762, -14.58939859131310790 ) ) ;
#19680=PRESENTATION_STYLE_ASSIGNMENT (( #29356 ) ) ;
#19691=EDGE_CURVE ( 'NONE', #59863, #65026, #82706, .T. ) ;
#19692=EDGE_LOOP ( 'NONE', ( #78633, #93442, #76260, #94962 ) ) ;
#19694=FACE_OUTER_BOUND ( 'NONE', #49191, .T. ) ;
#19696=CARTESIAN_POINT ( 'NONE',  ( 6.068575646150123681, 51.26875262032900338, 8.262755242866147043 ) ) ;
#19707=CARTESIAN_POINT ( 'NONE',  ( -29.68315524076957246, 18.29184282782463455, 39.60535821593508388 ) ) ;
#19740=CARTESIAN_POINT ( 'NONE',  ( 30.64007947709951196, 12.99638611018202283, 41.66214316769377746 ) ) ;
#19748=EDGE_CURVE ( 'NONE', #43603, #100209, #95716, .T. ) ;
#19752=CARTESIAN_POINT ( 'NONE',  ( 0.4142243125050798502, 28.18107813451710442, 38.31766717693767532 ) ) ;
#19774=FACE_BOUND ( 'NONE', #13396, .T. ) ;
#19788=ORIENTED_EDGE ( 'NONE', *, *, #88459, .F. ) ;
#19789=DIRECTION ( 'NONE',  ( 0.000000000000000000, 0.000000000000000000, 1.000000000000000000 ) ) ;
#19810=FACE_BOUND ( 'NONE', #89145, .T. ) ;
#19815=CARTESIAN_POINT ( 'NONE',  ( 5.689121120886425409, 54.09406011002712944, 6.093839483979978766 ) ) ;
#19827=B_SPLINE_CURVE_WITH_KNOTS ( 'NONE', 3,
 ( #3417, #52479, #76757, #102097, #77836, #10426, #59538, #92947, #94017, #92406, #18555, #93499, #9893, #34751, #3947, #11480 ),
 .UNSPECIFIED., .F., .F.,
 ( 4, 2, 2, 2, 2, 2, 2, 4 ),
 ( 0.006919675597518590293, 0.007926800617648671263, 0.008933925637778750498, 0.009437488147843788380, 0.009941050657908824528, 0.01019283191294134347, 0.01044461316797386241, 0.01094817567803889682 ),
 .UNSPECIFIED. ) ;
#19830=CARTESIAN_POINT ( 'NONE',  ( 29.59437054465009354, 13.24940423479646157, -39.60535821593528283 ) ) ;
#19845=CARTESIAN_POINT ( 'NONE',  ( 17.15361759915018425, 37.01177862285504716, -21.87054431129734411 ) ) ;
#19847=ORIENTED_EDGE ( 'NONE', *, *, #72729, .F. ) ;
#19871=DIRECTION ( 'NONE',  ( 0.000000000000000000, 0.000000000000000000, 1.000000000000000000 ) ) ;
#19875=CARTESIAN_POINT ( 'NONE',  ( -1.250030556990739061, 27.68693347593793774, 39.65778548936075509 ) ) ;
#19876=CARTESIAN_POINT ( 'NONE',  ( 0.8406291878555783859, 36.41282694755211224, -29.42872758306872427 ) ) ;
#19893=EDGE_LOOP ( 'NONE', ( #65662, #18162 ) ) ;
#19897=ORIENTED_EDGE ( 'NONE', *, *, #35011, .F. ) ;
#19932=EDGE_CURVE ( 'NONE', #66410, #21651, #66551, .T. ) ;
#19933=ORIENTED_EDGE ( 'NONE', *, *, #62351, .F. ) ;
#19966=B_SPLINE_CURVE_WITH_KNOTS ( 'NONE', 3,
 ( #56711, #15733, #65354, #98245, #93360, #44276, #92812, #61540, #85259, #68561, #59947, #18422, #52892, #100370, #3816, #28653 ),
 .UNSPECIFIED., .F., .F.,
 ( 4, 2, 2, 2, 2, 2, 2, 4 ),
 ( 0.006917039672641533445, 0.007923839859808178010, 0.008930640046974823443, 0.009434040140558146159, 0.009937440234141472345, 0.01018914028093313197, 0.01044084032772479333, 0.01094424042130811431 ),
 .UNSPECIFIED. ) ;
#19985=STYLED_ITEM ( 'NONE', ( #49835 ), #88434 ) ;
#20009=CYLINDRICAL_SURFACE ( 'NONE', #57948, 1.250000000000001110 ) ;
#20016=CARTESIAN_POINT ( 'NONE',  ( 27.10511071441197117, -1.200000000000000030E-05, 8.806984339685705265 ) ) ;
#20040=DIRECTION ( 'NONE',  ( 0.000000000000000000, -0.9221233147934838614, -0.3868961001538753219 ) ) ;
#20058=UNCERTAINTY_MEASURE_WITH_UNIT (LENGTH_MEASURE( 1.000000000000000082E-05 ), #69265, 'distance_accuracy_value', 'NONE');
#20083=EDGE_CURVE ( 'NONE', #66067, #89428, #74506, .T. ) ;
#20086=ORIENTED_EDGE ( 'NONE', *, *, #12577, .F. ) ;
#20097=ORIENTED_EDGE ( 'NONE', *, *, #71259, .F. ) ;
#20102=VERTEX_POINT ( 'NONE', #56 ) ;
#20106=CARTESIAN_POINT ( 'NONE',  ( -29.33008799483348028, 13.53038725678829124, -39.65490270820011887 ) ) ;
#20112=DIRECTION ( 'NONE',  ( 0.000000000000000000, 0.000000000000000000, 1.000000000000000000 ) ) ;
#20118=DIRECTION ( 'NONE',  ( -0.000000000000000000, -1.000000000000000000, -0.000000000000000000 ) ) ;
#20132=CARTESIAN_POINT ( 'NONE',  ( -9.169574833318794305, 51.60709747164507633, -1.678735602677582373 ) ) ;
#20144=CARTESIAN_POINT ( 'NONE',  ( -4.448391904179714196, 54.30568176866136554, -6.353132081348096705 ) ) ;
#20148=CARTESIAN_POINT ( 'NONE',  ( -9.067083174484388053, 46.09712060844259440, -13.87005886985725667 ) ) ;
#20155=CARTESIAN_POINT ( 'NONE',  ( 28.10498339410670354, 36.32170307983790991, -9.575481939047044477 ) ) ;
#20169=CARTESIAN_POINT ( 'NONE',  ( -0.6461882397993791161, 28.14391481035789155, -38.41680952378990099 ) ) ;
#20192=CARTESIAN_POINT ( 'NONE',  ( -22.65226583814422057, 26.07318025823565577, -30.83806826229820075 ) ) ;
#20204=CARTESIAN_POINT ( 'NONE',  ( -10.91073407590445932, 45.93358294599330804, -13.06300009034441523 ) ) ;
#20208=DIRECTION ( 'NONE',  ( -0.000000000000000000, -1.000000000000000000, -0.000000000000000000 ) ) ;
#20225=ORIENTED_EDGE ( 'NONE', *, *, #71259, .T. ) ;
#20227=VERTEX_POINT ( 'NONE', #3827 ) ;
#20228=CARTESIAN_POINT ( 'NONE',  ( 48.76594521878717359, 8.294242253543416155, -16.61919356891331745 ) ) ;
#20232=COLOUR_RGB ( '', 0.40784314, 0.44705882, 0.49803922) ;
#20250=LINE ( 'NONE', #27808, #3458 ) ;
#20260=CARTESIAN_POINT ( 'NONE',  ( 6.337538409676599689E-15, 7.746009256456446224, 51.75000000000000711 ) ) ;
#20282=CARTESIAN_POINT ( 'NONE',  ( -7.808575906223166108, 53.96872104851095742, 3.793266769575681430 ) ) ;
#20288=CARTESIAN_POINT ( 'NONE',  ( -30.25697458664245687, 12.04847113665175584, -39.73669343589890701 ) ) ;
#20294=EDGE_CURVE ( 'NONE', #57566, #23889, #47316, .T. ) ;
#20311=CARTESIAN_POINT ( 'NONE',  ( 5.125709143870056828, 54.24787127484101035, -6.031152949374436467 ) ) ;
#20350=ORIENTED_EDGE ( 'NONE', *, *, #69888, .T. ) ;
#20374=CARTESIAN_POINT ( 'NONE',  ( 28.58246259357159857, 11.06567680426941713, -41.45945986390915294 ) ) ;
#20377=CARTESIAN_POINT ( 'NONE',  ( -9.317927955922566952, 51.34044562560666236, 3.778188453665225932 ) ) ;
#20402=COLOUR_RGB ( '', 0.72549020, 0.75294118, 0.79215686) ;
#20409=COLOUR_RGB ( '', 0.40784314, 0.44705882, 0.49803922) ;
#20435=ORIENTED_EDGE ( 'NONE', *, *, #29726, .F. ) ;
#20459=VERTEX_POINT ( 'NONE', #50495 ) ;
#20469=DIRECTION ( 'NONE',  ( 0.000000000000000000, 1.000000000000000000, 0.000000000000000000 ) ) ;
#20477=B_SPLINE_CURVE_WITH_KNOTS ( 'NONE', 3,
 ( #57192, #73912, #89057, #90643, #39457, #98712, #99243, #88529, #56116, #105239, #90108, #106272, #64261, #520, #65309, #24349, #9408, #16752, #16213, #33484, #15154, #81461, #49099, #72843, #49642, #97652 ),
 .UNSPECIFIED., .F., .F.,
 ( 4, 2, 2, 2, 2, 2, 2, 2, 2, 2, 2, 2, 4 ),
 ( 0.001419956731861227216, 0.001671840766058725310, 0.001923724800256223404, 0.002175608834453721715, 0.002427492868651219375, 0.002931260937046222936, 0.003183144971243733173, 0.003435029005441242976, 0.004442565142231283924, 0.004694449176428796763, 0.004946333210626309602, 0.005198217244823822442, 0.005450101279021335281 ),
 .UNSPECIFIED. ) ;
#20516=CARTESIAN_POINT ( 'NONE',  ( -49.19520577559744368, 7.745679164654304394, 16.05969994618030228 ) ) ;
#20523=CARTESIAN_POINT ( 'NONE',  ( -30.36574723454835478, 11.76891213769395428, 39.80121650896526120 ) ) ;
#20536=AXIS2_PLACEMENT_3D ( 'NONE', #31363, #64240, #48017 ) ;
#20547=EDGE_CURVE ( 'NONE', #34601, #23687, #96880, .T. ) ;
#20557=CARTESIAN_POINT ( 'NONE',  ( 30.48982775277875135, 7.748378201987732972, -41.81310123456357530 ) ) ;
#20564=( LENGTH_UNIT ( ) NAMED_UNIT ( * ) SI_UNIT ( .MILLI., .METRE. ) );
#20569=ORIENTED_EDGE ( 'NONE', *, *, #37183, .F. ) ;
#20587=ORIENTED_EDGE ( 'NONE', *, *, #90249, .F. ) ;
#20592=CARTESIAN_POINT ( 'NONE',  ( -0.6440314167888865349, 52.10985070881105941, 7.915853150659584614 ) ) ;
#20610=CARTESIAN_POINT ( 'NONE',  ( -1.249701656895251700, 45.80093235429502840, 17.33947950171232577 ) ) ;
#20619=( LENGTH_UNIT ( ) NAMED_UNIT ( * ) SI_UNIT ( .MILLI., .METRE. ) );
#20620=DIRECTION ( 'NONE',  ( 0.000000000000000000, 0.000000000000000000, 1.000000000000000000 ) ) ;
#20637=CARTESIAN_POINT ( 'NONE',  ( 30.93388328643609242, 14.00942575955929748, -40.91282515498054551 ) ) ;
#20641=EDGE_CURVE ( 'NONE', #25026, #77058, #90351, .T. ) ;
#20646=CARTESIAN_POINT ( 'NONE',  ( -46.95966155981771095, 18.79500983734985553, 14.95375697514023017 ) ) ;
#20648=FACE_OUTER_BOUND ( 'NONE', #83077, .T. ) ;
#20651=CARTESIAN_POINT ( 'NONE',  ( 16.80337955834833252, 43.42153323332214399, 6.657797401561436068 ) ) ;
#20659=VECTOR ( 'NONE', #28799, 1000.000000000000000 ) ;
#20664=CARTESIAN_POINT ( 'NONE',  ( -28.28112556431591784, 36.39299121505979429, -8.375380894399709675 ) ) ;
#20669=CARTESIAN_POINT ( 'NONE',  ( 16.64348903516512834, 43.75610143575153899, -4.157797401561768247 ) ) ;
#20683=CARTESIAN_POINT ( 'NONE',  ( 5.290067270632161645, 53.47475093287481229, -8.531152949374595451 ) ) ;
#20684=CARTESIAN_POINT ( 'NONE',  ( 16.75187969033515145, 34.99134772383131775, -21.80698433968624528 ) ) ;
#20734=CARTESIAN_POINT ( 'NONE',  ( -21.97738170171518490, 25.77581552988312552, -32.31595285212490865 ) ) ;
#20737=CARTESIAN_POINT ( 'NONE',  ( -27.10511071441192144, 34.47735702144345282, -10.05698433968589178 ) ) ;
#20742=CARTESIAN_POINT ( 'NONE',  ( -48.80488232270442239, 14.82891652079445599, -14.61828285348522449 ) ) ;
#20759=AXIS2_PLACEMENT_3D ( 'NONE', #63327, #55198, #88126 ) ;
#20761=CARTESIAN_POINT ( 'NONE',  ( 9.032223969890491588, 46.05502784614110823, -14.03066199895145161 ) ) ;
#20788=CARTESIAN_POINT ( 'NONE',  ( 4.206664532338635354, 51.73451848529560237, 7.924518144939897368 ) ) ;
#20796=VECTOR ( 'NONE', #76126, 1000.000000000000000 ) ;
#20815=ORIENTED_EDGE ( 'NONE', *, *, #15666, .F. ) ;
#20822=B_SPLINE_CURVE_WITH_KNOTS ( 'NONE', 3,
 ( #5555, #79444, #8064, #57666, #40976, #4501, #48518, #57141, #89535, #16158, #97595, #7520, #21778, #90589, #87555, #40438, #13103, #38482, #73318, #54091, #72792, #46032, #46552, #105697 ),
 .UNSPECIFIED., .F., .F.,
 ( 4, 2, 2, 2, 2, 2, 2, 2, 2, 2, 2, 4 ),
 ( 0.003189860231642088848, 0.003693490673305733444, 0.004197121114969377606, 0.004448936335801199904, 0.004700751556633022202, 0.004952566777464845367, 0.005204381998296666798, 0.005708012439960319200, 0.005959827660792142365, 0.006211642881623965530, 0.006715273323287604922, 0.007218903764951243446 ),
 .UNSPECIFIED. ) ;
#20832=CARTESIAN_POINT ( 'NONE',  ( 9.554917598412142610, 53.41952622708690512, -3.541854172211333918 ) ) ;
#20844=CARTESIAN_POINT ( 'NONE',  ( 4.044483942431806867, 54.03592768539738955, -7.472348141917804831 ) ) ;
#20861=ORIENTED_EDGE ( 'NONE', *, *, #86571, .T. ) ;
#20868=CARTESIAN_POINT ( 'NONE',  ( -1.103634289736943552, 51.47986102780117079, -9.608635276217455612 ) ) ;
#20887=STYLED_ITEM ( 'NONE', ( #65203 ), #19142 ) ;
#20894=VERTEX_POINT ( 'NONE', #7139 ) ;
#20922=FILL_AREA_STYLE_COLOUR ( '', #16024 ) ;
#20974=VECTOR ( 'NONE', #44953, 1000.000000000000000 ) ;
#20977=CARTESIAN_POINT ( 'NONE',  ( -7.939150208838348100, 52.04628108490835814, 1.683917007163810764 ) ) ;
#20980=DIRECTION ( 'NONE',  ( 0.000000000000000000, 1.000000000000000000, -0.000000000000000000 ) ) ;
#20983=CARTESIAN_POINT ( 'NONE',  ( 5.290067270632322405, -1.200000000000000030E-05, 7.281152949374479100 ) ) ;
#21002=EDGE_LOOP ( 'NONE', ( #36593, #28650, #77510, #10956 ) ) ;
#21016=CARTESIAN_POINT ( 'NONE',  ( 16.18712010533798562, 37.20509496956294981, -21.93868532144439598 ) ) ;
#21026=VECTOR ( 'NONE', #9355, 1000.000000000000114 ) ;
#21027=EDGE_CURVE ( 'NONE', #83885, #22672, #81346, .T. ) ;
#21070=FILL_AREA_STYLE_COLOUR ( '', #48873 ) ;
#21074=ADVANCED_FACE ( 'NONE', ( #53460 ), #77199, .F. ) ;
#21090=( LENGTH_UNIT ( ) NAMED_UNIT ( * ) SI_UNIT ( .MILLI., .METRE. ) );
#21101=EDGE_CURVE ( 'NONE', #43603, #5811, #12447, .T. ) ;
#21102=CARTESIAN_POINT ( 'NONE',  ( -0.7843429689301302243, 52.06967622658047645, 8.013317272959927351 ) ) ;
#21113=CARTESIAN_POINT ( 'NONE',  ( -9.268239551722324165, 44.06621912919404593, -13.41314811874801016 ) ) ;
#21116=UNCERTAINTY_MEASURE_WITH_UNIT (LENGTH_MEASURE( 1.000000000000000082E-05 ), #29470, 'distance_accuracy_value', 'NONE');
#21123=CARTESIAN_POINT ( 'NONE',  ( -1.159787357822634979, 11.84251578204911759, 50.01779155637117924 ) ) ;
#21136=CARTESIAN_POINT ( 'NONE',  ( -15.98906220215687313, 34.48549488436115951, 24.06010465822882338 ) ) ;
#21151=CARTESIAN_POINT ( 'NONE',  ( 30.04234920459604652, 13.07620473719202714, -42.05403970751778076 ) ) ;
#21161=EDGE_CURVE ( 'NONE', #68169, #52941, #72834, .T. ) ;
#21167=CARTESIAN_POINT ( 'NONE',  ( 17.85301235858413804, 43.24702788698653677, 5.052089591447788131 ) ) ;
#21185=CARTESIAN_POINT ( 'NONE',  ( -7.800811591264651845, 52.08872798781089131, -1.773736857837786784 ) ) ;
#21191=UNCERTAINTY_MEASURE_WITH_UNIT (LENGTH_MEASURE( 1.000000000000000082E-05 ), #57602, 'distance_accuracy_value', 'NONE');
#21239=CARTESIAN_POINT ( 'NONE',  ( -9.634713197495671011, 53.53784324394835181, -2.122499012415343334 ) ) ;
#21252=VERTEX_POINT ( 'NONE', #39928 ) ;
#21265=CYLINDRICAL_SURFACE ( 'NONE', #61454, 1.250000000000001110 ) ;
#21271=CARTESIAN_POINT ( 'NONE',  ( 9.076853247125631796, 45.89842957983098870, -14.51167170299882336 ) ) ;
#21295=CARTESIAN_POINT ( 'NONE',  ( 5.122460025286957652, 51.37854414394068669, 8.531152949374495975 ) ) ;
#21329=CARTESIAN_POINT ( 'NONE',  ( 48.02835407290504577, 9.771516447483525880, -16.85535821593549954 ) ) ;
#21407=CARTESIAN_POINT ( 'NONE',  ( -9.736013035283027861, 51.35462565537034152, 2.350814639870274725 ) ) ;
#21439=AXIS2_PLACEMENT_3D ( 'NONE', #83375, #56960, #42384 ) ;
#21488=CARTESIAN_POINT ( 'NONE',  ( 17.73901163440294226, 36.76451030150755628, 22.27377543627835621 ) ) ;
#21500=CARTESIAN_POINT ( 'NONE',  ( 0.000000000000000000, 36.79151656018385097, -22.55262289886175964 ) ) ;
#21505=CARTESIAN_POINT ( 'NONE',  ( -27.71614854450405119, 36.65793962528498184, 7.705128702296750731 ) ) ;
#21521=( GEOMETRIC_REPRESENTATION_CONTEXT ( 3 ) GLOBAL_UNCERTAINTY_ASSIGNED_CONTEXT ( ( #48415 ) ) GLOBAL_UNIT_ASSIGNED_CONTEXT ( ( #75956, #99698, #67869 ) ) REPRESENTATION_CONTEXT ( 'NONE', 'WORKASPACE' ) );
#21536=EDGE_CURVE ( 'NONE', #12685, #1846, #49468, .T. ) ;
#21540=CARTESIAN_POINT ( 'NONE',  ( -49.22180010227538105, 7.740565218139797032, 15.98496799241658550 ) ) ;
#21546=CARTESIAN_POINT ( 'NONE',  ( -29.86026515094337341, 12.86933730193438485, 39.60535821593512651 ) ) ;
#21570=EDGE_LOOP ( 'NONE', ( #67666, #76803 ) ) ;
#21584=SURFACE_STYLE_FILL_AREA ( #78708 ) ;
#21585=STYLED_ITEM ( 'NONE', ( #61650 ), #56122 ) ;
#21615=EDGE_LOOP ( 'NONE', ( #40767, #90007 ) ) ;
#21630=B_SPLINE_CURVE_WITH_KNOTS ( 'NONE', 3,
 ( #20684, #38424, #61641, #14099, #103141, #47006, #95062, #96637, #44918, #62687, #103661, #77803, #36847, #62172, #53523, #71287, #29289, #3914, #63218, #29812 ),
 .UNSPECIFIED., .F., .F.,
 ( 4, 2, 2, 2, 2, 2, 2, 2, 2, 4 ),
 ( 0.003121586077445279335, 0.003625240300813460572, 0.004128894524181641809, 0.004632548747549822613, 0.005136202970918004283, 0.005639857194286185954, 0.005891684305970274621, 0.006143511417654363288, 0.006647165641022527612, 0.007150819864390691935 ),
 .UNSPECIFIED. ) ;
#21633=ORIENTED_EDGE ( 'NONE', *, *, #50456, .F. ) ;
#21635=CARTESIAN_POINT ( 'NONE',  ( 6.337538409676599689E-15, 7.746009256456446224, 51.75000000000000711 ) ) ;
#21650=FILL_AREA_STYLE_COLOUR ( '', #71504 ) ;
#21651=VERTEX_POINT ( 'NONE', #72684 ) ;
#21653=EDGE_CURVE ( 'NONE', #88418, #88217, #65895, .T. ) ;
#21663=MECHANICAL_DESIGN_GEOMETRIC_PRESENTATION_REPRESENTATION('',(#57792),#90526);
#21670=DIRECTION ( 'NONE',  ( -0.000000000000000000, 1.000000000000000000, -0.000000000000000000 ) ) ;
#21678=CARTESIAN_POINT ( 'NONE',  ( 16.91717221323107978, 34.22367470353576380, 24.29879862547840474 ) ) ;
#21679=CARTESIAN_POINT ( 'NONE',  ( 37.56673239365841255, 27.60449318992554169, -13.45617127781092215 ) ) ;
#21747=CARTESIAN_POINT ( 'NONE',  ( 10.61273427954644077, 46.03711080233982500, -12.94042145964163204 ) ) ;
#21773=CARTESIAN_POINT ( 'NONE',  ( -49.19747204248731265, 12.91412732281234810, -16.05397513443227808 ) ) ;
#21778=CARTESIAN_POINT ( 'NONE',  ( 28.35315596375243530, 34.20571024640019431, -8.697504746618690774 ) ) ;
#21779=B_SPLINE_CURVE_WITH_KNOTS ( 'NONE', 3,
 ( #51365, #58409, #57856, #33099, #58947, #65964, #98845, #91321, #42751, #57325, #92351, #16897, #34163, #84276, #10372, #74577, #654, #33619, #9304, #67040, #26092, #1744 ),
 .UNSPECIFIED., .F., .F.,
 ( 4, 2, 2, 2, 2, 2, 2, 2, 2, 2, 4 ),
 ( 0.003152549850706256023, 0.003404493534967637219, 0.003656437219229017981, 0.004160324587751784708, 0.004664211956274550569, 0.005168099324797318164, 0.005671986693320084025, 0.006175874061842850753, 0.006679761430365617481, 0.006931705114627000411, 0.007183648798888385076 ),
 .UNSPECIFIED. ) ;
#21802=FILL_AREA_STYLE ('',( #95663 ) ) ;
#21810=ADVANCED_FACE ( 'NONE', ( #88619 ), #6627, .F. ) ;
#21821=CARTESIAN_POINT ( 'NONE',  ( -36.57300281741547821, 26.05217144207286140, 11.44322539509465386 ) ) ;
#21822=AXIS2_PLACEMENT_3D ( 'NONE', #105790, #64807, #23853 ) ;
#21830=CIRCLE ( 'NONE', #75213, 11.27631144943088515 ) ;
#21886=CARTESIAN_POINT ( 'NONE',  ( 0.6424259193445743810, 34.23289850721570104, 29.57547277752458470 ) ) ;
#21887=CARTESIAN_POINT ( 'NONE',  ( 25.86712516739308398, 37.16009387618654358, 8.998664997537444421 ) ) ;
#21889=ORIENTED_EDGE ( 'NONE', *, *, #12577, .T. ) ;
#21894=CARTESIAN_POINT ( 'NONE',  ( 23.38404382908447943, 27.34872606290120700, -33.19783523858093588 ) ) ;
#21896=EDGE_LOOP ( 'NONE', ( #99585, #39872, #28176, #58849 ) ) ;
#21916=LINE ( 'NONE', #79060, #75537 ) ;
#21923=DIRECTION ( 'NONE',  ( -0.000000000000000000, 1.000000000000000000, -0.000000000000000000 ) ) ;
#21958=CARTESIAN_POINT ( 'NONE',  ( -1.484885661199817548E-13, 25.16821295365152622, -40.75000000000150635 ) ) ;
#21961=FILL_AREA_STYLE ('',( #97392 ) ) ;
#21983=( NAMED_UNIT ( * ) SI_UNIT ( $, .STERADIAN. ) SOLID_ANGLE_UNIT ( ) );
#22008=VECTOR ( 'NONE', #84998, 1000.000000000000000 ) ;
#22013=CARTESIAN_POINT ( 'NONE',  ( 17.83066785977196034, 36.70615155823221443, 22.40577935710491531 ) ) ;
#22014=( NAMED_UNIT ( * ) PLANE_ANGLE_UNIT ( ) SI_UNIT ( $, .RADIAN. ) );
#22028=CARTESIAN_POINT ( 'NONE',  ( -28.10508442060149292, 36.32168591140393943, 9.575330628090654272 ) ) ;
#22040=VECTOR ( 'NONE', #61378, 1000.000000000000000 ) ;
#22044=CARTESIAN_POINT ( 'NONE',  ( -27.10511071441192144, -1.200000000000000030E-05, -8.806984339685890006 ) ) ;
#22046=( GEOMETRIC_REPRESENTATION_CONTEXT ( 3 ) GLOBAL_UNCERTAINTY_ASSIGNED_CONTEXT ( ( #62087 ) ) GLOBAL_UNIT_ASSIGNED_CONTEXT ( ( #66155, #6311, #72126 ) ) REPRESENTATION_CONTEXT ( 'NONE', 'WORKASPACE' ) );
#22064=CARTESIAN_POINT ( 'NONE',  ( -49.27910061723718371, 7.914421806211214161, 15.56686240200379423 ) ) ;
#22086=VECTOR ( 'NONE', #87908, 1000.000000000000000 ) ;
#22106=( LENGTH_UNIT ( ) NAMED_UNIT ( * ) SI_UNIT ( .MILLI., .METRE. ) );
#22110=CARTESIAN_POINT ( 'NONE',  ( 0.000000000000000000, 43.19193163660326462, -24.55262289886175964 ) ) ;
#22120=CARTESIAN_POINT ( 'NONE',  ( -10.28624191511830155, 45.38549880562041494, -15.40779740156157196 ) ) ;
#22148=CARTESIAN_POINT ( 'NONE',  ( -9.657909026534005292, 43.42990472694053494, -15.25053491157621899 ) ) ;
#22149=CARTESIAN_POINT ( 'NONE',  ( -0.7843950794064245002, 34.98204345154115913, 27.51314879577667583 ) ) ;
#22151=UNCERTAINTY_MEASURE_WITH_UNIT (LENGTH_MEASURE( 1.000000000000000082E-05 ), #20564, 'distance_accuracy_value', 'NONE');
#22162=ORIENTED_EDGE ( 'NONE', *, *, #23083, .F. ) ;
#22167=CARTESIAN_POINT ( 'NONE',  ( 10.90727606233362756, 43.80400056797084574, 13.07007756734143555 ) ) ;
#22182=VERTEX_POINT ( 'NONE', #19273 ) ;
#22187=( GEOMETRIC_REPRESENTATION_CONTEXT ( 3 ) GLOBAL_UNCERTAINTY_ASSIGNED_CONTEXT ( ( #10572 ) ) GLOBAL_UNIT_ASSIGNED_CONTEXT ( ( #64046, #13863, #103423 ) ) REPRESENTATION_CONTEXT ( 'NONE', 'WORKASPACE' ) );
#22188=DIRECTION ( 'NONE',  ( -0.000000000000000000, 1.000000000000000000, -0.000000000000000000 ) ) ;
#22192=CIRCLE ( 'NONE', #20536, 13.27631144943088515 ) ;
#22193=CARTESIAN_POINT ( 'NONE',  ( 29.77344787310960328, 13.34785391060249538, -42.10535821593529704 ) ) ;
#22195=ORIENTED_EDGE ( 'NONE', *, *, #7815, .F. ) ;
#22218=UNCERTAINTY_MEASURE_WITH_UNIT (LENGTH_MEASURE( 1.000000000000000082E-05 ), #37013, 'distance_accuracy_value', 'NONE');
#22221=CARTESIAN_POINT ( 'NONE',  ( 4.142849616820252293E-15, 27.68727484027578356, 33.82893434829263413 ) ) ;
#22234=DIRECTION ( 'NONE',  ( -0.000000000000000000, 1.000000000000000000, -0.000000000000000000 ) ) ;
#22258=EDGE_CURVE ( 'NONE', #103579, #20459, #58163, .T. ) ;
#22270=EDGE_LOOP ( 'NONE', ( #27367, #4112 ) ) ;
#22271=CARTESIAN_POINT ( 'NONE',  ( -11.49412716574636306, 45.59192006558699006, 13.79863126508840487 ) ) ;
#22290=CARTESIAN_POINT ( 'NONE',  ( -9.769072601666671574, 53.46510771226535041, -2.425000069901109168 ) ) ;
#22303=CARTESIAN_POINT ( 'NONE',  ( 0.1684239960690284144, 43.17555810750861411, -18.75000000000000711 ) ) ;
#22311=CARTESIAN_POINT ( 'NONE',  ( 23.21751746555303342, 27.38103382803677377, 33.20617127781017075 ) ) ;
#22312=CARTESIAN_POINT ( 'NONE',  ( 0.000000000000000000, -945.0000000000000000, 0.000000000000000000 ) ) ;
#22341=B_SPLINE_CURVE_WITH_KNOTS ( 'NONE', 3,
 ( #72661, #73171, #32225, #84488, #68849, #10055, #100655, #76917, #83944, #19279, #75856, #60760, #59689, #51031, #18718, #101725, #76374, #17637, #85015, #51573, #75312, #42420, #26815, #1409, #44024, #42964 ),
 .UNSPECIFIED., .F., .F.,
 ( 4, 2, 2, 2, 2, 2, 2, 2, 2, 2, 2, 2, 4 ),
 ( 0.003090333073482954759, 0.003342552850341273894, 0.003594772627199593028, 0.003846992404057912162, 0.004099212180916231296, 0.004603651734632862626, 0.004855871511491176989, 0.005108091288349492221, 0.006116970395782750543, 0.006369190172641068376, 0.006621409949499387076, 0.006873629726357705777, 0.007125849503216023610 ),
 .UNSPECIFIED. ) ;
#22348=FILL_AREA_STYLE ('',( #6114 ) ) ;
#22354=CARTESIAN_POINT ( 'NONE',  ( 1.102560413418700813, 51.47929533831098325, -9.610321672475258481 ) ) ;
#22360=CARTESIAN_POINT ( 'NONE',  ( 11.53278078296752263, 43.31871327052838438, 14.28168592353131139 ) ) ;
#22378=CARTESIAN_POINT ( 'NONE',  ( 1.152188841818234133E-13, -1.200000000000000030E-05, 50.50000000000000000 ) ) ;
#22411=CARTESIAN_POINT ( 'NONE',  ( -15.54289451413713152, 36.90012926360033418, 23.41220851048981544 ) ) ;
#22419=CARTESIAN_POINT ( 'NONE',  ( 17.40745463263493065, 43.24839122124123492, -6.411055176082404827 ) ) ;
#22425=CARTESIAN_POINT ( 'NONE',  ( -23.38223461712482276, 25.21832460939182852, 33.20617127781060418 ) ) ;
#22428=B_SPLINE_CURVE_WITH_KNOTS ( 'NONE', 3,
 ( #1865, #52548, #85471, #59607, #36427, #67689, #43415, #25675, #51489, #58539, #17555, #83325, #42337, #29902, #87069, #79488, #6118, #21821, #62788, #61196, #71384, #78954, #13143, #4542 ),
 .UNSPECIFIED., .F., .F.,
 ( 4, 2, 2, 2, 2, 2, 2, 2, 2, 2, 2, 4 ),
 ( 0.002907281924855007089, 0.003411952726777704205, 0.003916623528700401320, 0.004168958929661742939, 0.004421294330623083690, 0.004673629731584425309, 0.004925965132545766928, 0.005430635934468451900, 0.005682971335429793519, 0.005935306736391136005, 0.006439977538313801028, 0.006944648340236465184 ),
 .UNSPECIFIED. ) ;
#22433=SURFACE_SIDE_STYLE ('',( #104918 ) ) ;
#22437=CARTESIAN_POINT ( 'NONE',  ( 0.5298411179699548113, 18.60179019596422023, -49.36142467042689219 ) ) ;
#22450=CYLINDRICAL_SURFACE ( 'NONE', #5806, 1.250000000000001110 ) ;
#22453=SURFACE_STYLE_USAGE ( .BOTH. , #83034 ) ;
#22468=CARTESIAN_POINT ( 'NONE',  ( 29.68315524077034340, 8.302504244945382084, 42.10535821593451544 ) ) ;
#22488=ADVANCED_FACE ( 'NONE', ( #64459 ), #88727, .F. ) ;
#22498=STYLED_ITEM ( 'NONE', ( #100845 ), #92066 ) ;
#22545=PRESENTATION_STYLE_ASSIGNMENT (( #5787 ) ) ;
#22561=( LENGTH_UNIT ( ) NAMED_UNIT ( * ) SI_UNIT ( .MILLI., .METRE. ) );
#22572=VERTEX_POINT ( 'NONE', #9915 ) ;
#22602=DIRECTION ( 'NONE',  ( 0.000000000000000000, 1.000000000000000000, 0.000000000000000000 ) ) ;
#22612=CARTESIAN_POINT ( 'NONE',  ( -38.66211280991526422, 27.30187666962869031, 12.83133664711218991 ) ) ;
#22648=CARTESIAN_POINT ( 'NONE',  ( -7.799656765069284958, 54.21738860527597126, -1.774909779959811473 ) ) ;
#22659=ORIENTED_EDGE ( 'NONE', *, *, #9265, .T. ) ;
#22672=VERTEX_POINT ( 'NONE', #66566 ) ;
#22674=CARTESIAN_POINT ( 'NONE',  ( -30.64007947709922419, 12.99638611018202639, -41.66214316769399773 ) ) ;
#22709=DIRECTION ( 'NONE',  ( 0.000000000000000000, 0.000000000000000000, -1.000000000000000000 ) ) ;
#22724=FILL_AREA_STYLE ('',( #46440 ) ) ;
#22745=CARTESIAN_POINT ( 'NONE',  ( 38.78863291229748000, 25.16502836992622960, 12.51984068333550759 ) ) ;
#22746=CARTESIAN_POINT ( 'NONE',  ( 1.249602959316253648, 25.67499641899253859, 39.33778172269227724 ) ) ;
#22750=CARTESIAN_POINT ( 'NONE',  ( -29.14590962570478183, 18.82625154611908513, -39.72466805691968972 ) ) ;
#22751=FILL_AREA_STYLE ('',( #96616 ) ) ;
#22783=( NAMED_UNIT ( * ) PLANE_ANGLE_UNIT ( ) SI_UNIT ( $, .RADIAN. ) );
#22798=VECTOR ( 'NONE', #4509, 1000.000000000000227 ) ;
#22810=CARTESIAN_POINT ( 'NONE',  ( -5.700380315796782504, 53.41403331668362853, -8.464922343797399051 ) ) ;
#22835=CARTESIAN_POINT ( 'NONE',  ( -49.13563689125227540, 12.95301730162678666, -16.19018188727108409 ) ) ;
#22838=B_SPLINE_CURVE_WITH_KNOTS ( 'NONE', 3,
 ( #102773, #13209, #28938, #61810, #37546, #95224, #46138, #79025, #41212, #65498, #40678, #98385, #24534, #82192, #88715, #14806, #105939, #41744, #32624, #81134, #57383, #48754 ),
 .UNSPECIFIED., .F., .F.,
 ( 4, 2, 2, 2, 2, 2, 2, 2, 2, 2, 4 ),
 ( 0.006964068074043574565, 0.007215909760093238735, 0.007467751446142902039, 0.007971434818242223441, 0.008475118190341546578, 0.008726959876391207280, 0.008978801562440866246, 0.009482484934540184179, 0.009986168306639502112, 0.01048985167873882005, 0.01099353505083813798 ),
 .UNSPECIFIED. ) ;
#22853=FILL_AREA_STYLE ('',( #97229 ) ) ;
#22862=CARTESIAN_POINT ( 'NONE',  ( -0.7799315185232612579, 13.54185226379499696, -51.48129177036200588 ) ) ;
#22865=CARTESIAN_POINT ( 'NONE',  ( 11.51386276761315308, 45.40501555918417864, 14.44555604779037061 ) ) ;
#22868=ORIENTED_EDGE ( 'NONE', *, *, #64773, .F. ) ;
#22875=CYLINDRICAL_SURFACE ( 'NONE', #87812, 1.250000000000001110 ) ;
#22905=( GEOMETRIC_REPRESENTATION_CONTEXT ( 3 ) GLOBAL_UNCERTAINTY_ASSIGNED_CONTEXT ( ( #83400 ) ) GLOBAL_UNIT_ASSIGNED_CONTEXT ( ( #48821, #34290, #15946 ) ) REPRESENTATION_CONTEXT ( 'NONE', 'WORKASPACE' ) );
#22915=ORIENTED_EDGE ( 'NONE', *, *, #21101, .T. ) ;
#22926=DIRECTION ( 'NONE',  ( 0.000000000000000000, 1.000000000000000000, 0.000000000000000000 ) ) ;
#22928=CARTESIAN_POINT ( 'NONE',  ( 5.523799489093671039E-15, 23.58303312036771615, 45.10524579772351217 ) ) ;
#22940=CARTESIAN_POINT ( 'NONE',  ( 3.643324519380566085E-15, 34.17188553058033307, 29.75000000000000355 ) ) ;
#22949=CARTESIAN_POINT ( 'NONE',  ( -5.126331210562743657, 52.11692832490694371, -6.039129629323012338 ) ) ;
#22953=CARTESIAN_POINT ( 'NONE',  ( -1.250638237768894268, 43.55834836214284422, -17.65405259223556556 ) ) ;
#22965=CARTESIAN_POINT ( 'NONE',  ( -47.90443661882622450, 17.06459462766618529, -14.35535821593460248 ) ) ;
#22989=STYLED_ITEM ( 'NONE', ( #1763 ), #52434 ) ;
#22991=DIRECTION ( 'NONE',  ( 0.000000000000000000, 1.000000000000000000, 0.000000000000000000 ) ) ;
#22995=CARTESIAN_POINT ( 'NONE',  ( 47.44667293595422564, 16.35698112199397158, 16.71846647949837461 ) ) ;
#23020=ADVANCED_FACE ( 'NONE', ( #15763, #23353, #38995, #106351, #40045 ), #64750, .F. ) ;
#23043=CARTESIAN_POINT ( 'NONE',  ( -10.28624191511820207, 43.99263840937192782, 12.90779740156163768 ) ) ;
#23062=CARTESIAN_POINT ( 'NONE',  ( 0.6442865410403176840, 25.22687333464023141, -40.58400936760502731 ) ) ;
#23069=CARTESIAN_POINT ( 'NONE',  ( -1.220536332002533753, 34.50324530966049963, -28.81383133510943040 ) ) ;
#23083=EDGE_CURVE ( 'NONE', #4914, #74421, #15770, .T. ) ;
#23095=CARTESIAN_POINT ( 'NONE',  ( 22.11640175898061855, 26.03333166199414350, 31.35866682975836639 ) ) ;
#23108=SURFACE_STYLE_FILL_AREA ( #30677 ) ;
#23125=B_SPLINE_CURVE_WITH_KNOTS ( 'NONE', 3,
 ( #69827, #52564, #85489, #28888, #61759, #37498, #62285, #95176, #13160, #103778, #29919, #55215, #55731, #64399, #39064, #73516, #40109, #30450 ),
 .UNSPECIFIED., .F., .F.,
 ( 4, 2, 2, 2, 2, 2, 2, 2, 4 ),
 ( 0.003067497823037675965, 0.003572718754844164939, 0.004077939686650653914, 0.004583160618457140720, 0.004835771084360384990, 0.005088381550263627526, 0.005593602482070121271, 0.006098823413876615883, 0.007109265277489604240 ),
 .UNSPECIFIED. ) ;
#23136=CARTESIAN_POINT ( 'NONE',  ( 28.98512335478687163, 9.657432045445739632, 41.89946025606963076 ) ) ;
#23138=CARTESIAN_POINT ( 'NONE',  ( 28.65204159835603548, 18.70303032895466089, 40.14586416981808270 ) ) ;
#23146=CARTESIAN_POINT ( 'NONE',  ( -27.86837958467689802, 36.37503241011537369, -9.810923704312715543 ) ) ;
#23162=EDGE_LOOP ( 'NONE', ( #51580, #100564, #80187, #70120 ) ) ;
#23166=DIRECTION ( 'NONE',  ( 0.000000000000000000, 1.000000000000000000, 0.000000000000000000 ) ) ;
#23185=CARTESIAN_POINT ( 'NONE',  ( -1.249962610845875011, 25.55812661083311710, 39.65902825006367749 ) ) ;
#23186=CARTESIAN_POINT ( 'NONE',  ( 7.149395896920095848E-21, 27.29656849860388235, -40.75000000000000000 ) ) ;
#23213=CARTESIAN_POINT ( 'NONE',  ( -0.6464587407298656441, 35.01841617270944340, 27.41698562527900407 ) ) ;
#23221=ORIENTED_EDGE ( 'NONE', *, *, #91189, .T. ) ;
#23226=SURFACE_SIDE_STYLE ('',( #13502 ) ) ;
#23227=CARTESIAN_POINT ( 'NONE',  ( 22.39889803669582236, 27.64071832785176852, 32.90416900124247945 ) ) ;
#23229=CYLINDRICAL_SURFACE ( 'NONE', #69027, 1.250000000000001110 ) ;
#23233=SURFACE_STYLE_USAGE ( .BOTH. , #97091 ) ;
#23247=EDGE_CURVE ( 'NONE', #12797, #6938, #57966, .T. ) ;
#23263=CARTESIAN_POINT ( 'NONE',  ( 38.77580872333679451, 25.24258365861260245, 11.84918804548649618 ) ) ;
#23290=UNCERTAINTY_MEASURE_WITH_UNIT (LENGTH_MEASURE( 1.000000000000000082E-05 ), #19208, 'distance_accuracy_value', 'NONE');
#23292=CARTESIAN_POINT ( 'NONE',  ( 29.28883047145494345, 14.13190579697306504, -42.04354307362351761 ) ) ;
#23301=B_SPLINE_CURVE_WITH_KNOTS ( 'NONE', 3,
 ( #83439, #3061, #42996, #51602, #93138, #10609, #68338, #101236, #34404, #67798, #67280, #100158, #18207, #34931, #26852, #27389, #60269, #95802 ),
 .UNSPECIFIED., .F., .F.,
 ( 4, 2, 2, 2, 2, 2, 2, 2, 4 ),
 ( 0.005148306559854647947, 0.006154786515368258250, 0.006658026493125070340, 0.006909646482003478120, 0.007161266470881886767, 0.007664506448638707531, 0.008167746426395530029, 0.008670986404152350793, 0.009174226381909171557 ),
 .UNSPECIFIED. ) ;
#23306=( LENGTH_UNIT ( ) NAMED_UNIT ( * ) SI_UNIT ( .MILLI., .METRE. ) );
#23323=CARTESIAN_POINT ( 'NONE',  ( -11.04556819181654426, 45.87714785467576917, 13.15211296974101174 ) ) ;
#23332=CARTESIAN_POINT ( 'NONE',  ( -6.544853860617209307, 53.53209805210580896, -7.402906068179443189 ) ) ;
#23353=FACE_BOUND ( 'NONE', #85068, .T. ) ;
#23357=LINE ( 'NONE', #47061, #26980 ) ;
#23359=CONICAL_SURFACE ( 'NONE', #80209, 46.94949242731048145, 0.3972631705159501148 ) ;
#23377=SURFACE_STYLE_FILL_AREA ( #22853 ) ;
#23382=ORIENTED_EDGE ( 'NONE', *, *, #99330, .T. ) ;
#23384=CARTESIAN_POINT ( 'NONE',  ( -38.81967570215591223, 27.30152829859311225, -12.34949243608158831 ) ) ;
#23395=SURFACE_STYLE_USAGE ( .BOTH. , #14197 ) ;
#23409=CARTESIAN_POINT ( 'NONE',  ( 38.76904556471400554, 27.37270507303107436, 11.85428640503262088 ) ) ;
#23426=CARTESIAN_POINT ( 'NONE',  ( -5.457055012756472756, 53.44272100380801049, 8.531152949374559924 ) ) ;
#23452=CARTESIAN_POINT ( 'NONE',  ( -22.22792991547117936, 27.72626095856944417, 32.73621634624660004 ) ) ;
#23471=CARTESIAN_POINT ( 'NONE',  ( 0.7786400534603282741, 34.26594929026200020, 29.48136253453525768 ) ) ;
#23479=CARTESIAN_POINT ( 'NONE',  ( -24.46377330976176623, 25.31537439212452867, 32.08272137679946212 ) ) ;
#23482=UNCERTAINTY_MEASURE_WITH_UNIT (LENGTH_MEASURE( 1.000000000000000082E-05 ), #79981, 'distance_accuracy_value', 'NONE');
#23492=CARTESIAN_POINT ( 'NONE',  ( 22.43887874261524473, 26.07878403154861502, -30.97467766248137622 ) ) ;
#23509=CARTESIAN_POINT ( 'NONE',  ( -9.203801892612585078, 43.65565976494217892, 14.80297099531582283 ) ) ;
#23511=ADVANCED_FACE ( 'NONE', ( #67263, #58637, #19810, #2502, #52116 ), #2829, .T. ) ;
#23533=CARTESIAN_POINT ( 'NONE',  ( 6.510002681445791417, 51.36730452995753637, -7.565658405795778307 ) ) ;
#23536=( NAMED_UNIT ( * ) PLANE_ANGLE_UNIT ( ) SI_UNIT ( $, .RADIAN. ) );
#23540=ORIENTED_EDGE ( 'NONE', *, *, #38757, .F. ) ;
#23551=EDGE_CURVE ( 'NONE', #21651, #77582, #92369, .T. ) ;
#23602=CARTESIAN_POINT ( 'NONE',  ( 1.251548456357452377, 53.70817747035267331, -9.313240114490840327 ) ) ;
#23656=MECHANICAL_DESIGN_GEOMETRIC_PRESENTATION_REPRESENTATION('',(#32274),#54636);
#23681=CARTESIAN_POINT ( 'NONE',  ( -28.18085356279351217, 36.45119673881288236, -8.149377185781427002 ) ) ;
#23687=VERTEX_POINT ( 'NONE', #86648 ) ;
#23700=CARTESIAN_POINT ( 'NONE',  ( 0.000000000000000000, 0.000000000000000000, 0.000000000000000000 ) ) ;
#23701=SURFACE_STYLE_USAGE ( .BOTH. , #54419 ) ;
#23704=CARTESIAN_POINT ( 'NONE',  ( -17.64253364725059825, 45.32498240469068662, 6.177274125185036269 ) ) ;
#23712=SURFACE_STYLE_USAGE ( .BOTH. , #56024 ) ;
#23724=CARTESIAN_POINT ( 'NONE',  ( 1.250028549308467740, 27.68639675375847986, -39.65926092309576489 ) ) ;
#23737=ORIENTED_EDGE ( 'NONE', *, *, #26486, .T. ) ;
#23744=UNCERTAINTY_MEASURE_WITH_UNIT (LENGTH_MEASURE( 1.000000000000000082E-05 ), #26669, 'distance_accuracy_value', 'NONE');
#23757=CARTESIAN_POINT ( 'NONE',  ( 8.876037421300598140, 51.71979065213020732, 1.561582822885281718 ) ) ;
#23758=ORIENTED_EDGE ( 'NONE', *, *, #99103, .F. ) ;
#23760=( GEOMETRIC_REPRESENTATION_CONTEXT ( 3 ) GLOBAL_UNCERTAINTY_ASSIGNED_CONTEXT ( ( #894 ) ) GLOBAL_UNIT_ASSIGNED_CONTEXT ( ( #12427, #76637, #86363 ) ) REPRESENTATION_CONTEXT ( 'NONE', 'WORKASPACE' ) );
#23767=PRESENTATION_STYLE_ASSIGNMENT (( #14555 ) ) ;
#23768=CARTESIAN_POINT ( 'NONE',  ( 22.11477862515263126, 27.78277355752726763, 32.62539941293114509 ) ) ;
#23794=CARTESIAN_POINT ( 'NONE',  ( 37.40781652519264355, 27.65894600026285843, 13.45617127781008193 ) ) ;
#23800=SURFACE_STYLE_FILL_AREA ( #57701 ) ;
#23801=CARTESIAN_POINT ( 'NONE',  ( -28.77610217197955933, 13.65956388957898682, -39.99200581488092610 ) ) ;
#23814=COLOUR_RGB ( '', 0.66274510, 0.83137255, 0.94901961) ;
#23820=ORIENTED_EDGE ( 'NONE', *, *, #1332, .F. ) ;
#23836=CARTESIAN_POINT ( 'NONE',  ( 28.52991250593590777, 16.51520549712911645, -41.35291476382084852 ) ) ;
#23848=( NAMED_UNIT ( * ) PLANE_ANGLE_UNIT ( ) SI_UNIT ( $, .RADIAN. ) );
#23853=DIRECTION ( 'NONE',  ( 0.000000000000000000, 0.000000000000000000, 1.000000000000000000 ) ) ;
#23865=AXIS2_PLACEMENT_3D ( 'NONE', #61813, #44008, #92549 ) ;
#23889=VERTEX_POINT ( 'NONE', #2371 ) ;
#23900=CARTESIAN_POINT ( 'NONE',  ( -38.81809298152867882, 25.18270264959180693, 12.26709487888331829 ) ) ;
#23902=CARTESIAN_POINT ( 'NONE',  ( 16.96051095573448819, 45.50173602991597477, 6.619600894237273714 ) ) ;
#23916=CARTESIAN_POINT ( 'NONE',  ( -21.96569361886333382, 28.02808497942502441, -31.91099187246642543 ) ) ;
#23929=CARTESIAN_POINT ( 'NONE',  ( -38.54737907208687631, 27.49609987706101677, -11.41442684321127565 ) ) ;
#23932=CARTESIAN_POINT ( 'NONE',  ( -0.07705973910397148630, 12.91535575337010933, -51.74999999999999289 ) ) ;
#23944=ADVANCED_FACE ( 'NONE', ( #53068 ), #21265, .F. ) ;
#23945=PRESENTATION_STYLE_ASSIGNMENT (( #63322 ) ) ;
#23950=CARTESIAN_POINT ( 'NONE',  ( 0.3378829312054938971, 51.28040138220650590, -10.21513970828568851 ) ) ;
#23954=CARTESIAN_POINT ( 'NONE',  ( 49.24240974153283901, 8.191948471291036427, 15.29453271768024258 ) ) ;
#23964=ORIENTED_EDGE ( 'NONE', *, *, #12691, .F. ) ;
#23989=CARTESIAN_POINT ( 'NONE',  ( 27.71624102341542439, 36.65790090521107913, -7.705193261028457918 ) ) ;
#24004=SURFACE_STYLE_USAGE ( .BOTH. , #89240 ) ;
#24011=CYLINDRICAL_SURFACE ( 'NONE', #76593, 1.250000000000001110 ) ;
#24015=FACE_OUTER_BOUND ( 'NONE', #6229, .T. ) ;
#24017=CARTESIAN_POINT ( 'NONE',  ( 24.42584379203400857, 27.59191556861860661, -31.59852321640943629 ) ) ;
#24019=ORIENTED_EDGE ( 'NONE', *, *, #38374, .T. ) ;
#24029=EDGE_CURVE ( 'NONE', #56766, #36063, #98808, .T. ) ;
#24035=CARTESIAN_POINT ( 'NONE',  ( 47.14735620107882141, 13.37129584416865313, -14.71343070694231514 ) ) ;
#24039=CARTESIAN_POINT ( 'NONE',  ( 0.1682271994785180524, 54.30758622938870417, 7.749999999999998224 ) ) ;
#24041=( LENGTH_UNIT ( ) NAMED_UNIT ( * ) SI_UNIT ( .MILLI., .METRE. ) );
#24047=SURFACE_SIDE_STYLE ('',( #100015 ) ) ;
#24049=CARTESIAN_POINT ( 'NONE',  ( -10.12027838911100730, 43.29307385079338388, 15.39942933061531782 ) ) ;
#24069=FILL_AREA_STYLE_COLOUR ( '', #34437 ) ;
#24071=CARTESIAN_POINT ( 'NONE',  ( 0.000000000000000000, 23.58303312036771615, -45.10524579772351217 ) ) ;
#24106=CARTESIAN_POINT ( 'NONE',  ( 15.50701386016346817, 34.82701475167880290, 23.25392551490321225 ) ) ;
#24128=LINE ( 'NONE', #61121, #25121 ) ;
#24137=AXIS2_PLACEMENT_3D ( 'NONE', #84935, #4018, #11023 ) ;
#24145=CARTESIAN_POINT ( 'NONE',  ( -0.6471460804167578074, 34.23036685099703647, -29.58265817172704004 ) ) ;
#24147=SURFACE_SIDE_STYLE ('',( #8449 ) ) ;
#24160=AXIS2_PLACEMENT_3D ( 'NONE', #62992, #5287, #96941 ) ;
#24182=CARTESIAN_POINT ( 'NONE',  ( -27.42168344121066426, 34.64432298653954945, -7.587308281121087461 ) ) ;
#24195=ORIENTED_EDGE ( 'NONE', *, *, #88646, .F. ) ;
#24199=EDGE_LOOP ( 'NONE', ( #105795, #8824, #128, #63445 ) ) ;
#24202=CARTESIAN_POINT ( 'NONE',  ( 29.68315524077034340, 8.302504244945382084, 42.10535821593451544 ) ) ;
#24206=CARTESIAN_POINT ( 'NONE',  ( 29.14590962570505894, 18.82625154611909934, 39.72466805691946234 ) ) ;
#24210=VECTOR ( 'NONE', #59086, 1000.000000000000000 ) ;
#24212=( LENGTH_UNIT ( ) NAMED_UNIT ( * ) SI_UNIT ( .MILLI., .METRE. ) );
#24213=CARTESIAN_POINT ( 'NONE',  ( -28.49074715056200802, 18.29855530143744602, 40.46824935483533636 ) ) ;
#24222=CYLINDRICAL_SURFACE ( 'NONE', #84865, 1.250000000000001110 ) ;
#24236=ORIENTED_EDGE ( 'NONE', *, *, #32464, .T. ) ;
#24249=DIRECTION ( 'NONE',  ( -0.000000000000000000, 1.000000000000000000, 0.000000000000000000 ) ) ;
#24257=CARTESIAN_POINT ( 'NONE',  ( 4.733165431326070832E-26, 13.70447791526910919, -49.25000000000000000 ) ) ;
#24265=ORIENTED_EDGE ( 'NONE', *, *, #2268, .F. ) ;
#24276=CARTESIAN_POINT ( 'NONE',  ( -10.36896828245630431, 43.24042510010813345, -15.40779740156158439 ) ) ;
#24277=CARTESIAN_POINT ( 'NONE',  ( -29.49710045460171770, 13.37160745013286167, 39.61402429467839426 ) ) ;
#24287=CARTESIAN_POINT ( 'NONE',  ( 37.56673239365841255, 27.60449318992554169, -13.45617127781092215 ) ) ;
#24291=EDGE_LOOP ( 'NONE', ( #67819, #46767, #16588, #13062 ) ) ;
#24320=STYLED_ITEM ( 'NONE', ( #15050 ), #19158 ) ;
#24332=DIRECTION ( 'NONE',  ( 0.000000000000000000, 0.000000000000000000, 1.000000000000000000 ) ) ;
#24338=CARTESIAN_POINT ( 'NONE',  ( 4.142849616820253082E-15, 32.68727484027578356, 33.82893434829263413 ) ) ;
#24349=CARTESIAN_POINT ( 'NONE',  ( 24.45707236316964384, 25.45848949702577713, 31.59252836779057816 ) ) ;
#24352=CARTESIAN_POINT ( 'NONE',  ( 4.044804397649282457, 54.03507251708755632, 7.474846107636844650 ) ) ;
#24363=CARTESIAN_POINT ( 'NONE',  ( 29.07959870117736756, 18.85554092054059794, -39.75803059074604562 ) ) ;
#24374=VECTOR ( 'NONE', #101243, 1000.000000000000000 ) ;
#24376=MECHANICAL_DESIGN_GEOMETRIC_PRESENTATION_REPRESENTATION('',(#209),#8786);
#24378=CARTESIAN_POINT ( 'NONE',  ( 0.000000000000000000, 24.35682532067546902, 0.000000000000000000 ) ) ;
#24383=SURFACE_SIDE_STYLE ('',( #30881 ) ) ;
#24401=CARTESIAN_POINT ( 'NONE',  ( -10.28624191511820207, 45.38549880562041494, 15.40779740156164124 ) ) ;
#24409=CARTESIAN_POINT ( 'NONE',  ( 17.84534382768862670, 43.24938063751061890, -5.054370945579135466 ) ) ;
#24439=CARTESIAN_POINT ( 'NONE',  ( 17.39146662423151568, 45.59957931493300265, 4.393505531746607851 ) ) ;
#24479=CARTESIAN_POINT ( 'NONE',  ( 1.125713873518663366, 34.84991794026092293, -27.86526467689072462 ) ) ;
#24484=CARTESIAN_POINT ( 'NONE',  ( 0.1699655916222989060, 51.26930509877139741, -10.25000000000000178 ) ) ;
#24487=CARTESIAN_POINT ( 'NONE',  ( 49.18559949472803083, 8.441045694768780194, 15.12439388195326195 ) ) ;
#24502=CARTESIAN_POINT ( 'NONE',  ( -6.509863194222623051, 53.49549999415722823, 7.566361094272520127 ) ) ;
#24510=VERTEX_POINT ( 'NONE', #33870 ) ;
#24520=CARTESIAN_POINT ( 'NONE',  ( 5.290067270632161645, 53.47475093287481229, -8.531152949374595451 ) ) ;
#24531=CARTESIAN_POINT ( 'NONE',  ( 15.42175249681818805, 44.08902557066564754, 5.093581733527382305 ) ) ;
#24534=CARTESIAN_POINT ( 'NONE',  ( -17.89487417552028248, 45.31800925772326138, -5.467316602108599710 ) ) ;
#24535=DIRECTION ( 'NONE',  ( -0.000000000000000000, 1.000000000000000000, -0.000000000000000000 ) ) ;
#24542=CARTESIAN_POINT ( 'NONE',  ( -4.661380720324451943, 51.51205150140802402, -8.373549780453599212 ) ) ;
#24548=CARTESIAN_POINT ( 'NONE',  ( -37.56673239365863282, 25.47613764497371847, -13.45617127781024891 ) ) ;
#24553=CARTESIAN_POINT ( 'NONE',  ( 0.1683204496895580327, 45.30680571434964321, 18.74148122118527482 ) ) ;
#24557=CARTESIAN_POINT ( 'NONE',  ( -10.12102021413168274, 45.41888843717377000, 15.40779740156163946 ) ) ;
#24561=CARTESIAN_POINT ( 'NONE',  ( 47.78440564129551404, 10.33446651290970308, -16.83708170412499072 ) ) ;
#24567=CARTESIAN_POINT ( 'NONE',  ( 0.5667977521132806507, 54.25196811838322475, 7.882806152410106293 ) ) ;
#24569=( NAMED_UNIT ( * ) SI_UNIT ( $, .STERADIAN. ) SOLID_ANGLE_UNIT ( ) );
#24575=CARTESIAN_POINT ( 'NONE',  ( -9.875831867757614901, 44.06546706392215640, 12.97410724739095755 ) ) ;
#24586=CARTESIAN_POINT ( 'NONE',  ( 46.97290287162415012, 17.76084728355337816, 16.28892042402536333 ) ) ;
#24599=ORIENTED_EDGE ( 'NONE', *, *, #95863, .F. ) ;
#24601=STYLED_ITEM ( 'NONE', ( #69967 ), #51962 ) ;
#24602=LINE ( 'NONE', #16484, #75528 ) ;
#24608=CARTESIAN_POINT ( 'NONE',  ( 3.616665348617805752E-21, 26.07813853931757464, -38.25000000000000000 ) ) ;
#24609=LINE ( 'NONE', #91972, #24210 ) ;
#24612=CARTESIAN_POINT ( 'NONE',  ( -1.249751218086241566, 43.67234525511032217, 17.34011378923078084 ) ) ;
#24618=CARTESIAN_POINT ( 'NONE',  ( 6.366644313785284837, 53.78389048455223787, 6.625974567219506284 ) ) ;
#24627=CARTESIAN_POINT ( 'NONE',  ( -8.239323762215395419, 53.79478660573261095, 3.999901775324819386 ) ) ;
#24650=CARTESIAN_POINT ( 'NONE',  ( 9.034470188793607193, 46.02977034662632150, 14.11149907944944104 ) ) ;
#24677=CARTESIAN_POINT ( 'NONE',  ( 23.55041599580185974, 25.19295639533963183, -33.17275278237224256 ) ) ;
#24688=CARTESIAN_POINT ( 'NONE',  ( 22.25838323674845043, 26.06530384004942391, 31.15016210260246510 ) ) ;
#24690=EDGE_CURVE ( 'NONE', #77058, #25026, #36047, .T. ) ;
#24702=CARTESIAN_POINT ( 'NONE',  ( -27.10511071441193565, 34.75829513984539432, -7.556984339685824281 ) ) ;
#24726=PRESENTATION_STYLE_ASSIGNMENT (( #32819 ) ) ;
#24730=CARTESIAN_POINT ( 'NONE',  ( 22.65267572660716766, 28.20149222899207686, -30.83791392134371989 ) ) ;
#24738=CARTESIAN_POINT ( 'NONE',  ( -22.11582326320239034, 26.03313043097262280, 31.35975099478267225 ) ) ;
#24760=ADVANCED_FACE ( 'NONE', ( #58928 ), #17941, .F. ) ;
#24764=CARTESIAN_POINT ( 'NONE',  ( -16.96324018633377051, 45.77154698568145363, 4.157797401561650119 ) ) ;
#24765=ORIENTED_EDGE ( 'NONE', *, *, #102166, .T. ) ;
#24781=CARTESIAN_POINT ( 'NONE',  ( 4.684274960302871098E-15, 26.07813853931757464, 38.25000000000000000 ) ) ;
#24788=B_SPLINE_CURVE_WITH_KNOTS ( 'NONE', 3,
 ( #54271, #87213, #34307, #8393, #40759, #9437, #66637, #48838, #24612, #97937, #15958, #67184, #42357, #75244, #16491, #90380, #41825, #17037, #58000, #91459, #74712, #73648 ),
 .UNSPECIFIED., .F., .F.,
 ( 4, 2, 2, 2, 2, 2, 2, 2, 2, 2, 4 ),
 ( 0.007183648798888384208, 0.007687614305072588451, 0.008191579811256791827, 0.008695545317440996069, 0.009199510823625200312, 0.009703476329809404555, 0.01020744183599360880, 0.01045942458908570745, 0.01071140734217780610, 0.01096339009526990475, 0.01121537284836200341 ),
 .UNSPECIFIED. ) ;
#24792=CARTESIAN_POINT ( 'NONE',  ( -17.88804523840099137, 43.18301036189587450, 5.551570213006435495 ) ) ;
#24795=CARTESIAN_POINT ( 'NONE',  ( -6.488521849125461038, 51.35019745309124772, -7.645917529146642799 ) ) ;
#24801=CARTESIAN_POINT ( 'NONE',  ( -29.68315524076989576, 13.12249633091057177, 39.60535821593503414 ) ) ;
#24802=EDGE_CURVE ( 'NONE', #14947, #101681, #16708, .T. ) ;
#24804=CIRCLE ( 'NONE', #85074, 63.00000000000000000 ) ;
#24810=CARTESIAN_POINT ( 'NONE',  ( 36.44012392015384449, 28.20304403842013841, -11.65813649474542579 ) ) ;
#24853=EDGE_CURVE ( 'NONE', #100346, #15839, #1190, .T. ) ;
#24856=CARTESIAN_POINT ( 'NONE',  ( 38.56016536716844456, 25.19268864103764471, 12.96944895395069786 ) ) ;
#24862=( LENGTH_UNIT ( ) NAMED_UNIT ( * ) SI_UNIT ( .MILLI., .METRE. ) );
#24871=( GEOMETRIC_REPRESENTATION_CONTEXT ( 3 ) GLOBAL_UNCERTAINTY_ASSIGNED_CONTEXT ( ( #68821 ) ) GLOBAL_UNIT_ASSIGNED_CONTEXT ( ( #16828, #56732, #66430 ) ) REPRESENTATION_CONTEXT ( 'NONE', 'WORKASPACE' ) );
#24874=CARTESIAN_POINT ( 'NONE',  ( -4.295862021341609882, 51.67716032263838599, 8.055692927004189485 ) ) ;
#24881=CARTESIAN_POINT ( 'NONE',  ( 29.35793203618246139, 13.99620286145417758, -42.06478814971845281 ) ) ;
#24896=CARTESIAN_POINT ( 'NONE',  ( -27.10511071441192144, -1.200000000000000030E-05, -8.806984339685890006 ) ) ;
#24918=ORIENTED_EDGE ( 'NONE', *, *, #16049, .F. ) ;
#24925=CARTESIAN_POINT ( 'NONE',  ( -23.21751746555280249, 28.11705169068991239, -30.70617127781034839 ) ) ;
#24953=CARTESIAN_POINT ( 'NONE',  ( 17.03955750629486943, 45.47802236175360235, 6.596165372994819087 ) ) ;
#24962=CARTESIAN_POINT ( 'NONE',  ( 27.10511071441176867, 36.60571256639526894, -10.05698433968634653 ) ) ;
#24979=CARTESIAN_POINT ( 'NONE',  ( -0.2961983223192701797, 12.99322937314420834, -51.71652672840411924 ) ) ;
#24991=CARTESIAN_POINT ( 'NONE',  ( 1.249862292819393650, 34.73247132126252978, -28.18210478855811019 ) ) ;
#24995=CARTESIAN_POINT ( 'NONE',  ( 7.561984444596827615, 52.15257306799382775, 2.009849713221146139 ) ) ;
#25009=( NAMED_UNIT ( * ) SI_UNIT ( $, .STERADIAN. ) SOLID_ANGLE_UNIT ( ) );
#25010=DIRECTION ( 'NONE',  ( -0.000000000000000000, 1.000000000000000000, -0.000000000000000000 ) ) ;
#25023=EDGE_LOOP ( 'NONE', ( #25639, #64621 ) ) ;
#25026=VERTEX_POINT ( 'NONE', #8798 ) ;
#25054=CARTESIAN_POINT ( 'NONE',  ( 15.43459503591739690, 44.00330752595467487, 5.765235879371150673 ) ) ;
#25060=DIRECTION ( 'NONE',  ( 0.000000000000000000, 1.000000000000000000, 0.000000000000000000 ) ) ;
#25079=CARTESIAN_POINT ( 'NONE',  ( -9.041225629235841055, 45.95386998337555440, 14.35441598012794628 ) ) ;
#25086=CARTESIAN_POINT ( 'NONE',  ( -36.32038103943577312, 28.15992945091319655, 12.39840696908056294 ) ) ;
#25098=CARTESIAN_POINT ( 'NONE',  ( -9.326356278839186942, 44.07198551910767037, 13.35271616244774151 ) ) ;
#25103=ADVANCED_FACE ( 'NONE', ( #48714, #91334, #75110, #17974, #17449 ), #83735, .F. ) ;
#25121=VECTOR ( 'NONE', #2325, 1000.000000000000000 ) ;
#25139=CARTESIAN_POINT ( 'NONE',  ( -1.098501441293660896, 25.84241065926105207, -38.88218280404267091 ) ) ;
#25145=SURFACE_SIDE_STYLE ('',( #58561 ) ) ;
#25148=CARTESIAN_POINT ( 'NONE',  ( 0.3378228332940266809, 45.31577368508814629, -18.71500938954003601 ) ) ;
#25153=CARTESIAN_POINT ( 'NONE',  ( 30.59355846058030082, 12.96027739219345243, 41.71512601614514182 ) ) ;
#25161=CARTESIAN_POINT ( 'NONE',  ( 25.85852276869992394, 35.03485039546205826, 8.998477900693142573 ) ) ;
#25164=CARTESIAN_POINT ( 'NONE',  ( 15.99032464848354884, 34.48495609265440720, 24.06104333071695223 ) ) ;
#25174=SURFACE_STYLE_FILL_AREA ( #74739 ) ;
#25177=DIRECTION ( 'NONE',  ( -0.000000000000000000, 1.000000000000000000, -0.000000000000000000 ) ) ;
#25181=ORIENTED_EDGE ( 'NONE', *, *, #8900, .T. ) ;
#25198=CARTESIAN_POINT ( 'NONE',  ( 0.4145533582058317235, 53.41936724997551522, -10.18222875895670576 ) ) ;
#25215=CARTESIAN_POINT ( 'NONE',  ( 46.81211797174984923, 13.24924033427095971, 15.90734432316328117 ) ) ;
#25216=CARTESIAN_POINT ( 'NONE',  ( 24.42526964689314184, 25.46411340096914699, -31.59704496624418724 ) ) ;
#25222=EDGE_LOOP ( 'NONE', ( #19105, #47832, #81685, #34511 ) ) ;
#25272=CARTESIAN_POINT ( 'NONE',  ( -28.79508601474831408, 15.38969543640857474, 41.74367987815701753 ) ) ;
#25295=CARTESIAN_POINT ( 'NONE',  ( 10.93080612294996712, 43.17347229229180527, -15.24212494374555504 ) ) ;
#25303=CARTESIAN_POINT ( 'NONE',  ( -46.77673112620464480, 13.57592939483832062, 15.58267473267816960 ) ) ;
#25305=ORIENTED_EDGE ( 'NONE', *, *, #93760, .T. ) ;
#25310=CARTESIAN_POINT ( 'NONE',  ( 9.636006000319470743, 53.53718130950936427, 2.125009785464772705 ) ) ;
#25317=CARTESIAN_POINT ( 'NONE',  ( -30.22873954704404298, 12.95661247755296941, 41.98212759391198290 ) ) ;
#25327=CARTESIAN_POINT ( 'NONE',  ( 1.255263095696489281E-15, 51.26930509877138320, 10.24999999999999822 ) ) ;
#25330=CARTESIAN_POINT ( 'NONE',  ( -17.16215690045858722, 34.18974779370575590, -24.24070848783700427 ) ) ;
#25348=CARTESIAN_POINT ( 'NONE',  ( 8.717882134064298683, 51.77839830771046081, 1.531152949373697281 ) ) ;
#25356=B_SPLINE_CURVE_WITH_KNOTS ( 'NONE', 3,
 ( #68924, #35510, #60310, #78578, #76996, #69970, #68389, #102872, #86179, #61363, #94256, #29037, #52179, #93185, #53777, #19876, #12252, #101282, #77533, #3651, #27432, #11177 ),
 .UNSPECIFIED., .F., .F.,
 ( 4, 2, 2, 2, 2, 2, 2, 2, 2, 2, 4 ),
 ( 0.003244682626514291002, 0.003748712926862984764, 0.004252743227211678960, 0.004756773527560372722, 0.005260803827909066484, 0.005764834128257760246, 0.006016849278432111030, 0.006268864428606461814, 0.006520879578780811731, 0.006772894728955162515, 0.007276925029303863215 ),
 .UNSPECIFIED. ) ;
#25359=CARTESIAN_POINT ( 'NONE',  ( -1.250612401299674659, 45.68690097979559539, -17.65351159749431531 ) ) ;
#25375=CARTESIAN_POINT ( 'NONE',  ( -4.523211276071191556, 53.69404211156058437, 8.281008664756861037 ) ) ;
#25377=CARTESIAN_POINT ( 'NONE',  ( -37.88570315047687131, 25.64574018102357655, -10.95617127781024003 ) ) ;
#25388=CARTESIAN_POINT ( 'NONE',  ( 0.000000000000000000, 0.000000000000000000, 63.00000000000000000 ) ) ;
#25406=SURFACE_STYLE_FILL_AREA ( #74963 ) ;
#25407=FILL_AREA_STYLE ('',( #65828 ) ) ;
#25409=ORIENTED_EDGE ( 'NONE', *, *, #32973, .T. ) ;
#25418=CARTESIAN_POINT ( 'NONE',  ( -4.044492309121838325, 51.90729595881780511, 7.473210932956116714 ) ) ;
#25421=ORIENTED_EDGE ( 'NONE', *, *, #92257, .T. ) ;
#25432=STYLED_ITEM ( 'NONE', ( #19113 ), #37977 ) ;
#25435=EDGE_CURVE ( 'NONE', #56430, #77058, #6007, .T. ) ;
#25445=CARTESIAN_POINT ( 'NONE',  ( 27.10511071441197117, 34.47735702144345282, 10.05698433968570704 ) ) ;
#25468=DIRECTION ( 'NONE',  ( 0.000000000000000000, -0.3420201433256727652, -0.9396926207859068736 ) ) ;
#25477=CARTESIAN_POINT ( 'NONE',  ( -10.28624191511830155, 43.99263840937192782, -12.90779740156156841 ) ) ;
#25485=VERTEX_POINT ( 'NONE', #89601 ) ;
#25489=B_SPLINE_CURVE_WITH_KNOTS ( 'NONE', 3,
 ( #106746, #17764, #57655, #58203, #65238, #32365, #106202, #57130, #42546, #65771, #56598, #7509, #40428, #89520, #31826, #83017, #40964, #74902, #25897, #98129, #41486, #82486, #73852, #50619, #33424, #17239, #15614, #24277, #90039, #24801 ),
 .UNSPECIFIED., .F., .F.,
 ( 4, 2, 2, 2, 2, 2, 2, 2, 2, 2, 2, 2, 2, 2, 4 ),
 ( 0.0004001071830457966967, 0.0008634720163662918963, 0.001326836849686787150, 0.002253566516327772454, 0.003180296182968758191, 0.004107025849609744796, 0.005033755516250729665, 0.005497120349571219498, 0.005960485182891710199, 0.006423850016212200031, 0.006655532432872437142, 0.006887214849532674252, 0.007118897266192911362, 0.007350579682853147605, 0.007813944516173620958 ),
 .UNSPECIFIED. ) ;
#25497=DIRECTION ( 'NONE',  ( -0.000000000000000000, 1.000000000000000000, -0.000000000000000000 ) ) ;
#25499=CARTESIAN_POINT ( 'NONE',  ( 17.25516560787562881, 45.65538004793684479, 4.306155947793937955 ) ) ;
#25517=CARTESIAN_POINT ( 'NONE',  ( 16.11174065067145733, 37.20923313995305648, -21.98001889856152147 ) ) ;
#25525=CARTESIAN_POINT ( 'NONE',  ( -5.290067270632216712, -1.200000000000000030E-05, 7.281152949374556371 ) ) ;
#25527=ADVANCED_FACE ( 'NONE', ( #3782 ), #20009, .F. ) ;
#25529=CARTESIAN_POINT ( 'NONE',  ( -46.79169002450407788, 18.53182619689688693, 15.81978731893011947 ) ) ;
#25534=CYLINDRICAL_SURFACE ( 'NONE', #69325, 1.250000000000001110 ) ;
#25541=CARTESIAN_POINT ( 'NONE',  ( 0.9542196423401080319, 34.32584019461168623, -29.31154340995110985 ) ) ;
#25544=FACE_OUTER_BOUND ( 'NONE', #82118, .T. ) ;
#25545=CARTESIAN_POINT ( 'NONE',  ( 8.559508646656405872, 51.55638410492942825, 4.031152949374444461 ) ) ;
#25554=B_SPLINE_CURVE_WITH_KNOTS ( 'NONE', 3,
 ( #65751, #71696, #7488, #32874, #72245, #81911, #97046, #31289, #89500, #23724, #38832, #73831, #106725, #104607, #64175, #98631, #90555, #46898, #79804, #96533, #5901, #23186 ),
 .UNSPECIFIED., .F., .F.,
 ( 4, 2, 2, 2, 2, 2, 2, 2, 2, 2, 4 ),
 ( 0.003250743696380571646, 0.003754779946395551526, 0.004258816196410531406, 0.004762852446425511720, 0.005266888696440491166, 0.005770924946455471480, 0.006022943071462952963, 0.006274961196470434446, 0.006526979321477914195, 0.006778997446485395678, 0.007283033696500349971 ),
 .UNSPECIFIED. ) ;
#25555=ORIENTED_EDGE ( 'NONE', *, *, #13692, .F. ) ;
#25558=CARTESIAN_POINT ( 'NONE',  ( -37.56673239365849781, -1.200000000000000030E-05, 12.20617127781066102 ) ) ;
#25568=CARTESIAN_POINT ( 'NONE',  ( 9.643395340371860414, 44.08772782729035100, -13.07263357742781196 ) ) ;
#25598=CARTESIAN_POINT ( 'NONE',  ( 7.350234075050753546, 52.09155505363125371, -3.136924920048258070 ) ) ;
#25601=CARTESIAN_POINT ( 'NONE',  ( 3.337162542380456721E-15, 35.08181111624585213, 27.25000000000000000 ) ) ;
#25612=ORIENTED_EDGE ( 'NONE', *, *, #26556, .F. ) ;
#25618=CARTESIAN_POINT ( 'NONE',  ( -0.07765829730716486412, 12.91535575337015196, 51.74999999999997868 ) ) ;
#25622=CARTESIAN_POINT ( 'NONE',  ( -0.6448886116837295734, 44.02064573959138016, -16.41618173662891778 ) ) ;
#25626=CARTESIAN_POINT ( 'NONE',  ( 0.7848998160350572073, 45.39389416767541263, 18.48651031598092587 ) ) ;
#25627=CARTESIAN_POINT ( 'NONE',  ( 2.607260012660386551E-19, 12.91535575337012354, -51.75000000000000711 ) ) ;
#25631=CARTESIAN_POINT ( 'NONE',  ( -10.28624191512074226, 46.12099395432516502, 12.90779740155501187 ) ) ;
#25639=ORIENTED_EDGE ( 'NONE', *, *, #80510, .T. ) ;
#25652=DIRECTION ( 'NONE',  ( 0.000000000000000000, 1.000000000000000000, -0.000000000000000000 ) ) ;
#25656=ORIENTED_EDGE ( 'NONE', *, *, #35012, .F. ) ;
#25674=MECHANICAL_DESIGN_GEOMETRIC_PRESENTATION_REPRESENTATION('',(#91086),#56706);
#25675=CARTESIAN_POINT ( 'NONE',  ( -36.49843703712726750, 25.91515891220674206, 12.86019707471129436 ) ) ;
#25693=CARTESIAN_POINT ( 'NONE',  ( -9.554383626907007709, 53.41962121727333823, 3.542541134239667766 ) ) ;
#25694=EDGE_CURVE ( 'NONE', #68832, #81828, #18938, .T. ) ;
#25704=CARTESIAN_POINT ( 'NONE',  ( 1.250306967194193764, 45.68544320488086896, -17.65754872500330208 ) ) ;
#25755=CARTESIAN_POINT ( 'NONE',  ( 7.308143880813624094, 54.29032144469603338, 2.719777064722692650 ) ) ;
#25766=CARTESIAN_POINT ( 'NONE',  ( 47.57454933833927413, 12.59078750739571184, 14.43852527042908918 ) ) ;
#25768=CARTESIAN_POINT ( 'NONE',  ( 23.54584815914472884, 25.90672388542958871, -30.73942196852247122 ) ) ;
#25783=( NAMED_UNIT ( * ) SI_UNIT ( $, .STERADIAN. ) SOLID_ANGLE_UNIT ( ) );
#25821=FILL_AREA_STYLE ('',( #33347 ) ) ;
#25853=EDGE_LOOP ( 'NONE', ( #90153, #7922 ) ) ;
#25855=CARTESIAN_POINT ( 'NONE',  ( -7.312676561755618643, 54.25590764141821154, -2.971987819145548215 ) ) ;
#25858=CARTESIAN_POINT ( 'NONE',  ( -17.89160253087132801, 45.33672951329189260, 5.299667771043163000 ) ) ;
#25867=CARTESIAN_POINT ( 'NONE',  ( 15.89400772911373672, 45.88919441563187718, 6.421120341668727249 ) ) ;
#25869=CARTESIAN_POINT ( 'NONE',  ( 15.54898481255689724, 46.20784644949144848, -4.780735607413824084 ) ) ;
#25891=CARTESIAN_POINT ( 'NONE',  ( 49.07537269081996811, 14.00518788141342164, 14.91829442325235000 ) ) ;
#25897=CARTESIAN_POINT ( 'NONE',  ( -28.61418328824325030, 13.49088233573900553, 40.19504096224933676 ) ) ;
#25934=CARTESIAN_POINT ( 'NONE',  ( 15.64449080980709361, 44.06115359459996483, -4.637972761859016302 ) ) ;
#25946=( NAMED_UNIT ( * ) SI_UNIT ( $, .STERADIAN. ) SOLID_ANGLE_UNIT ( ) );
#25971=AXIS2_PLACEMENT_3D ( 'NONE', #27006, #53375, #61481 ) ;
#25987=EDGE_LOOP ( 'NONE', ( #46808, #11864, #83005, #58454 ) ) ;
#26004=( NAMED_UNIT ( * ) PLANE_ANGLE_UNIT ( ) SI_UNIT ( $, .RADIAN. ) );
#26019=FACE_BOUND ( 'NONE', #25853, .T. ) ;
#26026=CARTESIAN_POINT ( 'NONE',  ( -9.721254568807728091, 44.08029630702152701, -13.03955032007097969 ) ) ;
#26042=CARTESIAN_POINT ( 'NONE',  ( -49.02741474918240527, 7.901513937033902479, -16.35941288907603308 ) ) ;
#26047=CARTESIAN_POINT ( 'NONE',  ( 17.64329382111521127, 45.32481993297742662, 6.176472982800854439 ) ) ;
#26069=( LENGTH_UNIT ( ) NAMED_UNIT ( * ) SI_UNIT ( .MILLI., .METRE. ) );
#26072=CARTESIAN_POINT ( 'NONE',  ( -0.9426293753149518340, 17.83864352553418442, -49.67541775974505924 ) ) ;
#26084=FACE_BOUND ( 'NONE', #92941, .T. ) ;
#26092=CARTESIAN_POINT ( 'NONE',  ( 0.08434562425236380445, 44.08548369317411897, 16.25000000000002842 ) ) ;
#26099=DIRECTION ( 'NONE',  ( 0.000000000000000000, 0.000000000000000000, 1.000000000000000000 ) ) ;
#26103=AXIS2_PLACEMENT_3D ( 'NONE', #8500, #26865, #43541 ) ;
#26105=CARTESIAN_POINT ( 'NONE',  ( -9.647409248820050465, 51.27677058736198745, -3.402434490781860443 ) ) ;
#26107=CARTESIAN_POINT ( 'NONE',  ( 16.64348903516496492, 43.47556584774762456, -6.657797401562562278 ) ) ;
#26126=CARTESIAN_POINT ( 'NONE',  ( 27.72723468844076322, 36.41215165560291922, -9.903269780309406300 ) ) ;
#26128=CARTESIAN_POINT ( 'NONE',  ( -22.57731121199999080, 28.20557510165627235, 30.87924556879399063 ) ) ;
#26141=CARTESIAN_POINT ( 'NONE',  ( 47.78396355473342538, 15.50490861890768635, -16.83695313132077231 ) ) ;
#26149=( NAMED_UNIT ( * ) SI_UNIT ( $, .STERADIAN. ) SOLID_ANGLE_UNIT ( ) );
#26157=CARTESIAN_POINT ( 'NONE',  ( -1.116779127739723210, 14.48579825753870765, 51.07894496868025414 ) ) ;
#26163=CARTESIAN_POINT ( 'NONE',  ( 0.3346317158865195207, 46.19713137549851467, 16.29267624532406344 ) ) ;
#26164=CARTESIAN_POINT ( 'NONE',  ( 0.9532286629884955120, 13.93731468125776374, -51.31239236590303676 ) ) ;
#26170=AXIS2_PLACEMENT_3D ( 'NONE', #56635, #33458, #73886 ) ;
#26179=CARTESIAN_POINT ( 'NONE',  ( -15.54267344201861434, 34.77189900418887447, -23.41194221326999525 ) ) ;
#26184=SURFACE_STYLE_USAGE ( .BOTH. , #24047 ) ;
#26204=CARTESIAN_POINT ( 'NONE',  ( -36.37766630548127722, 28.20754914235178390, -11.81157041065297975 ) ) ;
#26219=CARTESIAN_POINT ( 'NONE',  ( 0.000000000000000000, 0.000000000000000000, 35.82893434829263413 ) ) ;
#26226=CARTESIAN_POINT ( 'NONE',  ( -8.559508646656370345, 53.96349637827587031, 1.531152949374564365 ) ) ;
#26236=CARTESIAN_POINT ( 'NONE',  ( 30.71756172601006085, 13.08262462249239100, 41.56006324341294800 ) ) ;
#26246=CARTESIAN_POINT ( 'NONE',  ( -29.85247340496026780, 12.86254483752416711, -39.61457847635377050 ) ) ;
#26282=CARTESIAN_POINT ( 'NONE',  ( -9.182549847561064738, 53.50073754291216943, -3.877052053296246914 ) ) ;
#26306=CARTESIAN_POINT ( 'NONE',  ( -47.90305809253368352, 10.05329658600980380, -16.85535821593460781 ) ) ;
#26312=( NAMED_UNIT ( * ) PLANE_ANGLE_UNIT ( ) SI_UNIT ( $, .RADIAN. ) );
#26358=LINE ( 'NONE', #34442, #56638 ) ;
#26392=CARTESIAN_POINT ( 'NONE',  ( 15.55855383130857383, 46.20420475984591491, 4.781350493801785007 ) ) ;
#26399=CARTESIAN_POINT ( 'NONE',  ( 0.000000000000000000, 56.87938524157181774, 0.000000000000000000 ) ) ;
#26414=CARTESIAN_POINT ( 'NONE',  ( -5.930615719913575390, 51.27008138075110111, -8.357849859401051518 ) ) ;
#26419=CARTESIAN_POINT ( 'NONE',  ( -11.36440988823891018, 43.57563821449488017, -13.50564546251721509 ) ) ;
#26429=ORIENTED_EDGE ( 'NONE', *, *, #21027, .F. ) ;
#26443=CARTESIAN_POINT ( 'NONE',  ( 0.6418249586330869727, 37.14405262803889940, 27.42421770560467209 ) ) ;
#26448=CARTESIAN_POINT ( 'NONE',  ( -38.81968145246697333, 25.17318795309900281, -12.34933546114397984 ) ) ;
#26453=CARTESIAN_POINT ( 'NONE',  ( 16.02298420952691771, 43.96085526717300951, -4.310639523075502133 ) ) ;
#26477=ORIENTED_EDGE ( 'NONE', *, *, #38374, .F. ) ;
#26484=CARTESIAN_POINT ( 'NONE',  ( 4.885277709441186111, 53.57062629529884390, 8.466573372809225617 ) ) ;
#26486=EDGE_CURVE ( 'NONE', #12685, #79036, #77413, .T. ) ;
#26490=CARTESIAN_POINT ( 'NONE',  ( 28.28105526222837085, 36.39302830438535352, 8.375257444619659708 ) ) ;
#26497=CARTESIAN_POINT ( 'NONE',  ( 30.64348173561366195, 7.829960647508035443, -41.65811975367154218 ) ) ;
#26498=DIRECTION ( 'NONE',  ( 0.000000000000000000, 1.000000000000000000, -0.000000000000000000 ) ) ;
#26505=CARTESIAN_POINT ( 'NONE',  ( 5.749654562269868196E-15, 24.35682532067546902, 46.94949242731048145 ) ) ;
#26520=CARTESIAN_POINT ( 'NONE',  ( 9.491091496279695579E-16, 54.30758622938872549, 7.749999999999999112 ) ) ;
#26540=CARTESIAN_POINT ( 'NONE',  ( -1.250441718889297782, 36.68885173498831165, -28.65503145627670989 ) ) ;
#26548=UNCERTAINTY_MEASURE_WITH_UNIT (LENGTH_MEASURE( 1.000000000000000082E-05 ), #51975, 'distance_accuracy_value', 'NONE');
#26556=EDGE_CURVE ( 'NONE', #92815, #104203, #56401, .T. ) ;
#26558=ORIENTED_EDGE ( 'NONE', *, *, #4748, .F. ) ;
#26577=COLOUR_RGB ( '', 0.66274510, 0.83137255, 0.94901961) ;
#26580=CARTESIAN_POINT ( 'NONE',  ( 26.11201203623409484, 37.18374287936713785, -8.043240354485387655 ) ) ;
#26583=FACE_OUTER_BOUND ( 'NONE', #35118, .T. ) ;
#26604=CARTESIAN_POINT ( 'NONE',  ( 0.1683254529209002592, 35.08181111624585924, -27.25000000000000711 ) ) ;
#26605=VECTOR ( 'NONE', #33318, 1000.000000000000227 ) ;
#26611=MECHANICAL_DESIGN_GEOMETRIC_PRESENTATION_REPRESENTATION('',(#48951),#86872);
#26623=CARTESIAN_POINT ( 'NONE',  ( -0.6190732552358791940, 13.31368202499944253, -49.41014691098467893 ) ) ;
#26627=CARTESIAN_POINT ( 'NONE',  ( 10.12089751115670566, 43.29055768924980185, -15.40779740156171052 ) ) ;
#26633=EDGE_LOOP ( 'NONE', ( #100676, #79635, #31894, #17939 ) ) ;
#26639=CARTESIAN_POINT ( 'NONE',  ( -16.48453010140518060, 43.81223275022514940, 4.157797401561229123 ) ) ;
#26642=CARTESIAN_POINT ( 'NONE',  ( -22.37422507490808954, 28.20471669103546475, 31.02961587878847638 ) ) ;
#26655=ORIENTED_EDGE ( 'NONE', *, *, #63996, .T. ) ;
#26658=CARTESIAN_POINT ( 'NONE',  ( 47.24423074384412757, 16.91655035847116650, -16.58644287016981522 ) ) ;
#26663=( NAMED_UNIT ( * ) SI_UNIT ( $, .STERADIAN. ) SOLID_ANGLE_UNIT ( ) );
#26669=( LENGTH_UNIT ( ) NAMED_UNIT ( * ) SI_UNIT ( .MILLI., .METRE. ) );
#26694=CARTESIAN_POINT ( 'NONE',  ( -46.77678417914653153, 18.74709138458503332, -15.58010501040351592 ) ) ;
#26698=CARTESIAN_POINT ( 'NONE',  ( -36.81701302529270237, 27.89050725896737859, 13.21903061592501061 ) ) ;
#26700=ORIENTED_EDGE ( 'NONE', *, *, #94079, .F. ) ;
#26703=CARTESIAN_POINT ( 'NONE',  ( -16.75187969033554936, 34.99134772383131065, -21.80698433968595751 ) ) ;
#26708=CARTESIAN_POINT ( 'NONE',  ( -17.39223945882862665, 34.17273883436914872, 24.13379576214062538 ) ) ;
#26712=CARTESIAN_POINT ( 'NONE',  ( 9.500904806078523279, 51.30114290918681519, -3.607704468417440857 ) ) ;
#26713=DIRECTION ( 'NONE',  ( 0.000000000000000000, 0.000000000000000000, 1.000000000000000000 ) ) ;
#26726=VERTEX_POINT ( 'NONE', #22120 ) ;
#26737=DIRECTION ( 'NONE',  ( 0.000000000000000000, 1.000000000000000000, 0.000000000000000000 ) ) ;
#26743=CARTESIAN_POINT ( 'NONE',  ( 1.231392085578007389, 11.27926140874486727, 50.25247630643868746 ) ) ;
#26757=SURFACE_STYLE_USAGE ( .BOTH. , #67713 ) ;
#26764=DIRECTION ( 'NONE',  ( 0.000000000000000000, 0.000000000000000000, 1.000000000000000000 ) ) ;
#26771=CARTESIAN_POINT ( 'NONE',  ( 0.08416673536544136414, 28.20649408426940141, 38.24999999999999289 ) ) ;
#26772=CARTESIAN_POINT ( 'NONE',  ( -30.82780738024908729, 10.08347807711980515, -40.33814864068006756 ) ) ;
#26781=ORIENTED_EDGE ( 'NONE', *, *, #69849, .T. ) ;
#26782=LINE ( 'NONE', #93071, #89472 ) ;
#26789=UNCERTAINTY_MEASURE_WITH_UNIT (LENGTH_MEASURE( 1.000000000000000082E-05 ), #72703, 'distance_accuracy_value', 'NONE');
#26790=FACE_BOUND ( 'NONE', #12184, .T. ) ;
#26804=EDGE_CURVE ( 'NONE', #34768, #13191, #5060, .T. ) ;
#26815=CARTESIAN_POINT ( 'NONE',  ( -16.42611686831678242, 36.46285186709818760, -24.26654634025086210 ) ) ;
#26817=VECTOR ( 'NONE', #54009, 1000.000000000000000 ) ;
#26820=UNCERTAINTY_MEASURE_WITH_UNIT (LENGTH_MEASURE( 1.000000000000000082E-05 ), #90012, 'distance_accuracy_value', 'NONE');
#26821=CARTESIAN_POINT ( 'NONE',  ( 24.46199350025671038, 25.40999692020810130, -31.75662788421451665 ) ) ;
#26828=ORIENTED_EDGE ( 'NONE', *, *, #97761, .T. ) ;
#26830=CARTESIAN_POINT ( 'NONE',  ( -48.02835407290533709, 9.771516447483559631, -16.85535821593460426 ) ) ;
#26833=CARTESIAN_POINT ( 'NONE',  ( -36.56938426534607345, 26.05443706425352346, -11.43459265307532746 ) ) ;
#26834=VECTOR ( 'NONE', #84481, 1000.000000000000000 ) ;
#26852=CARTESIAN_POINT ( 'NONE',  ( 17.26536970378601765, 45.41327343741739497, -6.504208684746127567 ) ) ;
#26854=CARTESIAN_POINT ( 'NONE',  ( -16.75187969033532553, 37.11970326878314808, 21.80698433968612093 ) ) ;
#26862=CYLINDRICAL_SURFACE ( 'NONE', #93422, 13.27631144943088515 ) ;
#26865=DIRECTION ( 'NONE',  ( -0.000000000000000000, 1.000000000000000000, 0.000000000000000000 ) ) ;
#26880=CARTESIAN_POINT ( 'NONE',  ( 0.000000000000000000, 32.68727484027578356, 0.000000000000000000 ) ) ;
#26913=ORIENTED_EDGE ( 'NONE', *, *, #38775, .F. ) ;
#26921=PRESENTATION_STYLE_ASSIGNMENT (( #35539 ) ) ;
#26958=CARTESIAN_POINT ( 'NONE',  ( -1.220619361806398961, 45.62969810379784974, -17.81327476936460030 ) ) ;
#26962=COLOUR_RGB ( '', 0.40784314, 0.44705882, 0.49803922) ;
#26971=CARTESIAN_POINT ( 'NONE',  ( -5.122788966609808092, 53.50683659463715713, 8.531152949374556371 ) ) ;
#26976=AXIS2_PLACEMENT_3D ( 'NONE', #75077, #82660, #50801 ) ;
#26980=VECTOR ( 'NONE', #89666, 1000.000000000000000 ) ;
#26989=ORIENTED_EDGE ( 'NONE', *, *, #91496, .T. ) ;
#27006=CARTESIAN_POINT ( 'NONE',  ( 0.000000000000000000, -1.200000000000000030E-05, 17.50000000000000000 ) ) ;
#27013=AXIS2_PLACEMENT_3D ( 'NONE', #74498, #40544, #65358 ) ;
#27019=CARTESIAN_POINT ( 'NONE',  ( 27.42610126120553460, 36.50006826818918171, 10.02586106038927305 ) ) ;
#27036=SURFACE_STYLE_USAGE ( .BOTH. , #9726 ) ;
#27041=CYLINDRICAL_SURFACE ( 'NONE', #88775, 1.250000000000001110 ) ;
#27057=ORIENTED_EDGE ( 'NONE', *, *, #11033, .T. ) ;
#27058=PRESENTATION_STYLE_ASSIGNMENT (( #68007 ) ) ;
#27071=CARTESIAN_POINT ( 'NONE',  ( -1.102002922838543730, 36.52516746709567030, -29.11124182180218511 ) ) ;
#27073=DIRECTION ( 'NONE',  ( -0.000000000000000000, 1.000000000000000000, -0.000000000000000000 ) ) ;
#27105=CARTESIAN_POINT ( 'NONE',  ( -16.75187969033554936, -1.200000000000000030E-05, -21.80698433968595751 ) ) ;
#27106=( NAMED_UNIT ( * ) PLANE_ANGLE_UNIT ( ) SI_UNIT ( $, .RADIAN. ) );
#27138=CARTESIAN_POINT ( 'NONE',  ( -1.152188841818234133E-13, -1.200000000000000030E-05, -49.25000000000000000 ) ) ;
#27150=CARTESIAN_POINT ( 'NONE',  ( -7.349939847252962011, 52.09173981223236183, -3.136341692644931456 ) ) ;
#27157=CARTESIAN_POINT ( 'NONE',  ( 36.31982962151198535, 26.03215893330996522, 12.39505216599222770 ) ) ;
#27159=CARTESIAN_POINT ( 'NONE',  ( 9.953339094172397594, 44.05804770646479085, -12.94124162574283510 ) ) ;
#27163=CARTESIAN_POINT ( 'NONE',  ( -4.036264873047459290, 54.13888204563361484, -7.153725211838067644 ) ) ;
#27189=ORIENTED_EDGE ( 'NONE', *, *, #11769, .T. ) ;
#27197=( NAMED_UNIT ( * ) SI_UNIT ( $, .STERADIAN. ) SOLID_ANGLE_UNIT ( ) );
#27237=CARTESIAN_POINT ( 'NONE',  ( -16.12443969100768371, 34.43093541110913236, -24.15018447417424241 ) ) ;
#27268=CARTESIAN_POINT ( 'NONE',  ( 48.91297851734898927, 13.22767571191357838, -16.49376885358496736 ) ) ;
#27274=B_SPLINE_CURVE_WITH_KNOTS ( 'NONE', 3,
 ( #50148, #68478, #34006, #1580, #66877, #99765, #50652, #27522, #59862, #76542, #9676, #99218, #25934, #67933, #26453, #34541, #58793, #83568 ),
 .UNSPECIFIED., .F., .F.,
 ( 4, 2, 2, 2, 2, 2, 2, 2, 4 ),
 ( 0.007186523243523818515, 0.007691201619852154787, 0.008195879996180491928, 0.008700558372508828200, 0.009205236748837164473, 0.009709915125165500746, 0.01021459350149383702, 0.01071927187782217329, 0.01122395025415050956 ),
 .UNSPECIFIED. ) ;
#27283=CARTESIAN_POINT ( 'NONE',  ( 0.1555636098919296328, 13.68574936779574891, 49.25766232864418726 ) ) ;
#27291=ADVANCED_FACE ( 'NONE', ( #5782 ), #69996, .F. ) ;
#27301=CARTESIAN_POINT ( 'NONE',  ( 30.90097930193326192, 13.60840423680625300, 41.14831600716837556 ) ) ;
#27342=CYLINDRICAL_SURFACE ( 'NONE', #23865, 1.250000000000001110 ) ;
#27352=DIRECTION ( 'NONE',  ( -0.000000000000000000, 1.000000000000000000, 0.000000000000000000 ) ) ;
#27367=ORIENTED_EDGE ( 'NONE', *, *, #18949, .T. ) ;
#27378=ORIENTED_EDGE ( 'NONE', *, *, #24853, .F. ) ;
#27389=CARTESIAN_POINT ( 'NONE',  ( 16.96468291457295052, 45.49948827470971224, -6.626685320826405601 ) ) ;
#27408=CARTESIAN_POINT ( 'NONE',  ( 17.86210361494363141, 36.33998000098823411, -23.65466217301442242 ) ) ;
#27410=EDGE_LOOP ( 'NONE', ( #50378, #9846 ) ) ;
#27411=SURFACE_SIDE_STYLE ('',( #27941 ) ) ;
#27432=CARTESIAN_POINT ( 'NONE',  ( 0.1682304686574977171, 36.30024107553214918, -29.74999999999999289 ) ) ;
#27440=ORIENTED_EDGE ( 'NONE', *, *, #79054, .T. ) ;
#27441=DIRECTION ( 'NONE',  ( 0.000000000000000000, 1.000000000000000000, -0.000000000000000000 ) ) ;
#27447=ORIENTED_EDGE ( 'NONE', *, *, #80414, .F. ) ;
#27451=EDGE_CURVE ( 'NONE', #44416, #32988, #53752, .T. ) ;
#27480=EDGE_CURVE ( 'NONE', #65902, #83087, #22838, .T. ) ;
#27494=ORIENTED_EDGE ( 'NONE', *, *, #4331, .F. ) ;
#27505=CARTESIAN_POINT ( 'NONE',  ( -23.97745264537545040, 25.74979706031962579, -30.95109073255507326 ) ) ;
#27510=CARTESIAN_POINT ( 'NONE',  ( 0.7847972972063655961, 36.39241504557466556, 29.48654454112834244 ) ) ;
#27522=CARTESIAN_POINT ( 'NONE',  ( 15.43434203115574377, 44.00353298636623123, -5.764138573818327949 ) ) ;
#27547=EDGE_LOOP ( 'NONE', ( #95971, #75692, #46122, #29223 ) ) ;
#27559=EDGE_LOOP ( 'NONE', ( #98012, #84254 ) ) ;
#27566=PRESENTATION_STYLE_ASSIGNMENT (( #76055 ) ) ;
#27572=( LENGTH_UNIT ( ) NAMED_UNIT ( * ) SI_UNIT ( .MILLI., .METRE. ) );
#27589=CARTESIAN_POINT ( 'NONE',  ( 1.464720647026959308E-15, 47.77514352166374323, 11.96035173608223090 ) ) ;
#27625=CARTESIAN_POINT ( 'NONE',  ( -48.49185632690704750, 10.49696353563009055, -14.43858684427239325 ) ) ;
#27639=VERTEX_POINT ( 'NONE', #68152 ) ;
#27661=FILL_AREA_STYLE ('',( #33596 ) ) ;
#27667=ORIENTED_EDGE ( 'NONE', *, *, #30862, .T. ) ;
#27679=B_SPLINE_CURVE_WITH_KNOTS ( 'NONE', 3,
 ( #56416, #15440, #106031, #7342, #32176, #59643, #84443, #59110, #34327, #35933, #61238, #11057, #10009, #18673, #52057, #10536, #68259, #43453, #84972, #26772, #94122, #67203, #43980, #100079, #20288, #42374, #50983, #26246, #69332, #60715 ),
 .UNSPECIFIED., .F., .F.,
 ( 4, 2, 2, 2, 2, 2, 2, 2, 2, 2, 2, 2, 2, 2, 4 ),
 ( 0.01451434872829001493, 0.01497952839231827919, 0.01521211822433241566, 0.01544470805634655386, 0.01567729788836069033, 0.01590988772037483026, 0.01637506738440308585, 0.01684024704843134143, 0.01730542671245959702, 0.01823578604051610125, 0.01916614536857260548, 0.02009650469662910624, 0.02102686402468561047, 0.02149204368871385912, 0.02195722335274210429 ),
 .UNSPECIFIED. ) ;
#27700=CARTESIAN_POINT ( 'NONE',  ( -5.126781800564398139, 54.24761383184393537, -6.031152949374157579 ) ) ;
#27709=CARTESIAN_POINT ( 'NONE',  ( 0.000000000000000000, 55.00000000000000000, 0.000000000000000000 ) ) ;
#27725=ORIENTED_EDGE ( 'NONE', *, *, #5205, .T. ) ;
#27731=VERTEX_POINT ( 'NONE', #77309 ) ;
#27739=EDGE_CURVE ( 'NONE', #27639, #16669, #7679, .T. ) ;
#27745=( NAMED_UNIT ( * ) SI_UNIT ( $, .STERADIAN. ) SOLID_ANGLE_UNIT ( ) );
#27752=CARTESIAN_POINT ( 'NONE',  ( -23.21751746555280249, 25.98869614573808207, -30.70617127781034839 ) ) ;
#27754=CARTESIAN_POINT ( 'NONE',  ( -26.70997489550019210, 34.89067225687768570, -7.618312596025223371 ) ) ;
#27801=CARTESIAN_POINT ( 'NONE',  ( -36.31989234532075272, 28.16027530257773392, -12.39692247340019371 ) ) ;
#27808=CARTESIAN_POINT ( 'NONE',  ( 1.380949872273418154E-15, 45.89575828009193259, 11.27631144943088337 ) ) ;
#27817=CARTESIAN_POINT ( 'NONE',  ( 1.159636676343374750, 11.84329530645718265, 50.01746790140171584 ) ) ;
#27850=CARTESIAN_POINT ( 'NONE',  ( 9.300970015859846285, 53.68222913732174817, -1.771665439178985446 ) ) ;
#27858=CARTESIAN_POINT ( 'NONE',  ( 0.000000000000000000, 27.68727484027578356, -33.82893434829263413 ) ) ;
#27861=ORIENTED_EDGE ( 'NONE', *, *, #48575, .T. ) ;
#27862=B_SPLINE_CURVE_WITH_KNOTS ( 'NONE', 3,
 ( #62909, #95278, #87187, #37604, #86670, #69933, #11671, #21407, #93681, #44604, #70466, #3609, #61860, #13797, #79602, #36011, #102292, #54242, #20377, #12739, #79079, #13266, #28993, #45661 ),
 .UNSPECIFIED., .F., .F.,
 ( 4, 2, 2, 2, 2, 2, 2, 2, 2, 2, 2, 4 ),
 ( 0.007009756851916126852, 0.007512278926379567512, 0.008014801000843008172, 0.008517323075306448832, 0.008768584112538169162, 0.009019845149769889492, 0.009271106187001611557, 0.009522367224233333621, 0.01002488929869677428, 0.01027615033592849635, 0.01052741137316021841, 0.01102993344762366601 ),
 .UNSPECIFIED. ) ;
#27876=SURFACE_STYLE_USAGE ( .BOTH. , #1931 ) ;
#27901=ORIENTED_EDGE ( 'NONE', *, *, #5146, .T. ) ;
#27909=CARTESIAN_POINT ( 'NONE',  ( -17.85280542844888529, 43.24717813759219354, -5.051306223358245973 ) ) ;
#27929=SURFACE_SIDE_STYLE ('',( #75346 ) ) ;
#27936=EDGE_CURVE ( 'NONE', #54576, #79036, #45599, .T. ) ;
#27941=SURFACE_STYLE_FILL_AREA ( #86155 ) ;
#27965=CARTESIAN_POINT ( 'NONE',  ( -1.011535333131581726, 27.47315533557190648, 40.25229125636516159 ) ) ;
#27970=DIRECTION ( 'NONE',  ( -0.000000000000000000, 1.000000000000000000, -0.000000000000000000 ) ) ;
#27995=EDGE_CURVE ( 'NONE', #54873, #96644, #62748, .T. ) ;
#28035=ORIENTED_EDGE ( 'NONE', *, *, #9671, .F. ) ;
#28037=CARTESIAN_POINT ( 'NONE',  ( 1.011934152981637691, 36.47529646805227088, 29.25177536496077835 ) ) ;
#28053=CARTESIAN_POINT ( 'NONE',  ( -16.32418145836352963, 45.71594865110102290, 6.626690021756176385 ) ) ;
#28074=DIRECTION ( 'NONE',  ( 0.000000000000000000, 1.000000000000000000, -0.000000000000000000 ) ) ;
#28085=VECTOR ( 'NONE', #61568, 1000.000000000000227 ) ;
#28089=( NAMED_UNIT ( * ) SI_UNIT ( $, .STERADIAN. ) SOLID_ANGLE_UNIT ( ) );
#28104=( LENGTH_UNIT ( ) NAMED_UNIT ( * ) SI_UNIT ( .MILLI., .METRE. ) );
#28109=LINE ( 'NONE', #85246, #71440 ) ;
#28120=FILL_AREA_STYLE_COLOUR ( '', #81592 ) ;
#28137=CARTESIAN_POINT ( 'NONE',  ( -15.89400772911371540, 45.88919441563189849, -6.421120341668841824 ) ) ;
#28143=CARTESIAN_POINT ( 'NONE',  ( -27.10511071441333542, 36.88665068479732412, -7.556984339679825524 ) ) ;
#28149=CARTESIAN_POINT ( 'NONE',  ( -28.35801031271196138, 36.30512300106359191, 8.950586257191373463 ) ) ;
#28153=CYLINDRICAL_SURFACE ( 'NONE', #106338, 1.250000000000001110 ) ;
#28176=ORIENTED_EDGE ( 'NONE', *, *, #17746, .T. ) ;
#28185=( NAMED_UNIT ( * ) PLANE_ANGLE_UNIT ( ) SI_UNIT ( $, .RADIAN. ) );
#28189=CARTESIAN_POINT ( 'NONE',  ( 0.6187927933819248327, 18.48342808587748820, 49.40998285506532994 ) ) ;
#28207=ORIENTED_EDGE ( 'NONE', *, *, #11033, .F. ) ;
#28210=CARTESIAN_POINT ( 'NONE',  ( 3.643324519380566085E-15, 34.17188553058033307, 29.75000000000000355 ) ) ;
#28214=FACE_BOUND ( 'NONE', #55252, .T. ) ;
#28225=CARTESIAN_POINT ( 'NONE',  ( -4.959717421002378224, 53.54742482023647909, -8.497505399302097473 ) ) ;
#28228=CARTESIAN_POINT ( 'NONE',  ( -10.11986806485388080, 46.15873290010527086, -12.90779740156157374 ) ) ;
#28254=CARTESIAN_POINT ( 'NONE',  ( 46.78576055570671599, 18.82161635153732959, -15.45372055756656948 ) ) ;
#28256=FACE_BOUND ( 'NONE', #27559, .T. ) ;
#28258=CARTESIAN_POINT ( 'NONE',  ( -48.69302668856963123, 13.59112006856911670, 16.66703530934380240 ) ) ;
#28261=FILL_AREA_STYLE ('',( #36363 ) ) ;
#28273=CARTESIAN_POINT ( 'NONE',  ( -26.49239580055373366, 34.70527438946334797, -9.907946246971482296 ) ) ;
#28282=CARTESIAN_POINT ( 'NONE',  ( -11.04468709431030149, 45.87751353276775035, -13.15154111190464548 ) ) ;
#28283=SURFACE_STYLE_USAGE ( .BOTH. , #43894 ) ;
#28291=( NAMED_UNIT ( * ) SI_UNIT ( $, .STERADIAN. ) SOLID_ANGLE_UNIT ( ) );
#28298=CARTESIAN_POINT ( 'NONE',  ( 9.058657501722350958, 46.09928351899775123, -13.86902144048109697 ) ) ;
#28302=CARTESIAN_POINT ( 'NONE',  ( 49.13349184603276854, 7.785586125543622948, -16.19411946323722873 ) ) ;
#28365=EDGE_CURVE ( 'NONE', #95805, #103579, #67218, .T. ) ;
#28366=CARTESIAN_POINT ( 'NONE',  ( 9.668542035780198773, 53.51952571152754246, -2.198707408830915533 ) ) ;
#28380=CARTESIAN_POINT ( 'NONE',  ( 4.658253368731117838, 53.64149773577107538, -8.371863789803988709 ) ) ;
#28384=PRESENTATION_STYLE_ASSIGNMENT (( #75827 ) ) ;
#28391=CARTESIAN_POINT ( 'NONE',  ( 16.75187969033571989, -1.200000000000000030E-05, 21.80698433968582961 ) ) ;
#28400=( NAMED_UNIT ( * ) PLANE_ANGLE_UNIT ( ) SI_UNIT ( $, .RADIAN. ) );
#28420=CARTESIAN_POINT ( 'NONE',  ( -5.290067270632216712, -1.200000000000000030E-05, 6.031152949374556371 ) ) ;
#28426=ORIENTED_EDGE ( 'NONE', *, *, #33349, .F. ) ;
#28434=CARTESIAN_POINT ( 'NONE',  ( 28.52985215182756917, 11.34625443571974657, -41.35275482200174224 ) ) ;
#28439=CONICAL_SURFACE ( 'NONE', #85214, 0.6840402866513453084, 1.221730476396026610 ) ;
#28440=EDGE_LOOP ( 'NONE', ( #63581, #4830 ) ) ;
#28459=( NAMED_UNIT ( * ) SI_UNIT ( $, .STERADIAN. ) SOLID_ANGLE_UNIT ( ) );
#28485=VERTEX_POINT ( 'NONE', #295 ) ;
#28503=ORIENTED_EDGE ( 'NONE', *, *, #88138, .F. ) ;
#28504=( GEOMETRIC_REPRESENTATION_CONTEXT ( 3 ) GLOBAL_UNCERTAINTY_ASSIGNED_CONTEXT ( ( #77428 ) ) GLOBAL_UNIT_ASSIGNED_CONTEXT ( ( #89013, #55550, #54487 ) ) REPRESENTATION_CONTEXT ( 'NONE', 'WORKASPACE' ) );
#28521=CARTESIAN_POINT ( 'NONE',  ( -1.411247199636991373E-12, 7.746009256445978153, -51.75000000000450484 ) ) ;
#28524=CARTESIAN_POINT ( 'NONE',  ( 17.39344025253047477, 36.29830519803331867, 24.14278306258518469 ) ) ;
#28534=DIRECTION ( 'NONE',  ( 0.000000000000000000, -0.000000000000000000, 1.000000000000000000 ) ) ;
#28554=CARTESIAN_POINT ( 'NONE',  ( -24.00296863125211644, 25.16459671810052257, -32.94325037771057652 ) ) ;
#28571=ORIENTED_EDGE ( 'NONE', *, *, #72519, .F. ) ;
#28612=ORIENTED_EDGE ( 'NONE', *, *, #86341, .F. ) ;
#28638=FACE_OUTER_BOUND ( 'NONE', #40179, .T. ) ;
#28650=ORIENTED_EDGE ( 'NONE', *, *, #103942, .F. ) ;
#28653=CARTESIAN_POINT ( 'NONE',  ( -5.290067270632216712, 51.34639538792298907, 8.531152949374556371 ) ) ;
#28666=CARTESIAN_POINT ( 'NONE',  ( -9.443162145033490162, 44.08363004829780607, -13.23108312906848560 ) ) ;
#28679=CARTESIAN_POINT ( 'NONE',  ( -49.24240974153273243, 8.191948471291029321, -15.29453271768056766 ) ) ;
#28714=CARTESIAN_POINT ( 'NONE',  ( 16.75187969033571989, 34.25544727262119693, 24.30698433968583316 ) ) ;
#28718=CARTESIAN_POINT ( 'NONE',  ( 1.235988652327632664, 15.32448820071590134, 50.72415524448811652 ) ) ;
#28744=DIRECTION ( 'NONE',  ( 0.000000000000000000, 0.000000000000000000, -1.000000000000000000 ) ) ;
#28749=CARTESIAN_POINT ( 'NONE',  ( -27.42583773761564103, 34.37177070069997598, 10.02613003525735991 ) ) ;
#28751=FACE_OUTER_BOUND ( 'NONE', #82475, .T. ) ;
#28753=CARTESIAN_POINT ( 'NONE',  ( -17.97174518249929420, 36.40624878439880518, 23.34175835912197883 ) ) ;
#28757=AXIS2_PLACEMENT_3D ( 'NONE', #82416, #65166, #91060 ) ;
#28771=SURFACE_STYLE_USAGE ( .BOTH. , #96116 ) ;
#28781=ORIENTED_EDGE ( 'NONE', *, *, #106748, .T. ) ;
#28799=DIRECTION ( 'NONE',  ( -0.000000000000000000, 1.000000000000000000, 0.000000000000000000 ) ) ;
#28875=CARTESIAN_POINT ( 'NONE',  ( 4.152134392769949223, 52.11347441213486320, 6.757182654997005322 ) ) ;
#28888=CARTESIAN_POINT ( 'NONE',  ( -26.48510057655429506, 37.08852406309646454, -7.709608770315281134 ) ) ;
#28898=MECHANICAL_DESIGN_GEOMETRIC_PRESENTATION_REPRESENTATION('',(#39178),#15044);
#28915=CARTESIAN_POINT ( 'NONE',  ( 9.481087872249203130, 53.60657805712472879, -1.932842531519640250 ) ) ;
#28921=AXIS2_PLACEMENT_3D ( 'NONE', #1207, #34176, #98347 ) ;
#28938=CARTESIAN_POINT ( 'NONE',  ( -16.80257523370084272, 45.55115703057131071, -6.650239426131814291 ) ) ;
#28952=CARTESIAN_POINT ( 'NONE',  ( -1.096874481644934729, 51.92397332506016028, -8.379925569044138101 ) ) ;
#28969=VECTOR ( 'NONE', #71403, 1000.000000000000000 ) ;
#28973=CARTESIAN_POINT ( 'NONE',  ( -36.81733651310691613, 25.76199643843586173, -13.21939386992400500 ) ) ;
#28979=ORIENTED_EDGE ( 'NONE', *, *, #61711, .F. ) ;
#28990=CARTESIAN_POINT ( 'NONE',  ( 29.68315524076926337, 8.302504244945327017, -42.10535821593530414 ) ) ;
#28993=CARTESIAN_POINT ( 'NONE',  ( -8.720088082017248610, 51.50350844580864162, 4.031152949374572358 ) ) ;
#29006=MECHANICAL_DESIGN_GEOMETRIC_PRESENTATION_REPRESENTATION('',(#40945),#58185);
#29029=DIRECTION ( 'NONE',  ( 0.000000000000000000, -0.9221233147934838614, -0.3868961001538753219 ) ) ;
#29030=ADVANCED_FACE ( 'NONE', ( #1790, #698, #64950, #9346, #74619 ), #95889, .T. ) ;
#29037=CARTESIAN_POINT ( 'NONE',  ( 1.130211174915330963, 36.55067354015870507, -29.03997593543449796 ) ) ;
#29047=SURFACE_STYLE_FILL_AREA ( #86716 ) ;
#29064=CARTESIAN_POINT ( 'NONE',  ( 0.000000000000000000, 45.89575828009193259, 0.000000000000000000 ) ) ;
#29079=CARTESIAN_POINT ( 'NONE',  ( 16.91815790875667602, 37.08283480489694028, 21.80698433968582961 ) ) ;
#29116=CARTESIAN_POINT ( 'NONE',  ( 16.42257055868354598, 36.46149248629888007, -24.27355254955534036 ) ) ;
#29129=CARTESIAN_POINT ( 'NONE',  ( -38.64320596748726899, 27.44866006653725776, 11.54985041964670067 ) ) ;
#29131=DIRECTION ( 'NONE',  ( 0.000000000000000000, 0.000000000000000000, 1.000000000000000000 ) ) ;
#29145=CARTESIAN_POINT ( 'NONE',  ( -16.09848981374117471, 43.93711403859757780, -4.279955985616452629 ) ) ;
#29149=EDGE_CURVE ( 'NONE', #38179, #45114, #39434, .T. ) ;
#29168=CARTESIAN_POINT ( 'NONE',  ( 0.000000000000000000, 23.58303312036771615, 0.000000000000000000 ) ) ;
#29186=AXIS2_PLACEMENT_3D ( 'NONE', #82831, #34317, #26764 ) ;
#29191=CARTESIAN_POINT ( 'NONE',  ( -17.39344025253030424, 36.29830519803331867, -24.14278306258530193 ) ) ;
#29201=CARTESIAN_POINT ( 'NONE',  ( -30.93190593211504691, 14.41219003788192055, -40.70233947780400996 ) ) ;
#29203=ORIENTED_EDGE ( 'NONE', *, *, #69888, .F. ) ;
#29217=VERTEX_POINT ( 'NONE', #63243 ) ;
#29219=CARTESIAN_POINT ( 'NONE',  ( -0.7709651574482678793, 13.06628101731643810, 49.51182408176356375 ) ) ;
#29223=ORIENTED_EDGE ( 'NONE', *, *, #17884, .F. ) ;
#29225=CARTESIAN_POINT ( 'NONE',  ( -48.59958381656765170, 10.21806572665720658, -14.48686862603874559 ) ) ;
#29240=( LENGTH_UNIT ( ) NAMED_UNIT ( * ) SI_UNIT ( .MILLI., .METRE. ) );
#29253=CARTESIAN_POINT ( 'NONE',  ( -47.14503195514129885, 18.54431490492956769, 14.71570748879569202 ) ) ;
#29255=CARTESIAN_POINT ( 'NONE',  ( 5.290067270632161645, -1.200000000000000030E-05, -7.281152949374595451 ) ) ;
#29256=CARTESIAN_POINT ( 'NONE',  ( 17.72007123370824644, 43.32272278278890809, 4.751713957287425849 ) ) ;
#29271=EDGE_LOOP ( 'NONE', ( #60334, #68463, #105247, #83621 ) ) ;
#29281=MECHANICAL_DESIGN_GEOMETRIC_PRESENTATION_REPRESENTATION('',(#5152),#65426);
#29289=CARTESIAN_POINT ( 'NONE',  ( 17.39562436205969931, 34.16980401269882606, -24.14171231524191086 ) ) ;
#29315=ORIENTED_EDGE ( 'NONE', *, *, #63234, .F. ) ;
#29318=CARTESIAN_POINT ( 'NONE',  ( -23.21751746555168339, 27.38103382803512176, 33.20617127781681432 ) ) ;
#29345=CARTESIAN_POINT ( 'NONE',  ( -49.03408319953958738, 14.13974658789107330, -14.85990013744726923 ) ) ;
#29355=DIRECTION ( 'NONE',  ( -0.000000000000000000, 1.000000000000000000, -0.000000000000000000 ) ) ;
#29356=SURFACE_STYLE_USAGE ( .BOTH. , #102138 ) ;
#29363=CARTESIAN_POINT ( 'NONE',  ( 9.721687949930782224, 46.20860120156268636, -13.03939565591218397 ) ) ;
#29388=CARTESIAN_POINT ( 'NONE',  ( 0.000000000000000000, 32.68727484027578356, 0.000000000000000000 ) ) ;
#29390=CARTESIAN_POINT ( 'NONE',  ( 4.062953383280827779, 52.05749732319144130, 6.990574348803606064 ) ) ;
#29392=CARTESIAN_POINT ( 'NONE',  ( 38.17827875822268879, 27.65674091414286195, 11.10456740074647897 ) ) ;
#29449=CARTESIAN_POINT ( 'NONE',  ( 0.000000000000000000, 25.16329480281783759, 0.000000000000000000 ) ) ;
#29450=CARTESIAN_POINT ( 'NONE',  ( 15.88167336557654430, 44.00174513017344680, 4.402966589011110266 ) ) ;
#29456=EDGE_CURVE ( 'NONE', #32552, #88140, #19966, .T. ) ;
#29470=( LENGTH_UNIT ( ) NAMED_UNIT ( * ) SI_UNIT ( .MILLI., .METRE. ) );
#29476=CARTESIAN_POINT ( 'NONE',  ( 22.88862750579858130, 25.33095312007748134, -33.17288371515036260 ) ) ;
#29544=EDGE_CURVE ( 'NONE', #67639, #53305, #94642, .T. ) ;
#29550=LINE ( 'NONE', #4711, #6077 ) ;
#29564=LINE ( 'NONE', #59925, #59608 ) ;
#29583=CARTESIAN_POINT ( 'NONE',  ( -7.473472438902638793, 52.16903957423301108, 2.156585108680202367 ) ) ;
#29589=CARTESIAN_POINT ( 'NONE',  ( 0.8472790622787957915, 12.94205918040166203, -49.56287671100434267 ) ) ;
#29592=ORIENTED_EDGE ( 'NONE', *, *, #97761, .F. ) ;
#29600=CARTESIAN_POINT ( 'NONE',  ( -10.28624191511820207, -1.200000000000000030E-05, 15.40779740156164124 ) ) ;
#29620=COLOUR_RGB ( '', 0.66274510, 0.83137255, 0.94901961) ;
#29621=DIRECTION ( 'NONE',  ( 0.000000000000000000, 0.000000000000000000, 1.000000000000000000 ) ) ;
#29628=EDGE_LOOP ( 'NONE', ( #79791, #20350 ) ) ;
#29647=CARTESIAN_POINT ( 'NONE',  ( -30.77208753046711820, 10.36816855262254933, 40.23037088889264368 ) ) ;
#29649=EDGE_CURVE ( 'NONE', #25485, #101, #14738, .T. ) ;
#29661=CARTESIAN_POINT ( 'NONE',  ( -16.56380429469772153, 43.78423957885634366, -4.157797401561426298 ) ) ;
#29697=B_SPLINE_CURVE_WITH_KNOTS ( 'NONE', 3,
 ( #89927, #39797, #66180, #99058, #56481, #24688, #97470, #23095, #58079, #47854, #80762, #6876, #82899, #81807, #40840, #81283, #32239, #72673, #105573, #90459 ),
 .UNSPECIFIED., .F., .F.,
 ( 4, 2, 2, 2, 2, 2, 2, 2, 2, 4 ),
 ( 0.005450101279021335281, 0.005953876227450323640, 0.006457651175879311999, 0.006709538650093809647, 0.006961426124308298623, 0.007465201072737251420, 0.007968976021166205084, 0.008472750969595158749, 0.008976525918024112413, 0.009480300866453066078 ),
 .UNSPECIFIED. ) ;
#29699=CYLINDRICAL_SURFACE ( 'NONE', #78813, 63.00000000000000000 ) ;
#29704=CARTESIAN_POINT ( 'NONE',  ( -16.91815790875651260, 37.08283480489694028, -21.80698433968595751 ) ) ;
#29720=LINE ( 'NONE', #19520, #59970 ) ;
#29724=CARTESIAN_POINT ( 'NONE',  ( 37.56673239365870387, -1.200000000000000030E-05, 10.95617127780998956 ) ) ;
#29726=EDGE_CURVE ( 'NONE', #492, #91653, #52923, .T. ) ;
#29733=CARTESIAN_POINT ( 'NONE',  ( -1.117054149123908102, 9.317683682317568383, 51.07842190223516354 ) ) ;
#29749=CARTESIAN_POINT ( 'NONE',  ( -15.73921121718460014, 35.05971934485130959, 22.31943800541765910 ) ) ;
#29789=FACE_BOUND ( 'NONE', #46451, .T. ) ;
#29797=ORIENTED_EDGE ( 'NONE', *, *, #102462, .T. ) ;
#29802=CARTESIAN_POINT ( 'NONE',  ( -27.73690841305016264, 34.52476796560765848, 7.681267181438511393 ) ) ;
#29805=CARTESIAN_POINT ( 'NONE',  ( -17.83130206370017845, 36.70573752982816274, 22.40672895700082634 ) ) ;
#29812=CARTESIAN_POINT ( 'NONE',  ( 16.75187969033515145, 34.25544727262118982, -24.30698433968624883 ) ) ;
#29821=CYLINDRICAL_SURFACE ( 'NONE', #18345, 35.82893434829263413 ) ;
#29836=CARTESIAN_POINT ( 'NONE',  ( -11.27392099353256505, 45.76150927139936897, 13.37519430359083472 ) ) ;
#29838=CARTESIAN_POINT ( 'NONE',  ( 11.04556819181643768, 45.87714785467576917, -13.15211296974108635 ) ) ;
#29840=CARTESIAN_POINT ( 'NONE',  ( 46.83368825528961565, 18.87956456981591202, -15.22947487995093496 ) ) ;
#29845=AXIS2_PLACEMENT_3D ( 'NONE', #546, #15178, #14628 ) ;
#29873=CIRCLE ( 'NONE', #50446, 63.00000000000000000 ) ;
#29885=ORIENTED_EDGE ( 'NONE', *, *, #61904, .F. ) ;
#29889=FACE_OUTER_BOUND ( 'NONE', #94389, .T. ) ;
#29896=DIRECTION ( 'NONE',  ( -0.000000000000000000, 1.000000000000000000, -0.000000000000000000 ) ) ;
#29902=CARTESIAN_POINT ( 'NONE',  ( -36.31365659032788074, 26.07273513814342181, 12.06405704682174651 ) ) ;
#29919=CARTESIAN_POINT ( 'NONE',  ( -25.85382071165692253, 37.19470222756634570, -8.744493950090857837 ) ) ;
#29950=EDGE_CURVE ( 'NONE', #74421, #4914, #59866, .T. ) ;
#29960=VERTEX_POINT ( 'NONE', #79687 ) ;
#29969=ADVANCED_FACE ( 'NONE', ( #55398 ), #38719, .F. ) ;
#29974=CARTESIAN_POINT ( 'NONE',  ( 17.88147771104465988, 43.22047798057329260, -5.216096487390331049 ) ) ;
#29979=CARTESIAN_POINT ( 'NONE',  ( 24.46206431567186002, 27.53832621860373209, -31.75666539158959623 ) ) ;
#29981=UNCERTAINTY_MEASURE_WITH_UNIT (LENGTH_MEASURE( 1.000000000000000082E-05 ), #67456, 'distance_accuracy_value', 'NONE');
#29983=PRESENTATION_STYLE_ASSIGNMENT (( #37560 ) ) ;
#29988=ORIENTED_EDGE ( 'NONE', *, *, #61904, .T. ) ;
#29989=EDGE_CURVE ( 'NONE', #32781, #34804, #88127, .T. ) ;
#30005=( LENGTH_UNIT ( ) NAMED_UNIT ( * ) SI_UNIT ( .MILLI., .METRE. ) );
#30010=CARTESIAN_POINT ( 'NONE',  ( 29.77450884433743639, 8.177050405881830741, 42.10535821593491335 ) ) ;
#30025=ORIENTED_EDGE ( 'NONE', *, *, #29456, .F. ) ;
#30043=STYLED_ITEM ( 'NONE', ( #42690 ), #62053 ) ;
#30047=CARTESIAN_POINT ( 'NONE',  ( 9.645652298885325493, 44.08758678901953942, 13.07143836443655616 ) ) ;
#30072=EDGE_CURVE ( 'NONE', #35442, #69405, #571, .T. ) ;
#30077=LINE ( 'NONE', #52324, #40641 ) ;
#30103=CARTESIAN_POINT ( 'NONE',  ( 17.97938082339186749, 36.40366709787542732, 23.34517568653148345 ) ) ;
#30114=CIRCLE ( 'NONE', #16301, 35.82893434829263413 ) ;
#30160=CARTESIAN_POINT ( 'NONE',  ( 29.33008799483377871, 13.53038725678830367, 39.65490270819991281 ) ) ;
#30169=CARTESIAN_POINT ( 'NONE',  ( 48.02835407290503866, 11.61227450977245468, -14.35535821593549954 ) ) ;
#30185=CARTESIAN_POINT ( 'NONE',  ( 29.77394335381455903, 8.177826981235266857, -42.10535821593531125 ) ) ;
#30187=STYLED_ITEM ( 'NONE', ( #65734 ), #88186 ) ;
#30192=PRESENTATION_STYLE_ASSIGNMENT (( #23701 ) ) ;
#30232=CARTESIAN_POINT ( 'NONE',  ( 1.152188841818234133E-13, -1.200000000000000030E-05, 51.75000000000000711 ) ) ;
#30278=( GEOMETRIC_REPRESENTATION_CONTEXT ( 3 ) GLOBAL_UNCERTAINTY_ASSIGNED_CONTEXT ( ( #23744 ) ) GLOBAL_UNIT_ASSIGNED_CONTEXT ( ( #26669, #57921, #75709 ) ) REPRESENTATION_CONTEXT ( 'NONE', 'WORKASPACE' ) );
#30279=CARTESIAN_POINT ( 'NONE',  ( 30.42537733501877639, 12.90981014178660757, -41.86413436173263136 ) ) ;
#30281=( NAMED_UNIT ( * ) SI_UNIT ( $, .STERADIAN. ) SOLID_ANGLE_UNIT ( ) );
#30288=CARTESIAN_POINT ( 'NONE',  ( 17.73840306501246289, 34.63647015383776306, 22.27315226561848149 ) ) ;
#30317=CARTESIAN_POINT ( 'NONE',  ( -28.29505784598654472, 34.17090463856185067, 9.198890806811057530 ) ) ;
#30319=CARTESIAN_POINT ( 'NONE',  ( -23.21751746555280249, -1.200000000000000030E-05, -31.95617127781034839 ) ) ;
#30333=FACE_OUTER_BOUND ( 'NONE', #42172, .T. ) ;
#30355=CARTESIAN_POINT ( 'NONE',  ( -11.39656771499227084, 45.34267223356314958, 14.75529722941189625 ) ) ;
#30370=EDGE_CURVE ( 'NONE', #9249, #29960, #50841, .T. ) ;
#30377=EDGE_LOOP ( 'NONE', ( #48508, #71765, #44248, #15886 ) ) ;
#30384=CARTESIAN_POINT ( 'NONE',  ( 16.75187969033571989, 37.11970326878314097, 21.80698433968582961 ) ) ;
#30388=CARTESIAN_POINT ( 'NONE',  ( -49.18580537133279762, 13.60959006579542674, -15.12486994001303486 ) ) ;
#30395=VECTOR ( 'NONE', #17887, 1000.000000000000000 ) ;
#30396=DIRECTION ( 'NONE',  ( -0.000000000000000000, -1.000000000000000000, -0.000000000000000000 ) ) ;
#30397=FACE_BOUND ( 'NONE', #51167, .T. ) ;
#30411=ORIENTED_EDGE ( 'NONE', *, *, #34009, .T. ) ;
#30413=CARTESIAN_POINT ( 'NONE',  ( -38.65357358930379661, 27.30496217644010315, -12.82931495569635238 ) ) ;
#30418=CARTESIAN_POINT ( 'NONE',  ( 11.29905645152050475, 45.32368457861270628, 14.89516444794118222 ) ) ;
#30422=B_SPLINE_CURVE_WITH_KNOTS ( 'NONE', 3,
 ( #103499, #21546, #104551, #78155, #20523, #79218, #70605, #29647, #30702, #53357, #94896, #4275, #12878, #53874, #63590, #45795, #71125, #78674, #88388, #5344, #95406, #46847, #87327, #102972, #69548, #94360, #5852, #37203 ),
 .UNSPECIFIED., .F., .F.,
 ( 4, 2, 2, 2, 2, 2, 2, 2, 2, 2, 2, 2, 2, 4 ),
 ( 0.007813944516173620958, 0.008738276158831484106, 0.009662607801489347253, 0.01058693944414721040, 0.01151127108680507355, 0.01243560272946293843, 0.01289776855079186914, 0.01335993437212079984, 0.01382210019344973229, 0.01405318310411419851, 0.01428426601477866473, 0.01451534892544312921, 0.01474643183610759717, 0.01520859765743652441 ),
 .UNSPECIFIED. ) ;
#30436=CARTESIAN_POINT ( 'NONE',  ( 0.08432500865644583510, 52.17923068443688095, -7.750000000000010658 ) ) ;
#30442=CARTESIAN_POINT ( 'NONE',  ( 11.50595937734579799, 43.27894158476472342, 14.44327389318907073 ) ) ;
#30450=CARTESIAN_POINT ( 'NONE',  ( -27.10511071441192144, 36.60571256639527604, -10.05698433968589178 ) ) ;
#30479=PRODUCT_DEFINITION ( 'UNKNOWN', '', #73150, #10041 ) ;
#30496=CARTESIAN_POINT ( 'NONE',  ( 26.94613286657595097, 36.94238815830848210, 7.556984339685560492 ) ) ;
#30497=FILL_AREA_STYLE_COLOUR ( '', #59375 ) ;
#30498=CARTESIAN_POINT ( 'NONE',  ( 16.80185279643511720, 43.70018028759842110, -4.157797401561335704 ) ) ;
#30506=CARTESIAN_POINT ( 'NONE',  ( -24.17834536076760443, 25.18046967552916371, 32.76024643191446017 ) ) ;
#30513=CARTESIAN_POINT ( 'NONE',  ( 1.221257515003810079, 51.58212317033902394, 9.311104479422620983 ) ) ;
#30517=CARTESIAN_POINT ( 'NONE',  ( -0.6461142731108306947, 51.32298069254813555, -10.08306419293876743 ) ) ;
#30519=CARTESIAN_POINT ( 'NONE',  ( 0.07752439927408807940, 18.87382441218277407, -49.25000000000001421 ) ) ;
#30526=EDGE_CURVE ( 'NONE', #68049, #35444, #57151, .T. ) ;
#30527=CARTESIAN_POINT ( 'NONE',  ( -8.559508646656370345, 53.96349637827587031, 1.531152949374564365 ) ) ;
#30556=EDGE_CURVE ( 'NONE', #88641, #95805, #62350, .T. ) ;
#30561=STYLED_ITEM ( 'NONE', ( #55344 ), #7393 ) ;
#30599=CARTESIAN_POINT ( 'NONE',  ( 26.34328342495543751, 35.00028662264767121, 7.802099556721183049 ) ) ;
#30610=SURFACE_STYLE_USAGE ( .BOTH. , #47807 ) ;
#30613=EDGE_LOOP ( 'NONE', ( #20815, #8319 ) ) ;
#30637=CARTESIAN_POINT ( 'NONE',  ( 1.231118141235101326, 11.28179331793877438, -50.25142030543173632 ) ) ;
#30639=SURFACE_STYLE_FILL_AREA ( #94838 ) ;
#30652=EDGE_CURVE ( 'NONE', #87776, #106068, #76516, .T. ) ;
#30671=MECHANICAL_DESIGN_GEOMETRIC_PRESENTATION_REPRESENTATION('',(#1347),#99523);
#30677=FILL_AREA_STYLE ('',( #5317 ) ) ;
#30679=AXIS2_PLACEMENT_3D ( 'NONE', #100119, #27352, #60230 ) ;
#30683=CARTESIAN_POINT ( 'NONE',  ( -26.78592122648698393, 36.71852912224116494, 10.02587077895928935 ) ) ;
#30688=CARTESIAN_POINT ( 'NONE',  ( 7.944798090354270315, 53.91010666794784356, -3.881035696276761815 ) ) ;
#30696=CARTESIAN_POINT ( 'NONE',  ( -38.31505842747957757, 27.60007494029672159, 11.19190443272380264 ) ) ;
#30702=CARTESIAN_POINT ( 'NONE',  ( -30.82729297445935401, 10.08692072324635269, 40.33672416147543771 ) ) ;
#30715=CARTESIAN_POINT ( 'NONE',  ( -28.32674270491142821, 36.29719069258228359, -9.120579834107232386 ) ) ;
#30746=VERTEX_POINT ( 'NONE', #84086 ) ;
#30768=CARTESIAN_POINT ( 'NONE',  ( -30.36582766586210269, 16.93822630193516332, -39.80117229897623332 ) ) ;
#30780=CARTESIAN_POINT ( 'NONE',  ( 3.643324519380566085E-15, 34.17188553058033307, 29.75000000000000355 ) ) ;
#30788=CARTESIAN_POINT ( 'NONE',  ( -0.5332643207086228410, 8.008635151459630563, 51.63718666259362777 ) ) ;
#30798=CARTESIAN_POINT ( 'NONE',  ( 22.57912246414751678, 28.20550200792851214, 30.87816999938226914 ) ) ;
#30840=CARTESIAN_POINT ( 'NONE',  ( 1.004575945865165298, 25.89076660835915789, 38.75180407462256937 ) ) ;
#30846=CARTESIAN_POINT ( 'NONE',  ( -28.62002530331259109, 18.65065574497671719, -40.19565755993163947 ) ) ;
#30853=B_SPLINE_CURVE_WITH_KNOTS ( 'NONE', 3,
 ( #58442, #51923, #76200, #34729, #84838, #684, #9330, #91350, #10921, #99950, #43841, #33646, #84308, #67069, #68673, #59510, #17464, #50329, #100479, #83236, #26639, #91866 ),
 .UNSPECIFIED., .F., .F.,
 ( 4, 2, 2, 2, 2, 2, 2, 2, 2, 2, 4 ),
 ( 0.002967698420317519022, 0.003472853738152583466, 0.003978009055987647910, 0.004230586714905180783, 0.004483164373822715390, 0.004988319691657781135, 0.005493475009492846881, 0.005746052668410379753, 0.005998630327327913493, 0.006503785645162972300, 0.007008940962998030239 ),
 .UNSPECIFIED. ) ;
#30862=EDGE_CURVE ( 'NONE', #90581, #62158, #62480, .T. ) ;
#30869=CARTESIAN_POINT ( 'NONE',  ( 6.536663219763930499, 53.53350969017542127, -7.404483222291337263 ) ) ;
#30876=EDGE_LOOP ( 'NONE', ( #64713, #51994, #69068, #52341 ) ) ;
#30881=SURFACE_STYLE_FILL_AREA ( #104730 ) ;
#30930=CARTESIAN_POINT ( 'NONE',  ( -48.59987877357447417, 15.38663336896752831, -14.48702310944117322 ) ) ;
#30941=ORIENTED_EDGE ( 'NONE', *, *, #91080, .T. ) ;
#30950=CARTESIAN_POINT ( 'NONE',  ( -29.68315524076956891, -1.200000000000000030E-05, 40.85535821593508388 ) ) ;
#30959=ORIENTED_EDGE ( 'NONE', *, *, #23551, .T. ) ;
#30970=SURFACE_SIDE_STYLE ('',( #56785 ) ) ;
#30976=CARTESIAN_POINT ( 'NONE',  ( 0.5695365293531072792, 51.31240171329326216, -10.11587879637332854 ) ) ;
#30992=CARTESIAN_POINT ( 'NONE',  ( 1.530808498934191324E-16, -1.200000000000000030E-05, -10.24999999999999822 ) ) ;
#31006=ADVANCED_FACE ( 'NONE', ( #105575 ), #58081, .F. ) ;
#31020=CARTESIAN_POINT ( 'NONE',  ( -23.21751746555168339, 27.38103382803512176, 33.20617127781681432 ) ) ;
#31041=CARTESIAN_POINT ( 'NONE',  ( 1.250969861546604722, 34.50283871661307700, 28.81357323150970018 ) ) ;
#31051=CARTESIAN_POINT ( 'NONE',  ( -24.32060867053207076, 25.57659486167563756, 31.28716424263922846 ) ) ;
#31056=B_SPLINE_CURVE_WITH_KNOTS ( 'NONE', 3,
 ( #60438, #53389, #27019, #101923, #60959, #67970, #100327, #10255, #2693, #4299, #93843, #37234, #26490, #35643, #2150, #59363, #92225, #84156, #76049, #43167 ),
 .UNSPECIFIED., .F., .F.,
 ( 4, 2, 2, 2, 2, 2, 2, 2, 2, 4 ),
 ( 0.003111094938513713805, 0.003615343640734996339, 0.004119592342956278005, 0.004623841045177561407, 0.005128089747398843073, 0.005380214098509484774, 0.005632338449620125607, 0.006136587151841411611, 0.006640835854062701084, 0.007145084556283989689 ),
 .UNSPECIFIED. ) ;
#31070=EDGE_CURVE ( 'NONE', #39760, #43850, #12720, .T. ) ;
#31071=CARTESIAN_POINT ( 'NONE',  ( 46.77673112620454532, 13.57592939483829220, -15.58267473267858350 ) ) ;
#31072=EDGE_LOOP ( 'NONE', ( #75949, #88971 ) ) ;
#31082=CARTESIAN_POINT ( 'NONE',  ( 48.02835407290544367, -1.200000000000000030E-05, 16.85535821593427386 ) ) ;
#31095=DIRECTION ( 'NONE',  ( -0.000000000000000000, 1.000000000000000000, 0.000000000000000000 ) ) ;
#31098=LINE ( 'NONE', #81182, #10215 ) ;
#31111=ORIENTED_EDGE ( 'NONE', *, *, #106328, .T. ) ;
#31119=STYLED_ITEM ( 'NONE', ( #89050 ), #91858 ) ;
#31120=CARTESIAN_POINT ( 'NONE',  ( -0.4140831102887818638, 26.05273726750685981, -38.31762812124991058 ) ) ;
#31133=EDGE_CURVE ( 'NONE', #89868, #30746, #46171, .T. ) ;
#31138=CARTESIAN_POINT ( 'NONE',  ( 25.85214958460326429, 35.07651433957570930, 8.662971501749767711 ) ) ;
#31144=CARTESIAN_POINT ( 'NONE',  ( -0.8386384795610041243, 54.17551965392264179, -8.069541871738774574 ) ) ;
#31160=DIRECTION ( 'NONE',  ( -0.000000000000000000, 1.000000000000000000, 0.000000000000000000 ) ) ;
#31167=CARTESIAN_POINT ( 'NONE',  ( 0.1687358743861622490, 25.16821295365203071, -40.75000000000001421 ) ) ;
#31168=AXIS2_PLACEMENT_3D ( 'NONE', #73277, #24249, #98098 ) ;
#31172=CARTESIAN_POINT ( 'NONE',  ( 29.68315524077034340, 18.29184282782460969, 39.60535821593451544 ) ) ;
#31173=EDGE_CURVE ( 'NONE', #95054, #92720, #21916, .T. ) ;
#31179=CARTESIAN_POINT ( 'NONE',  ( -0.6188199107750348427, 18.48321454451371082, 49.41007108123974945 ) ) ;
#31192=CARTESIAN_POINT ( 'NONE',  ( -0.8413420114633378688, 36.41305800915415603, 29.42807188061774681 ) ) ;
#31195=VERTEX_POINT ( 'NONE', #39150 ) ;
#31197=CARTESIAN_POINT ( 'NONE',  ( -27.42501128590891568, 36.50037190240711737, 10.02642919151490553 ) ) ;
#31228=FACE_OUTER_BOUND ( 'NONE', #27547, .T. ) ;
#31237=CARTESIAN_POINT ( 'NONE',  ( 29.09375146990877070, 9.378808818926399837, 41.96648843557815667 ) ) ;
#31248=CARTESIAN_POINT ( 'NONE',  ( -28.30696098233519820, 36.37587947255391896, -8.453513908488865525 ) ) ;
#31264=CARTESIAN_POINT ( 'NONE',  ( 11.54066681168268715, 43.31748179290343614, -14.27987094040936178 ) ) ;
#31270=DIRECTION ( 'NONE',  ( -0.000000000000000000, 1.000000000000000000, -0.000000000000000000 ) ) ;
#31280=SURFACE_STYLE_FILL_AREA ( #95994 ) ;
#31287=LINE ( 'NONE', #65212, #22086 ) ;
#31289=CARTESIAN_POINT ( 'NONE',  ( 1.219859450172373405, 27.85995443672884875, -39.18316543001691343 ) ) ;
#31298=CARTESIAN_POINT ( 'NONE',  ( -0.1689405702170302670, 52.17923068443690937, 7.749999999999985789 ) ) ;
#31305=CIRCLE ( 'NONE', #12324, 22.55262289886175964 ) ;
#31313=CARTESIAN_POINT ( 'NONE',  ( 4.181459352178379163, 52.13185942279471874, -6.680504396420412050 ) ) ;
#31315=CARTESIAN_POINT ( 'NONE',  ( -0.1697973226534593427, 35.07848417048374046, 27.25873575795114334 ) ) ;
#31316=LINE ( 'NONE', #29724, #62089 ) ;
#31317=B_SPLINE_CURVE_WITH_KNOTS ( 'NONE', 3,
 ( #91913, #24557, #75181, #8330, #59026, #82757, #90859, #74120, #25079, #50903, #32647, #18044, #16975, #56872, #9923, #74649, #42831, #32102, #48777, #25631 ),
 .UNSPECIFIED., .F., .F.,
 ( 4, 2, 2, 2, 2, 2, 2, 2, 2, 4 ),
 ( 0.0009508909574247033456, 0.001455760884198638739, 0.001960630810972573915, 0.002465500737746509526, 0.002970370664520444702, 0.003475240591294379879, 0.003980110518068315055, 0.004232545481455281776, 0.004484980444842248497, 0.004989850371616175000 ),
 .UNSPECIFIED. ) ;
#31321=CARTESIAN_POINT ( 'NONE',  ( -0.1553312384537495483, 13.68574913102198742, 49.25766246113545321 ) ) ;
#31334=DIRECTION ( 'NONE',  ( 0.000000000000000000, 0.000000000000000000, 1.000000000000000000 ) ) ;
#31361=CARTESIAN_POINT ( 'NONE',  ( 36.35715703853927039, 28.12785541995608085, 12.56221659471220242 ) ) ;
#31363=CARTESIAN_POINT ( 'NONE',  ( 0.000000000000000000, 47.29617335651134624, 0.000000000000000000 ) ) ;
#31368=( NAMED_UNIT ( * ) SI_UNIT ( $, .STERADIAN. ) SOLID_ANGLE_UNIT ( ) );
#31369=CARTESIAN_POINT ( 'NONE',  ( -28.53023071193248583, 11.34323491540338580, -41.35403323942997389 ) ) ;
#31372=CARTESIAN_POINT ( 'NONE',  ( 37.56673239365841255, 27.60449318992554169, -13.45617127781092215 ) ) ;
#31373=CARTESIAN_POINT ( 'NONE',  ( 0.9531491022388255407, 25.91474801773795633, 38.68721158006705707 ) ) ;
#31379=VERTEX_POINT ( 'NONE', #99825 ) ;
#31380=STYLED_ITEM ( 'NONE', ( #96072 ), #82778 ) ;
#31383=STYLED_ITEM ( 'NONE', ( #41148 ), #51627 ) ;
#31393=EDGE_CURVE ( 'NONE', #5108, #66410, #95765, .T. ) ;
#31397=FILL_AREA_STYLE_COLOUR ( '', #23814 ) ;
#31411=FACE_BOUND ( 'NONE', #101169, .T. ) ;
#31432=CARTESIAN_POINT ( 'NONE',  ( 11.50618969897577948, 45.40753567543398361, -14.44225189481717031 ) ) ;
#31441=EDGE_CURVE ( 'NONE', #62805, #54759, #82755, .T. ) ;
#31458=CARTESIAN_POINT ( 'NONE',  ( -49.25998992636563401, 12.93544608831240161, -15.83190612885685589 ) ) ;
#31474=CARTESIAN_POINT ( 'NONE',  ( -22.11477862515238968, 27.78277355752724631, -32.62539941293130852 ) ) ;
#31491=LINE ( 'NONE', #49216, #41665 ) ;
#31499=ORIENTED_EDGE ( 'NONE', *, *, #18949, .F. ) ;
#31505=DIRECTION ( 'NONE',  ( 0.000000000000000000, -0.3420201433256725987, -0.9396926207859068736 ) ) ;
#31507=CARTESIAN_POINT ( 'NONE',  ( 38.18741658151765250, 27.41008188141410074, 13.30318076387803572 ) ) ;
#31522=CARTESIAN_POINT ( 'NONE',  ( -5.616399669216317392, 54.12011764772116607, 6.063970369565759633 ) ) ;
#31551=CARTESIAN_POINT ( 'NONE',  ( 28.31477239889190756, 34.24506016859675128, 8.451634719143738650 ) ) ;
#31554=ORIENTED_EDGE ( 'NONE', *, *, #2378, .T. ) ;
#31562=FILL_AREA_STYLE_COLOUR ( '', #67012 ) ;
#31563=CARTESIAN_POINT ( 'NONE',  ( 3.337162542380456721E-15, 35.08181111624585213, 27.25000000000000000 ) ) ;
#31565=SURFACE_STYLE_FILL_AREA ( #80601 ) ;
#31576=CARTESIAN_POINT ( 'NONE',  ( -0.7866107806117342838, 43.26603872651622851, -18.48505893840705383 ) ) ;
#31601=CARTESIAN_POINT ( 'NONE',  ( 30.00061906993038363, 12.59382690271831251, 39.64398720750875071 ) ) ;
#31616=CARTESIAN_POINT ( 'NONE',  ( 47.36618468514978986, 18.16301677597534336, 14.54218830158920639 ) ) ;
#31621=( LENGTH_UNIT ( ) NAMED_UNIT ( * ) SI_UNIT ( .MILLI., .METRE. ) );
#31634=COLOUR_RGB ( '', 0.31764706, 0.68627451, 0.89019608) ;
#31637=CARTESIAN_POINT ( 'NONE',  ( -1.131308492565942458, 25.42167126197779936, -40.03766171172649280 ) ) ;
#31664=CARTESIAN_POINT ( 'NONE',  ( -0.6401524832913686458, 54.23522517489366379, -7.923242704504276368 ) ) ;
#31675=EDGE_LOOP ( 'NONE', ( #81009, #79863 ) ) ;
#31684=CARTESIAN_POINT ( 'NONE',  ( 0.5680201850460122603, 26.02808649538077646, -38.38338999498244419 ) ) ;
#31689=CARTESIAN_POINT ( 'NONE',  ( 1.097844465543542425, 54.05176034408437857, -8.381373465022610603 ) ) ;
#31738=CARTESIAN_POINT ( 'NONE',  ( 8.238701406685740025, 53.79503307339000173, -3.999633084520308302 ) ) ;
#31763=DIRECTION ( 'NONE',  ( 0.000000000000000000, 0.000000000000000000, 1.000000000000000000 ) ) ;
#31786=CARTESIAN_POINT ( 'NONE',  ( -46.83547786243088495, 13.71028427728498045, 15.22387951581991672 ) ) ;
#31815=CARTESIAN_POINT ( 'NONE',  ( -16.75187969033554936, 34.99134772383131065, -21.80698433968595751 ) ) ;
#31826=CARTESIAN_POINT ( 'NONE',  ( -28.43950163419759747, 12.73412882672193724, 40.70661530191370758 ) ) ;
#31839=DIRECTION ( 'NONE',  ( 0.000000000000000000, 0.000000000000000000, 1.000000000000000000 ) ) ;
#31846=CARTESIAN_POINT ( 'NONE',  ( 22.81472563493030492, 27.48372958372127783, 33.14224123365016794 ) ) ;
#31876=CARTESIAN_POINT ( 'NONE',  ( 25.91508385773364154, 35.08289675578968314, -8.415194575045109815 ) ) ;
#31889=CARTESIAN_POINT ( 'NONE',  ( -28.71549002648981030, 15.67055689680110753, -41.65541077617267973 ) ) ;
#31891=( LENGTH_UNIT ( ) NAMED_UNIT ( * ) SI_UNIT ( .MILLI., .METRE. ) );
#31894=ORIENTED_EDGE ( 'NONE', *, *, #77233, .T. ) ;
#31923=FACE_BOUND ( 'NONE', #28440, .T. ) ;
#31924=ADVANCED_FACE ( 'NONE', ( #98383 ), #15343, .F. ) ;
#31926=FACE_OUTER_BOUND ( 'NONE', #63709, .T. ) ;
#31930=LINE ( 'NONE', #48074, #76109 ) ;
#31944=CARTESIAN_POINT ( 'NONE',  ( 10.36871714652611054, 45.36883139708660906, -15.40779740156172295 ) ) ;
#31955=DIRECTION ( 'NONE',  ( 0.000000000000000000, 0.000000000000000000, 1.000000000000000000 ) ) ;
#31956=DIRECTION ( 'NONE',  ( 0.000000000000000000, 1.000000000000000000, -0.000000000000000000 ) ) ;
#31959=B_SPLINE_CURVE_WITH_KNOTS ( 'NONE', 3,
 ( #56757, #97749, #105331, #81549, #98810, #89684, #40063, #41655, #8218, #50272, #98294, #17397, #33581, #7671, #23916, #16860, #31474, #40590, #15782, #89150, #93, #48664, #73471, #90743, #57820, #97225 ),
 .UNSPECIFIED., .F., .F.,
 ( 4, 2, 2, 2, 2, 2, 2, 2, 2, 2, 2, 2, 4 ),
 ( 0.003090214743966922337, 0.003342416748342341183, 0.003594618752717760463, 0.003846820757093179308, 0.004099022761468598154, 0.004603426770219428907, 0.004855628774594835176, 0.005107830778970241445, 0.006116638796471930706, 0.006368840800847349118, 0.006621042805222767530, 0.006873244809598185075, 0.007125446813973602619 ),
 .UNSPECIFIED. ) ;
#31976=CIRCLE ( 'NONE', #50871, 56.32976553137783782 ) ;
#31982=CARTESIAN_POINT ( 'NONE',  ( 0.000000000000000000, 56.87938524157181774, 0.000000000000000000 ) ) ;
#31995=DIRECTION ( 'NONE',  ( 0.000000000000000000, 1.000000000000000000, -0.000000000000000000 ) ) ;
#32013=( NAMED_UNIT ( * ) SI_UNIT ( $, .STERADIAN. ) SOLID_ANGLE_UNIT ( ) );
#32040=CARTESIAN_POINT ( 'NONE',  ( -9.500789678090530543, 51.30116685821661804, -3.607819160377707668 ) ) ;
#32042=CARTESIAN_POINT ( 'NONE',  ( -6.536694770564420942, 53.53355194758169233, 7.404301873595124484 ) ) ;
#32051=EDGE_LOOP ( 'NONE', ( #86513, #63721, #18805, #13066 ) ) ;
#32066=CARTESIAN_POINT ( 'NONE',  ( -22.88839214066252836, 27.45938914059933467, 33.17277703389353860 ) ) ;
#32085=( NAMED_UNIT ( * ) SI_UNIT ( $, .STERADIAN. ) SOLID_ANGLE_UNIT ( ) );
#32090=CARTESIAN_POINT ( 'NONE',  ( 23.21751746555220564, 28.11705169068991950, -30.70617127781077116 ) ) ;
#32097=CARTESIAN_POINT ( 'NONE',  ( 0.4142090692292615395, 46.18735664537236829, 16.31767936258320262 ) ) ;
#32102=CARTESIAN_POINT ( 'NONE',  ( -9.953549941019272040, 46.18635266956800223, 12.94124874758487742 ) ) ;
#32109=ORIENTED_EDGE ( 'NONE', *, *, #90040, .F. ) ;
#32119=CARTESIAN_POINT ( 'NONE',  ( 30.06815944328944923, 12.45816842452745021, 39.66421731453360877 ) ) ;
#32131=CIRCLE ( 'NONE', #66519, 45.10524579772351217 ) ;
#32158=CARTESIAN_POINT ( 'NONE',  ( -9.686158086385539434, 53.40057947480783440, 3.329218293922611593 ) ) ;
#32176=CARTESIAN_POINT ( 'NONE',  ( -30.10565283232759981, 7.858405490276831884, -42.03377155531590148 ) ) ;
#32187=( GEOMETRIC_REPRESENTATION_CONTEXT ( 3 ) GLOBAL_UNCERTAINTY_ASSIGNED_CONTEXT ( ( #68839 ) ) GLOBAL_UNIT_ASSIGNED_CONTEXT ( ( #61167, #70842, #93534 ) ) REPRESENTATION_CONTEXT ( 'NONE', 'WORKASPACE' ) );
#32193=CYLINDRICAL_SURFACE ( 'NONE', #14852, 1.250000000000001110 ) ;
#32209=CARTESIAN_POINT ( 'NONE',  ( -1.484885661199817548E-13, 25.16821295365152622, -40.75000000000150635 ) ) ;
#32215=CARTESIAN_POINT ( 'NONE',  ( -1.250481436861478945, 34.56029847975127467, -28.65557344373550563 ) ) ;
#32219=DIRECTION ( 'NONE',  ( -0.000000000000000000, 1.000000000000000000, -0.000000000000000000 ) ) ;
#32221=PRESENTATION_STYLE_ASSIGNMENT (( #103959 ) ) ;
#32225=CARTESIAN_POINT ( 'NONE',  ( -16.58646281676584522, 37.15392203743714816, -21.81520449073906320 ) ) ;
#32239=CARTESIAN_POINT ( 'NONE',  ( 22.59000000144133935, 25.42954125889399819, 33.04937649237353980 ) ) ;
#32274=STYLED_ITEM ( 'NONE', ( #101421 ), #3855 ) ;
#32286=DIRECTION ( 'NONE',  ( -0.000000000000000000, 1.000000000000000000, -0.000000000000000000 ) ) ;
#32289=CARTESIAN_POINT ( 'NONE',  ( 28.49053509030336073, 18.29756676117402492, 40.46890581211940940 ) ) ;
#32312=EDGE_CURVE ( 'NONE', #20227, #95973, #9924, .T. ) ;
#32325=CARTESIAN_POINT ( 'NONE',  ( -47.50581258546153407, 12.72782412601323720, 14.46700746232338908 ) ) ;
#32335=( NAMED_UNIT ( * ) SI_UNIT ( $, .STERADIAN. ) SOLID_ANGLE_UNIT ( ) );
#32344=CARTESIAN_POINT ( 'NONE',  ( -0.1695571859891748800, 26.07487066857262192, 38.25869140465272267 ) ) ;
#32357=CARTESIAN_POINT ( 'NONE',  ( -17.73845910361362499, 34.63644398513737599, -22.27319956676174684 ) ) ;
#32365=CARTESIAN_POINT ( 'NONE',  ( -29.09616027395263416, 9.373446874598341694, 41.96755440745693022 ) ) ;
#32366=DIRECTION ( 'NONE',  ( -0.000000000000000000, 1.000000000000000000, -0.000000000000000000 ) ) ;
#32368=ORIENTED_EDGE ( 'NONE', *, *, #100828, .F. ) ;
#32374=EDGE_LOOP ( 'NONE', ( #87481, #52563 ) ) ;
#32381=CARTESIAN_POINT ( 'NONE',  ( -37.40757794985528761, 25.81202373761992774, -10.96376234217055234 ) ) ;
#32415=CARTESIAN_POINT ( 'NONE',  ( 27.10511071441176867, 34.75829513984540142, -7.556984339686343866 ) ) ;
#32418=CYLINDRICAL_SURFACE ( 'NONE', #90476, 1.249999999999999334 ) ;
#32430=CARTESIAN_POINT ( 'NONE',  ( -29.49550841906124887, 18.54274624009277161, -39.61427208276962375 ) ) ;
#32450=CARTESIAN_POINT ( 'NONE',  ( 28.46824965450711531, 18.16842165451063451, -40.55076743663480698 ) ) ;
#32462=ORIENTED_EDGE ( 'NONE', *, *, #49598, .T. ) ;
#32464=EDGE_CURVE ( 'NONE', #86888, #34804, #104092, .T. ) ;
#32475=EDGE_LOOP ( 'NONE', ( #93267, #97753, #80177, #93812 ) ) ;
#32488=CARTESIAN_POINT ( 'NONE',  ( -48.02835407290516656, 9.771516447483513446, 16.85535821593516559 ) ) ;
#32503=FACE_OUTER_BOUND ( 'NONE', #71603, .T. ) ;
#32515=CARTESIAN_POINT ( 'NONE',  ( 0.8398752165421072835, 43.96108724165920734, -16.57059267381174550 ) ) ;
#32518=CARTESIAN_POINT ( 'NONE',  ( 17.40604945778712676, 45.37707562542234996, 6.412274061844262185 ) ) ;
#32521=( NAMED_UNIT ( * ) SI_UNIT ( $, .STERADIAN. ) SOLID_ANGLE_UNIT ( ) );
#32552=VERTEX_POINT ( 'NONE', #87927 ) ;
#32566=CARTESIAN_POINT ( 'NONE',  ( 48.48458519718480630, 8.810627846918919204, 16.77132102101048616 ) ) ;
#32597=STYLED_ITEM ( 'NONE', ( #4183 ), #45279 ) ;
#32613=CARTESIAN_POINT ( 'NONE',  ( 27.86692020406142589, 34.24704128939396952, 9.812054281695964164 ) ) ;
#32624=CARTESIAN_POINT ( 'NONE',  ( -17.25516560787559683, 45.65538004793684479, -4.306155947794052530 ) ) ;
#32635=ORIENTED_EDGE ( 'NONE', *, *, #82466, .F. ) ;
#32637=CARTESIAN_POINT ( 'NONE',  ( 1.103059070678794606, 51.47956408706726705, 9.609521617059924026 ) ) ;
#32642=CARTESIAN_POINT ( 'NONE',  ( 0.5675612687379431032, 46.16185839072779373, 16.38316274734319222 ) ) ;
#32647=CARTESIAN_POINT ( 'NONE',  ( -9.058657501722457539, 46.09928351899775123, 13.86902144048102059 ) ) ;
#32650=CARTESIAN_POINT ( 'NONE',  ( 46.79755470960057551, 13.68519846643611260, -15.37381431200700810 ) ) ;
#32658=CARTESIAN_POINT ( 'NONE',  ( -27.10511071441183262, -1.200000000000000030E-05, 7.556984339686156460 ) ) ;
#32664=PRESENTATION_STYLE_ASSIGNMENT (( #26184 ) ) ;
#32665=VERTEX_POINT ( 'NONE', #40423 ) ;
#32668=CARTESIAN_POINT ( 'NONE',  ( 9.647540759884607908, 51.27675344764688958, -3.402203074467008648 ) ) ;
#32673=FACE_BOUND ( 'NONE', #31072, .T. ) ;
#32682=AXIS2_PLACEMENT_3D ( 'NONE', #10105, #2001, #43016 ) ;
#32721=CARTESIAN_POINT ( 'NONE',  ( 27.10511071441197117, 34.47735702144345282, 10.05698433968570704 ) ) ;
#32728=B_SPLINE_CURVE_WITH_KNOTS ( 'NONE', 3,
 ( #106266, #97129, #32430, #97646, #6517, #22750, #56113, #16209, #55588, #14601, #89584, #5990, #30846, #41025, #49092, #48035, #15150, #32958, #98706, #65827, #38916, #71783, #72329, #31889, #96615, #80942, #89049, #47513, #80404, #39452 ),
 .UNSPECIFIED., .F., .F.,
 ( 4, 2, 2, 2, 2, 2, 2, 2, 2, 2, 2, 2, 2, 2, 4 ),
 ( 0.006732386592399363864, 0.007201418480221516427, 0.007435934424132591841, 0.007670450368043668123, 0.007904966311954744404, 0.008139482255865821553, 0.008373998199776896967, 0.008608514143687972381, 0.009077546031510112801, 0.009546577919332253220, 0.01048464169497652365, 0.01142270547062079582, 0.01236076924626506798, 0.01329883302190933841, 0.01423689679755360885 ),
 .UNSPECIFIED. ) ;
#32745=CARTESIAN_POINT ( 'NONE',  ( 9.443351513663944985, 46.21199249391290920, 13.23092383815001760 ) ) ;
#32746=ORIENTED_EDGE ( 'NONE', *, *, #91786, .T. ) ;
#32751=DIRECTION ( 'NONE',  ( 0.000000000000000000, 1.000000000000000000, 0.000000000000000000 ) ) ;
#32756=CARTESIAN_POINT ( 'NONE',  ( 0.08494585571554005843, 54.30758622938873259, -7.750000000000002665 ) ) ;
#32774=CARTESIAN_POINT ( 'NONE',  ( 0.000000000000000000, 36.79151656018385097, 0.000000000000000000 ) ) ;
#32781=VERTEX_POINT ( 'NONE', #39790 ) ;
#32796=CARTESIAN_POINT ( 'NONE',  ( -27.72576971702810411, 34.28420696235267684, -9.904009874722952134 ) ) ;
#32800=CARTESIAN_POINT ( 'NONE',  ( 0.000000000000000000, -1.200000000000000030E-05, -9.000000000000000000 ) ) ;
#32807=AXIS2_PLACEMENT_3D ( 'NONE', #91315, #17424, #2267 ) ;
#32819=SURFACE_STYLE_USAGE ( .BOTH. , #55454 ) ;
#32828=CARTESIAN_POINT ( 'NONE',  ( -29.14598918812196615, 18.82621124954751224, 39.72463063980541875 ) ) ;
#32831=CARTESIAN_POINT ( 'NONE',  ( -22.22732789360396666, 25.59821783804387607, 32.73558766513509255 ) ) ;
#32849=CARTESIAN_POINT ( 'NONE',  ( 11.53059725919837497, 43.41062336697758184, -13.95763859544337215 ) ) ;
#32874=CARTESIAN_POINT ( 'NONE',  ( 0.6444865106606342264, 28.14418859657819283, -38.41607911672674902 ) ) ;
#32895=CARTESIAN_POINT ( 'NONE',  ( -11.07168871570084079, 43.17206246446114903, -15.14491642044191977 ) ) ;
#32903=CARTESIAN_POINT ( 'NONE',  ( 9.553684976492661463, 51.29138652321832836, 3.543474137435660420 ) ) ;
#32927=CARTESIAN_POINT ( 'NONE',  ( -4.504779885944381057, 54.31184324146714459, 6.294090811699073029 ) ) ;
#32958=CARTESIAN_POINT ( 'NONE',  ( -28.43956359133921552, 17.90386495480483120, -40.70637206596309454 ) ) ;
#32963=CARTESIAN_POINT ( 'NONE',  ( 23.21751746555220564, 28.11705169068991950, -30.70617127781077116 ) ) ;
#32973=EDGE_CURVE ( 'NONE', #91653, #492, #5028, .T. ) ;
#32974=EDGE_CURVE ( 'NONE', #100346, #74421, #90452, .T. ) ;
#32988=VERTEX_POINT ( 'NONE', #13098 ) ;
#32995=COLOUR_RGB ( '', 0.40784314, 0.44705882, 0.49803922) ;
#33024=CARTESIAN_POINT ( 'NONE',  ( -24.46190898409515313, 27.53854914924986730, -31.75601090834104312 ) ) ;
#33025=CARTESIAN_POINT ( 'NONE',  ( -6.400492677076282000, 53.43410452881639827, -7.878742231350887693 ) ) ;
#33028=CARTESIAN_POINT ( 'NONE',  ( 0.000000000000000000, 50.89575828009192549, 0.000000000000000000 ) ) ;
#33045=CARTESIAN_POINT ( 'NONE',  ( -49.28004588020300503, 7.871673175840900427, -15.62336800674829007 ) ) ;
#33078=CARTESIAN_POINT ( 'NONE',  ( -0.1547416878174255328, 12.93287229451991571, -51.74246760002737489 ) ) ;
#33080=DIRECTION ( 'NONE',  ( 0.000000000000000000, 1.000000000000000000, 0.000000000000000000 ) ) ;
#33090=CARTESIAN_POINT ( 'NONE',  ( -7.980179952708205483E-13, 34.17188553057791722, -29.75000000000694911 ) ) ;
#33094=CARTESIAN_POINT ( 'NONE',  ( 7.940845330314040496, 52.04497172380727932, 1.691901466013218780 ) ) ;
#33099=CARTESIAN_POINT ( 'NONE',  ( 0.3336880381504699900, 43.18998736639818503, 18.70756200222306020 ) ) ;
#33112=CARTESIAN_POINT ( 'NONE',  ( 37.40775037356466726, 25.53061312228623692, 13.45617127781006594 ) ) ;
#33130=FACE_OUTER_BOUND ( 'NONE', #25987, .T. ) ;
#33140=EDGE_CURVE ( 'NONE', #79335, #66879, #34427, .T. ) ;
#33160=CARTESIAN_POINT ( 'NONE',  ( -0.9529166959714684415, 13.93637536997674786, 51.31279264900302195 ) ) ;
#33166=CARTESIAN_POINT ( 'NONE',  ( 0.1694652132101762132, 46.21043659876566778, 16.25867386421069938 ) ) ;
#33170=CARTESIAN_POINT ( 'NONE',  ( 22.88520313534120731, 26.05176548070731712, -30.73931513807078986 ) ) ;
#33174=CARTESIAN_POINT ( 'NONE',  ( 46.86248696599233199, 13.70470512780037353, -15.14813956650342419 ) ) ;
#33190=CARTESIAN_POINT ( 'NONE',  ( 30.25697458664275530, 12.04847113665178071, 39.73669343589866543 ) ) ;
#33205=DIRECTION ( 'NONE',  ( -0.000000000000000000, 1.000000000000000000, -0.000000000000000000 ) ) ;
#33226=CARTESIAN_POINT ( 'NONE',  ( -8.875443049772991699, 53.84837620808301750, 1.561318058200789505 ) ) ;
#33233=CARTESIAN_POINT ( 'NONE',  ( 0.1682126576532519957, 45.30391365246044444, -18.75000000000000711 ) ) ;
#33237=CARTESIAN_POINT ( 'NONE',  ( 30.48515219902060736, 12.91670175270528098, 41.81704193310803674 ) ) ;
#33245=CARTESIAN_POINT ( 'NONE',  ( 25.89618882946261991, 35.00184838547495048, 9.164364432303852226 ) ) ;
#33269=CARTESIAN_POINT ( 'NONE',  ( 10.12028333941264080, 45.42143084255511809, 15.39942097377729446 ) ) ;
#33272=B_SPLINE_CURVE_WITH_KNOTS ( 'NONE', 3,
 ( #40828, #51034, #83412, #25766, #9510, #8460, #83947, #90449, #57002, #67250, #49444, #89916, #99590, #81798, #58624, #90994, #33294, #10059, #16560, #75316, #25215, #98004, #1414, #41361, #18173, #17640, #17104, #33835, #74254, #82888 ),
 .UNSPECIFIED., .F., .F.,
 ( 4, 2, 2, 2, 2, 2, 2, 2, 2, 2, 2, 2, 2, 2, 4 ),
 ( 0.004754800762794653829, 0.005690253947496240472, 0.006157980539847035528, 0.006625707132197830584, 0.006859570428373221174, 0.007093433724548612630, 0.007327297020724004087, 0.007561160316899394676, 0.007795023613074785265, 0.008028886909250175855, 0.008496613501600955298, 0.009432066686302517655, 0.01036751987100408001, 0.01130297305570564584, 0.01223842624040720820 ),
 .UNSPECIFIED. ) ;
#33276=ORIENTED_EDGE ( 'NONE', *, *, #30370, .F. ) ;
#33280=CARTESIAN_POINT ( 'NONE',  ( 1.128592495958797404, 53.60018988584262445, -9.630884289430918344 ) ) ;
#33283=ORIENTED_EDGE ( 'NONE', *, *, #71779, .F. ) ;
#33294=CARTESIAN_POINT ( 'NONE',  ( 46.78712017075152829, 13.65728975790556454, 15.44288672244329419 ) ) ;
#33298=CARTESIAN_POINT ( 'NONE',  ( 24.29736616268256100, 25.57611167045289591, -31.30689180755234702 ) ) ;
#33309=VECTOR ( 'NONE', #17129, 1000.000000000000227 ) ;
#33318=DIRECTION ( 'NONE',  ( 0.000000000000000000, -0.3420201433256733758, -0.9396926207859066515 ) ) ;
#33347=FILL_AREA_STYLE_COLOUR ( '', #42395 ) ;
#33349=EDGE_CURVE ( 'NONE', #78599, #45114, #84230, .T. ) ;
#33357=CARTESIAN_POINT ( 'NONE',  ( -29.33036678664092278, 18.69950024370077202, 39.65481841613247838 ) ) ;
#33360=CARTESIAN_POINT ( 'NONE',  ( -22.00819901261985123, 25.77094897315768662, 32.31068855013590735 ) ) ;
#33375=LINE ( 'NONE', #91079, #17296 ) ;
#33376=CARTESIAN_POINT ( 'NONE',  ( 11.04658362184419218, 43.74827273734751998, -13.15312417557731628 ) ) ;
#33383=CARTESIAN_POINT ( 'NONE',  ( -46.77767549600498853, 13.52659353100013995, 15.64517449361655466 ) ) ;
#33387=ORIENTED_EDGE ( 'NONE', *, *, #77992, .T. ) ;
#33392=CARTESIAN_POINT ( 'NONE',  ( 8.880600455183216724, 53.58356968164088840, 4.000111768521608546 ) ) ;
#33397=AXIS2_PLACEMENT_3D ( 'NONE', #89554, #80915, #48007 ) ;
#33401=CARTESIAN_POINT ( 'NONE',  ( -30.64177940627137531, 12.99790429510468570, 41.66010176663436937 ) ) ;
#33410=ORIENTED_EDGE ( 'NONE', *, *, #57348, .F. ) ;
#33414=CARTESIAN_POINT ( 'NONE',  ( -16.80382109351738862, 43.42138402310583700, 6.657797401561657225 ) ) ;
#33417=CARTESIAN_POINT ( 'NONE',  ( -5.855287526011301757, 51.27353136529828959, -8.399225406922926851 ) ) ;
#33424=CARTESIAN_POINT ( 'NONE',  ( -29.14716730816305201, 13.65620768952807751, 39.72410719430370563 ) ) ;
#33431=CARTESIAN_POINT ( 'NONE',  ( 9.797840486031143215, 51.31133413807796728, 2.591606615044619311 ) ) ;
#33434=ORIENTED_EDGE ( 'NONE', *, *, #24853, .T. ) ;
#33453=CARTESIAN_POINT ( 'NONE',  ( -5.290067270632215823, 53.47475093287481229, 8.531152949374556371 ) ) ;
#33455=CARTESIAN_POINT ( 'NONE',  ( -38.66182218138258975, 25.17353944418798761, -12.83206308700384746 ) ) ;
#33458=DIRECTION ( 'NONE',  ( -0.000000000000000000, -1.000000000000000000, -0.000000000000000000 ) ) ;
#33484=CARTESIAN_POINT ( 'NONE',  ( 23.83970809494289611, 25.80407537208032664, 30.86910450433977005 ) ) ;
#33486=CARTESIAN_POINT ( 'NONE',  ( 5.206803358412888549, 53.49072178898849472, 8.531152949374478212 ) ) ;
#33489=B_SPLINE_CURVE_WITH_KNOTS ( 'NONE', 3,
 ( #55007, #70160, #31321, #47454, #104102, #39395, #103064, #29219, #87939, #71724, #94984, #14020, #21123, #78763, #53953, #46415, #13493, #46928, #29733, #71207, #37829, #12961, #30788, #70692, #103581, #95491, #63672, #21635 ),
 .UNSPECIFIED., .F., .F.,
 ( 4, 2, 2, 2, 2, 2, 2, 2, 2, 2, 2, 2, 2, 4 ),
 ( 0.007977619942176784537, 0.008210484177485675994, 0.008443348412794569186, 0.008909076883412357303, 0.009374805354030147156, 0.009840533824647937008, 0.01077199076588351845, 0.01170344770711909989, 0.01263490464835468133, 0.01356636158959026277, 0.01449781853082584421, 0.01496354700144363406, 0.01519641123675252725, 0.01542927547206142044 ),
 .UNSPECIFIED. ) ;
#33522=CARTESIAN_POINT ( 'NONE',  ( -1.249260851835055197, 53.88049993730678722, 8.835555377234499019 ) ) ;
#33550=CARTESIAN_POINT ( 'NONE',  ( -23.21751746555244722, 28.11705169068991594, 30.70617127781060418 ) ) ;
#33560=ORIENTED_EDGE ( 'NONE', *, *, #50545, .T. ) ;
#33564=CARTESIAN_POINT ( 'NONE',  ( 16.34886101041479378, 36.48569306717565297, 24.24298062968059853 ) ) ;
#33567=CARTESIAN_POINT ( 'NONE',  ( -38.19885457863131251, 25.52371017071349613, 11.08075699806225423 ) ) ;
#33581=CARTESIAN_POINT ( 'NONE',  ( -21.99817791066553951, 28.09376123749146714, -31.66916887880079301 ) ) ;
#33589=STYLED_ITEM ( 'NONE', ( #64448 ), #41857 ) ;
#33596=FILL_AREA_STYLE_COLOUR ( '', #18495 ) ;
#33603=EDGE_CURVE ( 'NONE', #54759, #62805, #57467, .T. ) ;
#33617=CARTESIAN_POINT ( 'NONE',  ( 48.15042790184239863, 11.33351092753205513, 14.35535821593427386 ) ) ;
#33619=CARTESIAN_POINT ( 'NONE',  ( 0.4139731306290318491, 44.05904992622305372, 16.31755368115256033 ) ) ;
#33625=FACE_OUTER_BOUND ( 'NONE', #26633, .T. ) ;
#33646=CARTESIAN_POINT ( 'NONE',  ( -15.39039450733990400, 44.07978680685108230, 5.266078492798498267 ) ) ;
#33670=DIRECTION ( 'NONE',  ( 0.000000000000000000, 0.000000000000000000, 1.000000000000000000 ) ) ;
#33675=EDGE_CURVE ( 'NONE', #89428, #69676, #91065, .T. ) ;
#33695=CARTESIAN_POINT ( 'NONE',  ( 0.08412207463451333578, 46.21383923812597772, 16.25000000000000355 ) ) ;
#33697=VERTEX_POINT ( 'NONE', #76523 ) ;
#33699=CARTESIAN_POINT ( 'NONE',  ( -11.42604336269055487, 45.35830052782390709, -14.67759751612683417 ) ) ;
#33703=CARTESIAN_POINT ( 'NONE',  ( -47.90217879170931781, 15.22462055664102465, -16.85535821593460781 ) ) ;
#33705=CARTESIAN_POINT ( 'NONE',  ( -36.58660523126660280, 27.99651712798071657, 12.99820278958899067 ) ) ;
#33717=CARTESIAN_POINT ( 'NONE',  ( -9.959852493538001283, 43.33480949895421475, 15.36720373720356747 ) ) ;
#33720=CARTESIAN_POINT ( 'NONE',  ( 9.635035931158675737, 51.40929392797971786, -2.123426622847617296 ) ) ;
#33721=CARTESIAN_POINT ( 'NONE',  ( 5.612821243144477279, 51.99076548715343193, 6.070840976756991303 ) ) ;
#33735=CARTESIAN_POINT ( 'NONE',  ( 5.912699410789617360, 51.88565102575169874, -6.185454916783826640 ) ) ;
#33745=DIRECTION ( 'NONE',  ( -0.000000000000000000, 1.000000000000000000, -0.000000000000000000 ) ) ;
#33764=DIRECTION ( 'NONE',  ( 0.000000000000000000, 1.000000000000000000, -0.000000000000000000 ) ) ;
#33771=DIRECTION ( 'NONE',  ( 0.000000000000000000, 1.000000000000000000, 0.000000000000000000 ) ) ;
#33774=SURFACE_SIDE_STYLE ('',( #49923 ) ) ;
#33779=CARTESIAN_POINT ( 'NONE',  ( 26.35557460423923359, 34.76314064348615318, 9.820069159921292368 ) ) ;
#33786=CARTESIAN_POINT ( 'NONE',  ( 0.000000000000000000, 0.000000000000000000, 11.27631144943088515 ) ) ;
#33795=ORIENTED_EDGE ( 'NONE', *, *, #38757, .T. ) ;
#33797=FACE_BOUND ( 'NONE', #177, .T. ) ;
#33799=EDGE_LOOP ( 'NONE', ( #73172, #27725 ) ) ;
#33803=CARTESIAN_POINT ( 'NONE',  ( 9.040043340647704539, 46.05340506531722866, 14.03079106125270670 ) ) ;
#33809=ORIENTED_EDGE ( 'NONE', *, *, #99330, .F. ) ;
#33824=CARTESIAN_POINT ( 'NONE',  ( 7.562131307723813478, 54.28093583783773823, 2.009306609246827691 ) ) ;
#33835=CARTESIAN_POINT ( 'NONE',  ( 47.78242936231066551, 10.33916499670818645, 16.83675847388925106 ) ) ;
#33837=CARTESIAN_POINT ( 'NONE',  ( 24.46940115168818508, 25.33847118171375712, -31.99855969730282368 ) ) ;
#33847=CARTESIAN_POINT ( 'NONE',  ( -46.79015243495860688, 13.37233443428283053, -15.81143384442421151 ) ) ;
#33863=CARTESIAN_POINT ( 'NONE',  ( -27.86725909167721937, 34.24694088119783686, -9.811934799320198408 ) ) ;
#33867=CYLINDRICAL_SURFACE ( 'NONE', #81468, 1.250000000000000222 ) ;
#33868=EDGE_LOOP ( 'NONE', ( #25305, #51077 ) ) ;
#33869=PRESENTATION_STYLE_ASSIGNMENT (( #75889 ) ) ;
#33870=CARTESIAN_POINT ( 'NONE',  ( 4.684273348644264514E-15, 28.20649408426940141, 38.25000000000000000 ) ) ;
#33884=CARTESIAN_POINT ( 'NONE',  ( 16.75187969033515145, 34.25544727262118982, -24.30698433968624883 ) ) ;
#33888=( GEOMETRIC_REPRESENTATION_CONTEXT ( 3 ) GLOBAL_UNCERTAINTY_ASSIGNED_CONTEXT ( ( #18143 ) ) GLOBAL_UNIT_ASSIGNED_CONTEXT ( ( #43549, #99647, #76429 ) ) REPRESENTATION_CONTEXT ( 'NONE', 'WORKASPACE' ) );
#33895=EDGE_CURVE ( 'NONE', #22182, #101681, #52961, .T. ) ;
#33896=( NAMED_UNIT ( * ) PLANE_ANGLE_UNIT ( ) SI_UNIT ( $, .RADIAN. ) );
#33897=CARTESIAN_POINT ( 'NONE',  ( -28.73029465396694349, 18.79238081053094334, 40.04376963015451452 ) ) ;
#33910=SURFACE_STYLE_FILL_AREA ( #9053 ) ;
#33917=DIRECTION ( 'NONE',  ( 0.000000000000000000, 0.000000000000000000, 1.000000000000000000 ) ) ;
#33919=CARTESIAN_POINT ( 'NONE',  ( -25.85870200593686263, 35.03474222141309724, 8.998851137906763498 ) ) ;
#33925=CARTESIAN_POINT ( 'NONE',  ( -7.807718295557010357, 53.96912438917611610, -3.792492973880838836 ) ) ;
#33938=CARTESIAN_POINT ( 'NONE',  ( 9.559166278073435663, 53.41734968321387100, 3.549940974394473425 ) ) ;
#33940=CARTESIAN_POINT ( 'NONE',  ( 15.88102029263265003, 46.13028405480692129, -4.403441971141990763 ) ) ;
#33944=CARTESIAN_POINT ( 'NONE',  ( -29.87369781377633515, 13.22774345441025190, 42.09617408282262829 ) ) ;
#33945=FACE_BOUND ( 'NONE', #105798, .T. ) ;
#33961=CARTESIAN_POINT ( 'NONE',  ( 48.02835407290545078, 16.78162100668605206, 14.35535821593427386 ) ) ;
#33973=CARTESIAN_POINT ( 'NONE',  ( 9.539304943379745438, 51.45347982738971382, 1.988540865056009022 ) ) ;
#33981=VECTOR ( 'NONE', #2236, 1000.000000000000000 ) ;
#33983=CARTESIAN_POINT ( 'NONE',  ( -17.89642918806200100, 43.18034132965723870, -5.550938134534490587 ) ) ;
#33987=STYLED_ITEM ( 'NONE', ( #79273 ), #37228 ) ;
#34002=CARTESIAN_POINT ( 'NONE',  ( -38.81333125807601903, 25.21178128392378071, -12.01546574933351330 ) ) ;
#34006=CARTESIAN_POINT ( 'NONE',  ( 16.32476346754885554, 43.58736234942514898, -6.626941870814922808 ) ) ;
#34009=EDGE_CURVE ( 'NONE', #31379, #38179, #39321, .T. ) ;
#34018=( NAMED_UNIT ( * ) PLANE_ANGLE_UNIT ( ) SI_UNIT ( $, .RADIAN. ) );
#34038=CARTESIAN_POINT ( 'NONE',  ( 4.278063764781172118, 54.28324999937112239, 6.542721817263923434 ) ) ;
#34042=VECTOR ( 'NONE', #67730, 1000.000000000000000 ) ;
#34081=( NAMED_UNIT ( * ) SI_UNIT ( $, .STERADIAN. ) SOLID_ANGLE_UNIT ( ) );
#34093=CARTESIAN_POINT ( 'NONE',  ( 36.37640517269390728, 26.07922816359034712, -11.81515425344730552 ) ) ;
#34101=CARTESIAN_POINT ( 'NONE',  ( -10.12089030649893395, 44.03014547783647004, -12.90779740156153643 ) ) ;
#34117=CARTESIAN_POINT ( 'NONE',  ( 15.51166181318966508, 36.90500793569743365, 23.41746243165347607 ) ) ;
#34139=EDGE_LOOP ( 'NONE', ( #7534, #70689 ) ) ;
#34142=CARTESIAN_POINT ( 'NONE',  ( -0.9887154240794179261, 17.70149142468999770, -49.73206415546439985 ) ) ;
#34143=CARTESIAN_POINT ( 'NONE',  ( 38.31542881513956189, 27.59987916515866857, -11.19254653711393566 ) ) ;
#34146=FACE_OUTER_BOUND ( 'NONE', #79813, .T. ) ;
#34155=CARTESIAN_POINT ( 'NONE',  ( 1.005674572306967995, 34.34876838514327346, -29.24676969006877769 ) ) ;
#34163=CARTESIAN_POINT ( 'NONE',  ( 1.218727205067523522, 43.73156354412988378, 17.17928489613208143 ) ) ;
#34169=FILL_AREA_STYLE_COLOUR ( '', #68687 ) ;
#34175=CARTESIAN_POINT ( 'NONE',  ( -8.559508646656389885, 51.55638410492942825, -4.031152949374503081 ) ) ;
#34176=DIRECTION ( 'NONE',  ( -0.000000000000000000, -1.000000000000000000, -0.000000000000000000 ) ) ;
#34185=ORIENTED_EDGE ( 'NONE', *, *, #10240, .F. ) ;
#34247=CARTESIAN_POINT ( 'NONE',  ( -47.36618468514944880, 18.16301677597580877, -14.54218830158967179 ) ) ;
#34254=CARTESIAN_POINT ( 'NONE',  ( -15.73379620320076633, 35.06307335795982283, -22.31246066629909208 ) ) ;
#34274=LINE ( 'NONE', #66076, #55742 ) ;
#34285=ADVANCED_FACE ( 'NONE', ( #78563, #4696, #37629, #100716, #93170 ), #62012, .T. ) ;
#34290=( NAMED_UNIT ( * ) PLANE_ANGLE_UNIT ( ) SI_UNIT ( $, .RADIAN. ) );
#34303=CARTESIAN_POINT ( 'NONE',  ( -8.719010170337146093, 53.63221892593892193, 4.031152949374982697 ) ) ;
#34307=CARTESIAN_POINT ( 'NONE',  ( -0.3381768955574565028, 44.07166901386596436, 16.28514545986189077 ) ) ;
#34310=CYLINDRICAL_SURFACE ( 'NONE', #74415, 1.250000000000001110 ) ;
#34312=CARTESIAN_POINT ( 'NONE',  ( 6.068667535695539073, 53.39711552543036532, 8.262660017157307024 ) ) ;
#34315=CARTESIAN_POINT ( 'NONE',  ( 30.22667580650593422, 12.95764659710603262, 41.98307762325157455 ) ) ;
#34317=DIRECTION ( 'NONE',  ( 0.000000000000000000, 1.000000000000000000, -0.000000000000000000 ) ) ;
#34326=CARTESIAN_POINT ( 'NONE',  ( 0.4150691409093130169, 27.32056545513875534, 40.68202461718954055 ) ) ;
#34327=CARTESIAN_POINT ( 'NONE',  ( -30.48935137155294228, 7.748232456195979445, -41.81352479775729591 ) ) ;
#34354=DIRECTION ( 'NONE',  ( 0.000000000000000000, 0.000000000000000000, 1.000000000000000000 ) ) ;
#34364=CARTESIAN_POINT ( 'NONE',  ( -8.559508646656370345, 53.68473964988125857, -4.031152949374577688 ) ) ;
#34369=VECTOR ( 'NONE', #82217, 1000.000000000000000 ) ;
#34379=CARTESIAN_POINT ( 'NONE',  ( 24.43701635837512498, 25.27496214381292106, -32.24253520507857473 ) ) ;
#34386=CARTESIAN_POINT ( 'NONE',  ( -47.14858110737391428, 13.36679009520639205, -14.71571165017404326 ) ) ;
#34404=CARTESIAN_POINT ( 'NONE',  ( 17.89160253087129604, 45.33672951329190681, -5.299667771043276687 ) ) ;
#34413=CARTESIAN_POINT ( 'NONE',  ( 8.559508646656350805, 53.96349637827587031, -1.531152949374623651 ) ) ;
#34423=CARTESIAN_POINT ( 'NONE',  ( 16.91704105317847961, 37.08060170114688958, -21.81528127871695233 ) ) ;
#34427=B_SPLINE_CURVE_WITH_KNOTS ( 'NONE', 3,
 ( #16294, #7137, #33567, #90728, #15235, #23900, #99323, #56742, #89667, #49181, #48647, #47591, #41642, #82084, #98794, #8202 ),
 .UNSPECIFIED., .F., .F.,
 ( 4, 2, 2, 2, 2, 2, 2, 4 ),
 ( 0.006944648340236465184, 0.007952274378483222689, 0.008959900416729980194, 0.009211806926291664366, 0.009463713435853348538, 0.009967526454976709943, 0.01047133947410007135, 0.01097515249322343275 ),
 .UNSPECIFIED. ) ;
#34433=B_SPLINE_CURVE_WITH_KNOTS ( 'NONE', 3,
 ( #53042, #64197, #53568, #71714, #101591, #45497, #10959, #63665, #44963, #94582, #104630, #31313, #6453, #80339, #77845, #78365, #39389, #93511, #77314, #52490 ),
 .UNSPECIFIED., .F., .F.,
 ( 4, 2, 2, 2, 2, 2, 2, 2, 2, 4 ),
 ( 0.006888862763265872317, 0.007392898550706275898, 0.007896934338146680346, 0.008905005913027484038, 0.009157023806747679323, 0.009409041700467876343, 0.009913077487908265178, 0.01016509538162846220, 0.01041711327534865748, 0.01092114906278904979 ),
 .UNSPECIFIED. ) ;
#34437=COLOUR_RGB ( '', 0.72549020, 0.75294118, 0.79215686) ;
#34440=FILL_AREA_STYLE ('',( #98061 ) ) ;
#34442=CARTESIAN_POINT ( 'NONE',  ( -3.825321387738104166E-14, -1.200000000000000030E-05, -29.75000000000000355 ) ) ;
#34461=EDGE_CURVE ( 'NONE', #38377, #85099, #80707, .T. ) ;
#34468=DIRECTION ( 'NONE',  ( 0.000000000000000000, 0.000000000000000000, 1.000000000000000000 ) ) ;
#34477=EDGE_CURVE ( 'NONE', #59035, #34768, #100060, .T. ) ;
#34479=CARTESIAN_POINT ( 'NONE',  ( 9.749646486200582274, 53.39674446004222119, 3.172643523868706961 ) ) ;
#34486=CARTESIAN_POINT ( 'NONE',  ( -30.25691101598808075, 17.21809272184236761, 39.73659737107620771 ) ) ;
#34503=CARTESIAN_POINT ( 'NONE',  ( 49.25998992636648666, 12.93544608831382625, 15.83190612885223381 ) ) ;
#34508=CARTESIAN_POINT ( 'NONE',  ( -11.27197637059353852, 43.63422769103391374, -13.37297449460065657 ) ) ;
#34511=ORIENTED_EDGE ( 'NONE', *, *, #20294, .F. ) ;
#34523=CARTESIAN_POINT ( 'NONE',  ( -0.6462747240831046014, 46.14873864537771908, -16.41685720443574681 ) ) ;
#34541=CARTESIAN_POINT ( 'NONE',  ( 16.32339259644602691, 43.86638882296026765, -4.188650191876186035 ) ) ;
#34542=ORIENTED_EDGE ( 'NONE', *, *, #47419, .F. ) ;
#34551=EDGE_CURVE ( 'NONE', #12439, #65026, #24609, .T. ) ;
#34571=UNCERTAINTY_MEASURE_WITH_UNIT (LENGTH_MEASURE( 1.000000000000000082E-05 ), #84528, 'distance_accuracy_value', 'NONE');
#34572=CARTESIAN_POINT ( 'NONE',  ( 23.21751746555303342, 25.98869614573808207, 30.70617127781016720 ) ) ;
#34574=CARTESIAN_POINT ( 'NONE',  ( 4.189070928813702466, 54.25757288370531484, 6.683458472214860002 ) ) ;
#34578=CARTESIAN_POINT ( 'NONE',  ( -4.659280067791637059, 51.51274114929807979, 8.372560506775856837 ) ) ;
#34580=VECTOR ( 'NONE', #6519, 1000.000000000000114 ) ;
#34601=VERTEX_POINT ( 'NONE', #34837 ) ;
#34608=CARTESIAN_POINT ( 'NONE',  ( -1.013900655853712918, 53.56097311263275174, 9.749521719900309691 ) ) ;
#34625=CARTESIAN_POINT ( 'NONE',  ( 36.48001451349853852, 26.06917801760574704, -11.58280953890916720 ) ) ;
#34627=VECTOR ( 'NONE', #47607, 1000.000000000000227 ) ;
#34628=DIRECTION ( 'NONE',  ( -0.000000000000000000, -1.000000000000000000, -0.000000000000000000 ) ) ;
#34635=CARTESIAN_POINT ( 'NONE',  ( -9.508798884265706519, 44.08617864742008408, -13.17536625225998215 ) ) ;
#34636=SURFACE_SIDE_STYLE ('',( #73440 ) ) ;
#34642=COLOUR_RGB ( '', 0.31764706, 0.68627451, 0.89019608) ;
#34655=CARTESIAN_POINT ( 'NONE',  ( 16.64348903516523848, 45.88445698070336221, 4.157797401561420081 ) ) ;
#34670=B_SPLINE_CURVE_WITH_KNOTS ( 'NONE', 3,
 ( #33550, #90713, #49161, #81515, #1128, #58, #49708, #42683, #82068, #66421, #58335, #90173, #48631, #8187, #82614, #66974, #42145, #8716, #9770, #41624, #41094, #65894, #99306, #99853 ),
 .UNSPECIFIED., .F., .F.,
 ( 4, 2, 2, 2, 2, 2, 2, 2, 2, 2, 2, 4 ),
 ( 0.004982639409921949328, 0.005234721249241279864, 0.005486803088560610400, 0.005990966767199284483, 0.006495130445837957699, 0.006999294124476631782, 0.007251375963795969257, 0.007503457803115305864, 0.008007621481753976478, 0.008511785160392649693, 0.008763866999711983699, 0.009015948839031319439 ),
 .UNSPECIFIED. ) ;
#34672=CYLINDRICAL_SURFACE ( 'NONE', #42614, 1.250000000000001110 ) ;
#34682=CARTESIAN_POINT ( 'NONE',  ( 11.36440886748424361, 45.70401808670207799, 13.50555938308142245 ) ) ;
#34695=CARTESIAN_POINT ( 'NONE',  ( 7.738564917571006063, 52.10541356253746414, 1.834888082847005997 ) ) ;
#34696=FACE_OUTER_BOUND ( 'NONE', #43569, .T. ) ;
#34706=( NAMED_UNIT ( * ) PLANE_ANGLE_UNIT ( ) SI_UNIT ( $, .RADIAN. ) );
#34711=CARTESIAN_POINT ( 'NONE',  ( -0.9888730084721008007, 12.53170386526280211, -49.73224619698263638 ) ) ;
#34715=CARTESIAN_POINT ( 'NONE',  ( 9.203147141233843698, 43.65617212538753478, -14.80172050158656383 ) ) ;
#34720=( NAMED_UNIT ( * ) PLANE_ANGLE_UNIT ( ) SI_UNIT ( $, .RADIAN. ) );
#34729=CARTESIAN_POINT ( 'NONE',  ( -16.02936841876867291, 43.70325603760588251, 6.508067950779399702 ) ) ;
#34736=DIRECTION ( 'NONE',  ( -0.000000000000000000, 1.000000000000000000, -0.000000000000000000 ) ) ;
#34743=VERTEX_POINT ( 'NONE', #35368 ) ;
#34744=CARTESIAN_POINT ( 'NONE',  ( 8.559508646656103892, 51.55638410492932167, -4.031152949375861105 ) ) ;
#34747=CARTESIAN_POINT ( 'NONE',  ( -0.3375343507057477765, 27.30883569689895296, -40.71519194888146131 ) ) ;
#34751=CARTESIAN_POINT ( 'NONE',  ( -10.61958778326375175, 43.19936960986098740, 15.37415780603073578 ) ) ;
#34753=CARTESIAN_POINT ( 'NONE',  ( -49.22174280021781811, 12.91003493663466628, 15.98497293137739561 ) ) ;
#34755=SURFACE_STYLE_FILL_AREA ( #28261 ) ;
#34767=CARTESIAN_POINT ( 'NONE',  ( -0.7804417267264509572, 13.54273479047304285, 51.48091406469324482 ) ) ;
#34768=VERTEX_POINT ( 'NONE', #71405 ) ;
#34790=CARTESIAN_POINT ( 'NONE',  ( -16.11301951124610099, 35.08081939474628541, -21.97927874236063417 ) ) ;
#34800=LINE ( 'NONE', #92452, #1974 ) ;
#34804=VERTEX_POINT ( 'NONE', #80025 ) ;
#34832=CARTESIAN_POINT ( 'NONE',  ( 0.3592208079800993104, 13.57940237358916669, 49.30120215405869999 ) ) ;
#34835=CARTESIAN_POINT ( 'NONE',  ( 38.81137242944067367, 25.17601004987945501, -12.34914416957476568 ) ) ;
#34837=CARTESIAN_POINT ( 'NONE',  ( 0.000000000000000000, 27.68727484027578356, 33.82893434829263413 ) ) ;
#34840=DIRECTION ( 'NONE',  ( 0.000000000000000000, 0.000000000000000000, 1.000000000000000000 ) ) ;
#34854=ORIENTED_EDGE ( 'NONE', *, *, #81656, .F. ) ;
#34856=CARTESIAN_POINT ( 'NONE',  ( 0.1685692406266287302, 27.29958877905243142, 40.74143671976548120 ) ) ;
#34869=LINE ( 'NONE', #27858, #56255 ) ;
#34883=ORIENTED_EDGE ( 'NONE', *, *, #1562, .F. ) ;
#34904=ORIENTED_EDGE ( 'NONE', *, *, #33140, .T. ) ;
#34913=VERTEX_POINT ( 'NONE', #10650 ) ;
#34915=CARTESIAN_POINT ( 'NONE',  ( -46.96405579082744453, 13.62080378033662420, -14.94667195310861985 ) ) ;
#34930=EDGE_LOOP ( 'NONE', ( #24918, #36639 ) ) ;
#34931=CARTESIAN_POINT ( 'NONE',  ( 17.40646473312635578, 45.37698912868005863, -6.411815653116820002 ) ) ;
#34949=CARTESIAN_POINT ( 'NONE',  ( 16.75187969033515145, -1.200000000000000030E-05, -24.30698433968624883 ) ) ;
#34970=EDGE_CURVE ( 'NONE', #84082, #79044, #10132, .T. ) ;
#34978=CARTESIAN_POINT ( 'NONE',  ( -0.5691298260866446412, 27.34388701663959509, 40.61608021419867498 ) ) ;
#35011=EDGE_CURVE ( 'NONE', #106068, #67879, #25356, .T. ) ;
#35012=EDGE_CURVE ( 'NONE', #59308, #69676, #29550, .T. ) ;
#35022=ORIENTED_EDGE ( 'NONE', *, *, #88752, .T. ) ;
#35024=CARTESIAN_POINT ( 'NONE',  ( 49.18580537133217945, 13.60959006579815700, 15.12486994001107909 ) ) ;
#35025=CARTESIAN_POINT ( 'NONE',  ( -6.536855819840425852, 51.40560724102103052, -7.402653316414548712 ) ) ;
#35032=CARTESIAN_POINT ( 'NONE',  ( 0.3381990287830299868, 46.20001774662581084, -16.28516304919335411 ) ) ;
#35040=ORIENTED_EDGE ( 'NONE', *, *, #14085, .T. ) ;
#35047=CARTESIAN_POINT ( 'NONE',  ( -0.3377172304431446115, 45.31573710349624662, -18.71511598565236056 ) ) ;
#35050=CARTESIAN_POINT ( 'NONE',  ( -23.30007435341033073, 25.23546008595426215, -33.20617127781038391 ) ) ;
#35054=CARTESIAN_POINT ( 'NONE',  ( 3.337161262018383995E-15, 37.21016666119768246, 27.25000000000000000 ) ) ;
#35088=FILL_AREA_STYLE_COLOUR ( '', #40521 ) ;
#35089=CYLINDRICAL_SURFACE ( 'NONE', #25971, 1.250000000000001110 ) ;
#35108=CARTESIAN_POINT ( 'NONE',  ( 30.90131729786656223, 8.441056540751519677, -41.14701368050901920 ) ) ;
#35118=EDGE_LOOP ( 'NONE', ( #8149, #70884, #66135, #84108 ) ) ;
#35119=DIRECTION ( 'NONE',  ( -0.000000000000000000, 1.000000000000000000, -0.000000000000000000 ) ) ;
#35124=SURFACE_STYLE_USAGE ( .BOTH. , #52327 ) ;
#35137=( LENGTH_UNIT ( ) NAMED_UNIT ( * ) SI_UNIT ( .MILLI., .METRE. ) );
#35152=EDGE_CURVE ( 'NONE', #85099, #38377, #11169, .T. ) ;
#35162=CARTESIAN_POINT ( 'NONE',  ( -0.7777183698329714900, 45.39552846407493547, 18.48206553968775268 ) ) ;
#35168=CARTESIAN_POINT ( 'NONE',  ( -48.98943663899283507, 7.951733423214400354, -16.40652009737680217 ) ) ;
#35179=ORIENTED_EDGE ( 'NONE', *, *, #10500, .T. ) ;
#35187=( LENGTH_UNIT ( ) NAMED_UNIT ( * ) SI_UNIT ( .MILLI., .METRE. ) );
#35188=SURFACE_STYLE_FILL_AREA ( #59451 ) ;
#35192=CARTESIAN_POINT ( 'NONE',  ( 30.55667715332029744, 16.37467338430768038, -39.95293003182862890 ) ) ;
#35213=MECHANICAL_DESIGN_GEOMETRIC_PRESENTATION_REPRESENTATION('',(#57563),#9365);
#35233=CARTESIAN_POINT ( 'NONE',  ( 36.57467119294569358, 26.05182110615610469, 11.44111246432268736 ) ) ;
#35253=CARTESIAN_POINT ( 'NONE',  ( 28.34968022077493188, 36.30790721977597713, -8.950547681938596511 ) ) ;
#35264=ORIENTED_EDGE ( 'NONE', *, *, #12962, .T. ) ;
#35265=CARTESIAN_POINT ( 'NONE',  ( 7.939818003892609610, 52.04606761948748073, -1.683583523684331729 ) ) ;
#35290=CARTESIAN_POINT ( 'NONE',  ( -22.10805348356095124, 26.03559744305474055, -31.35713886023327390 ) ) ;
#35293=CARTESIAN_POINT ( 'NONE',  ( -0.1698333930863181740, 44.08205155922173901, -16.25874923821028162 ) ) ;
#35299=( GEOMETRIC_REPRESENTATION_CONTEXT ( 3 ) GLOBAL_UNCERTAINTY_ASSIGNED_CONTEXT ( ( #59195 ) ) GLOBAL_UNIT_ASSIGNED_CONTEXT ( ( #105425, #56309, #32085 ) ) REPRESENTATION_CONTEXT ( 'NONE', 'WORKASPACE' ) );
#35304=B_SPLINE_CURVE_WITH_KNOTS ( 'NONE', 3,
 ( #82301, #7871, #98479, #73670, #8411, #56951, #91477, #58016, #81223, #24106, #40251, #50453, #82838, #25164, #8939, #90944, #97957, #89871 ),
 .UNSPECIFIED., .F., .F.,
 ( 4, 2, 2, 2, 2, 2, 2, 2, 4 ),
 ( 0.005485713726180331713, 0.005989477085366931401, 0.006493240444553531089, 0.006997003803740123838, 0.007500767162926716587, 0.008004530522113308469, 0.008508293881299901218, 0.009012057240486493967, 0.009515820599673086716 ),
 .UNSPECIFIED. ) ;
#35305=PRESENTATION_STYLE_ASSIGNMENT (( #52508 ) ) ;
#35318=CARTESIAN_POINT ( 'NONE',  ( -15.50700860752355759, 34.82687621134751055, -23.25438777637638310 ) ) ;
#35323=CARTESIAN_POINT ( 'NONE',  ( -17.99814426515498056, 34.31762318392226518, 23.18337261660863291 ) ) ;
#35329=CARTESIAN_POINT ( 'NONE',  ( 48.90200833301634731, 9.381371963275078940, -14.70088518568461566 ) ) ;
#35330=SURFACE_SIDE_STYLE ('',( #52529 ) ) ;
#35332=CARTESIAN_POINT ( 'NONE',  ( 6.046357265851751706, 51.82880103987274367, 6.273311111885435665 ) ) ;
#35342=EDGE_CURVE ( 'NONE', #22572, #8098, #63361, .T. ) ;
#35357=ORIENTED_EDGE ( 'NONE', *, *, #17490, .F. ) ;
#35359=CARTESIAN_POINT ( 'NONE',  ( 0.2968935920006570695, 7.824247317432593718, 51.71637011724927646 ) ) ;
#35366=AXIS2_PLACEMENT_3D ( 'NONE', #92835, #51842, #84755 ) ;
#35368=CARTESIAN_POINT ( 'NONE',  ( 37.56673239365899519, 25.75719283951025318, -10.95617127780834998 ) ) ;
#35380=CARTESIAN_POINT ( 'NONE',  ( 30.63818566637229779, 16.09127295623281029, 40.04027533505442449 ) ) ;
#35386=CARTESIAN_POINT ( 'NONE',  ( -7.345544385418572908, 54.30768395588341946, 2.471487999594874196 ) ) ;
#35388=B_SPLINE_CURVE_WITH_KNOTS ( 'NONE', 3,
 ( #33884, #60807, #83462, #74826, #907, #99645, #18777, #58673, #2005, #75365, #1466, #18226, #67300, #92086, #51080, #84001, #10107, #62928, #95822, #61881 ),
 .UNSPECIFIED., .F., .F.,
 ( 4, 2, 2, 2, 2, 2, 2, 2, 2, 4 ),
 ( 0.007150819864390691935, 0.007654630284942562542, 0.008158440705494433148, 0.008662251126046304622, 0.009166061546598176096, 0.009669871967150047570, 0.01017368238770191731, 0.01042558759797785305, 0.01067749280825378705, 0.01118130322880565505 ),
 .UNSPECIFIED. ) ;
#35390=CARTESIAN_POINT ( 'NONE',  ( 1.250300626116370273, 27.68715609264891597, 39.65716501001974592 ) ) ;
#35405=ORIENTED_EDGE ( 'NONE', *, *, #11141, .T. ) ;
#35425=UNCERTAINTY_MEASURE_WITH_UNIT (LENGTH_MEASURE( 1.000000000000000082E-05 ), #73187, 'distance_accuracy_value', 'NONE');
#35442=VERTEX_POINT ( 'NONE', #74600 ) ;
#35444=VERTEX_POINT ( 'NONE', #73532 ) ;
#35446=CARTESIAN_POINT ( 'NONE',  ( -47.90468627969800508, 11.89467801380304834, -14.35535821593460781 ) ) ;
#35465=CARTESIAN_POINT ( 'NONE',  ( 28.43950163419728483, 12.73412882672191770, -40.70661530191392785 ) ) ;
#35487=DIRECTION ( 'NONE',  ( 0.000000000000000000, 0.000000000000000000, 1.000000000000000000 ) ) ;
#35488=MECHANICAL_DESIGN_GEOMETRIC_PRESENTATION_REPRESENTATION('',(#44085),#64706);
#35509=CARTESIAN_POINT ( 'NONE',  ( -0.1683297036434198424, 28.20649408426939786, 38.25000000000000711 ) ) ;
#35510=CARTESIAN_POINT ( 'NONE',  ( 0.1689026954396629643, 37.21016666119767535, -27.24999999999999289 ) ) ;
#35515=PRESENTATION_STYLE_ASSIGNMENT (( #3657 ) ) ;
#35539=SURFACE_STYLE_USAGE ( .BOTH. , #91098 ) ;
#35557=ORIENTED_EDGE ( 'NONE', *, *, #99103, .T. ) ;
#35573=EDGE_CURVE ( 'NONE', #6732, #26726, #106285, .T. ) ;
#35587=CARTESIAN_POINT ( 'NONE',  ( 1.249225752714849813, 36.86244653973282226, 28.17767836393376513 ) ) ;
#35592=ORIENTED_EDGE ( 'NONE', *, *, #43186, .F. ) ;
#35628=( NAMED_UNIT ( * ) PLANE_ANGLE_UNIT ( ) SI_UNIT ( $, .RADIAN. ) );
#35632=LINE ( 'NONE', #92216, #60592 ) ;
#35637=CARTESIAN_POINT ( 'NONE',  ( 0.000000000000000000, 50.89575828009192549, -11.27631144943088692 ) ) ;
#35643=CARTESIAN_POINT ( 'NONE',  ( 28.18125686882138226, 36.45097005328995721, 8.150216328741358041 ) ) ;
#35658=FACE_OUTER_BOUND ( 'NONE', #93755, .T. ) ;
#35692=CARTESIAN_POINT ( 'NONE',  ( 36.31532598674183987, 26.06253081513260739, -12.14693892978808876 ) ) ;
#35694=FACE_BOUND ( 'NONE', #58077, .T. ) ;
#35700=CARTESIAN_POINT ( 'NONE',  ( -15.39661048887588102, 46.16593794825681130, -5.596966726906050127 ) ) ;
#35705=CARTESIAN_POINT ( 'NONE',  ( -1.010678914899137304, 46.02204249784927725, 16.74682395785559663 ) ) ;
#35734=CARTESIAN_POINT ( 'NONE',  ( 30.77329953030971765, 15.53171713056514491, -40.23250653748806371 ) ) ;
#35735=MECHANICAL_DESIGN_GEOMETRIC_PRESENTATION_REPRESENTATION('',(#30561),#9806);
#35744=CARTESIAN_POINT ( 'NONE',  ( -0.8337482156482161066, 18.10529858437485728, -49.56546807274770572 ) ) ;
#35745=CARTESIAN_POINT ( 'NONE',  ( 38.81818101478957317, 27.31133193661636227, -12.26431571994239000 ) ) ;
#35749=CARTESIAN_POINT ( 'NONE',  ( 1.167749971007850274, 14.75947676340571313, 50.96289688649348193 ) ) ;
#35759=LINE ( 'NONE', #45420, #98183 ) ;
#35766=AXIS2_PLACEMENT_3D ( 'NONE', #43869, #76762, #59542 ) ;
#35767=DIRECTION ( 'NONE',  ( 0.000000000000000000, 0.000000000000000000, -1.000000000000000000 ) ) ;
#35776=FACE_BOUND ( 'NONE', #39892, .T. ) ;
#35780=CYLINDRICAL_SURFACE ( 'NONE', #60484, 1.249999999999999778 ) ;
#35782=CARTESIAN_POINT ( 'NONE',  ( -16.91846161659832859, 36.35180932965544542, 24.29864124313478868 ) ) ;
#35789=CIRCLE ( 'NONE', #18524, 46.61112130868859538 ) ;
#35809=CARTESIAN_POINT ( 'NONE',  ( 7.561403392358007736, 52.15275433178552333, -2.010202227193783830 ) ) ;
#35820=CARTESIAN_POINT ( 'NONE',  ( -49.26989972136284024, 12.96118195421251507, 15.76560135797571505 ) ) ;
#35823=SURFACE_STYLE_USAGE ( .BOTH. , #61130 ) ;
#35837=AXIS2_PLACEMENT_3D ( 'NONE', #37900, #84824, #44912 ) ;
#35848=CARTESIAN_POINT ( 'NONE',  ( 16.64348903516523848, -1.200000000000000030E-05, 5.407797401561420969 ) ) ;
#35852=DIRECTION ( 'NONE',  ( -0.000000000000000000, 1.000000000000000000, -0.000000000000000000 ) ) ;
#35870=CARTESIAN_POINT ( 'NONE',  ( 49.27018817646321480, 7.792903869376768711, -15.76322754694156281 ) ) ;
#35872=CARTESIAN_POINT ( 'NONE',  ( 5.454359399073367420, 52.03812987433942538, 6.039366617364852807 ) ) ;
#35887=CARTESIAN_POINT ( 'NONE',  ( -36.58618025929193607, 27.99671736784095799, -12.99775655248998874 ) ) ;
#35900=LINE ( 'NONE', #86562, #80185 ) ;
#35902=CARTESIAN_POINT ( 'NONE',  ( 8.455951367436818379E-15, 13.70447791526914294, 49.24999999999998579 ) ) ;
#35906=CYLINDRICAL_SURFACE ( 'NONE', #9962, 24.55262289886175964 ) ;
#35910=ADVANCED_FACE ( 'NONE', ( #31923, #49669, #41585, #16240, #97684 ), #23359, .T. ) ;
#35922=CARTESIAN_POINT ( 'NONE',  ( 30.93371285580988328, 14.00361151752279198, 40.91601221254699539 ) ) ;
#35927=CARTESIAN_POINT ( 'NONE',  ( -7.561790601661408928, 54.28098289519358843, 2.010020282033269989 ) ) ;
#35933=CARTESIAN_POINT ( 'NONE',  ( -30.59731729458119531, 7.793314453875768599, -41.71112871039140657 ) ) ;
#35939=B_SPLINE_CURVE_WITH_KNOTS ( 'NONE', 3,
 ( #70064, #79212, #40740, #87319, #12345, #71636, #94353, #102965, #71120, #78666, #45271, #22064, #45787, #54923, #13398, #21540, #20516, #37739, #104546, #5336, #63039, #14457, #70600, #47368, #46842, #38259, #87849, #104009, #53351, #103492 ),
 .UNSPECIFIED., .F., .F.,
 ( 4, 2, 2, 2, 2, 2, 2, 2, 2, 2, 2, 2, 2, 2, 4 ),
 ( 0.01009607051181185544, 0.01101525429224261762, 0.01193443807267337807, 0.01285362185310414025, 0.01377280563353490243, 0.01423239752375028352, 0.01446219346885797494, 0.01469198941396566288, 0.01492178535907335256, 0.01515158130418104224, 0.01538137724928873018, 0.01561117319439641812, 0.01607076508461179054, 0.01653035697482716296, 0.01744954075525791126 ),
 .UNSPECIFIED. ) ;
#35941=ORIENTED_EDGE ( 'NONE', *, *, #1677, .T. ) ;
#35950=CARTESIAN_POINT ( 'NONE',  ( 4.512020406555891761, 54.30832494546023526, -6.299191669131390725 ) ) ;
#35953=ORIENTED_EDGE ( 'NONE', *, *, #4748, .T. ) ;
#35961=CARTESIAN_POINT ( 'NONE',  ( -23.55048488053928324, 27.32134238698565554, -33.17259636481922769 ) ) ;
#35979=VERTEX_POINT ( 'NONE', #22 ) ;
#35989=CARTESIAN_POINT ( 'NONE',  ( -47.50656546823834958, 12.72630541683655458, -14.46671989142072512 ) ) ;
#35995=CARTESIAN_POINT ( 'NONE',  ( -16.96448817358102801, 43.37119804630366104, -6.626685396512355553 ) ) ;
#36004=EDGE_CURVE ( 'NONE', #14145, #18144, #31976, .T. ) ;
#36008=CARTESIAN_POINT ( 'NONE',  ( 28.56401049668863479, 13.37477103922271304, -40.29034081819158075 ) ) ;
#36011=CARTESIAN_POINT ( 'NONE',  ( -9.655270732726616956, 51.27407282810504086, 3.405563007191358960 ) ) ;
#36014=FILL_AREA_STYLE_COLOUR ( '', #62500 ) ;
#36047=B_SPLINE_CURVE_WITH_KNOTS ( 'NONE', 3,
 ( #106, #23932, #33078, #24979, #47093, #72956, #39566, #22862, #90758, #88630, #79995, #63837, #96730, #14720, #80521, #6639, #72441, #105344, #97242, #34142, #26072, #35744, #84256, #1170, #91300, #10872, #58383, #8762, #1726, #60011 ),
 .UNSPECIFIED., .F., .F.,
 ( 4, 2, 2, 2, 2, 2, 2, 2, 2, 2, 2, 2, 2, 2, 4 ),
 ( 0.01399668719228680698, 0.01422696114353627292, 0.01445723509478573886, 0.01491778299728466380, 0.01537833089978358700, 0.01583887880228251194, 0.01675997460728035141, 0.01768107041227819087, 0.01860216621727603381, 0.01952326202227386981, 0.01998380992477279475, 0.02044435782727171969, 0.02090490572977064115, 0.02113517968102010883, 0.02136545363226957303 ),
 .UNSPECIFIED. ) ;
#36049=VERTEX_POINT ( 'NONE', #25445 ) ;
#36063=VERTEX_POINT ( 'NONE', #105784 ) ;
#36068=( GEOMETRIC_REPRESENTATION_CONTEXT ( 3 ) GLOBAL_UNCERTAINTY_ASSIGNED_CONTEXT ( ( #54182 ) ) GLOBAL_UNIT_ASSIGNED_CONTEXT ( ( #85424, #44436, #11509 ) ) REPRESENTATION_CONTEXT ( 'NONE', 'WORKASPACE' ) );
#36082=AXIS2_PLACEMENT_3D ( 'NONE', #87234, #44660, #37656 ) ;
#36108=EDGE_CURVE ( 'NONE', #95845, #88418, #30077, .T. ) ;
#36109=CARTESIAN_POINT ( 'NONE',  ( -1.250111696621528434, 36.68807930902310943, 28.65717016957791685 ) ) ;
#36134=CARTESIAN_POINT ( 'NONE',  ( 1.101222382041291858, 36.52459501129955299, 29.11284624768989460 ) ) ;
#36149=CARTESIAN_POINT ( 'NONE',  ( -16.02196273765588330, 46.08952128005078919, 4.311160109051469291 ) ) ;
#36172=ORIENTED_EDGE ( 'NONE', *, *, #30526, .T. ) ;
#36191=FACE_BOUND ( 'NONE', #105244, .T. ) ;
#36195=SURFACE_SIDE_STYLE ('',( #67463 ) ) ;
#36211=CARTESIAN_POINT ( 'NONE',  ( 24.32789867356907720, 27.33682607920834684, 32.55354264101764983 ) ) ;
#36212=CARTESIAN_POINT ( 'NONE',  ( -48.02835407290516656, -1.200000000000000030E-05, 16.85535821593516559 ) ) ;
#36213=CARTESIAN_POINT ( 'NONE',  ( -17.77153375527955603, 36.31766862386357531, -23.79949801963322997 ) ) ;
#36214=VECTOR ( 'NONE', #103243, 1000.000000000000000 ) ;
#36219=CARTESIAN_POINT ( 'NONE',  ( -29.68315524077005207, 18.29184282782459547, -39.60535821593474282 ) ) ;
#36228=CARTESIAN_POINT ( 'NONE',  ( -3.311033882356798252E-14, 37.21016666119783167, -27.24999999999961986 ) ) ;
#36234=CARTESIAN_POINT ( 'NONE',  ( -15.65186372275021931, 46.18633577147561908, -4.642160826816701835 ) ) ;
#36237=UNCERTAINTY_MEASURE_WITH_UNIT (LENGTH_MEASURE( 1.000000000000000082E-05 ), #84288, 'distance_accuracy_value', 'NONE');
#36245=EDGE_CURVE ( 'NONE', #41831, #53305, #29564, .T. ) ;
#36249=CARTESIAN_POINT ( 'NONE',  ( -28.30714194752022195, 36.37574732085258944, 8.454175457664668158 ) ) ;
#36251=CARTESIAN_POINT ( 'NONE',  ( -49.27893332325997022, 7.918143476871234654, -15.56220613712109468 ) ) ;
#36256=DIRECTION ( 'NONE',  ( -0.000000000000000000, 1.000000000000000000, -0.000000000000000000 ) ) ;
#36282=VERTEX_POINT ( 'NONE', #11324 ) ;
#36288=CARTESIAN_POINT ( 'NONE',  ( 17.63688729554944601, 43.19915187278243707, 6.171107486271527165 ) ) ;
#36297=EDGE_CURVE ( 'NONE', #492, #9858, #10274, .T. ) ;
#36314=CARTESIAN_POINT ( 'NONE',  ( -7.481934216406634697, 52.00372086678742534, -3.435407541340197657 ) ) ;
#36317=CARTESIAN_POINT ( 'NONE',  ( -0.5307430543511253429, 13.43124519068178557, -49.36191628181192925 ) ) ;
#36327=STYLED_ITEM ( 'NONE', ( #36780 ), #49987 ) ;
#36353=ORIENTED_EDGE ( 'NONE', *, *, #31441, .T. ) ;
#36355=ORIENTED_EDGE ( 'NONE', *, *, #91786, .F. ) ;
#36357=CARTESIAN_POINT ( 'NONE',  ( 47.57308385268299844, 17.76309546253586191, -14.43907613026851422 ) ) ;
#36359=FACE_BOUND ( 'NONE', #21570, .T. ) ;
#36363=FILL_AREA_STYLE_COLOUR ( '', #6440 ) ;
#36365=DIRECTION ( 'NONE',  ( 0.000000000000000000, 1.000000000000000000, 0.000000000000000000 ) ) ;
#36367=ADVANCED_FACE ( 'NONE', ( #96915 ), #32193, .F. ) ;
#36372=AXIS2_PLACEMENT_3D ( 'NONE', #60731, #10552, #92539 ) ;
#36404=CARTESIAN_POINT ( 'NONE',  ( 9.507180395704930120, 46.21450860196618038, -13.17662286211872669 ) ) ;
#36408=CARTESIAN_POINT ( 'NONE',  ( 48.80588606933620355, 9.656672550839653368, -14.61916856843063250 ) ) ;
#36421=CARTESIAN_POINT ( 'NONE',  ( 6.250413015032560970, 51.28038719428062819, -8.085695086823610822 ) ) ;
#36424=CARTESIAN_POINT ( 'NONE',  ( 49.26579422795299479, 13.23794831108222603, -15.39367580924973211 ) ) ;
#36427=CARTESIAN_POINT ( 'NONE',  ( -36.81742733023035896, 25.76195274633174392, 13.21949667342699897 ) ) ;
#36440=VECTOR ( 'NONE', #12385, 1000.000000000000000 ) ;
#36447=AXIS2_PLACEMENT_3D ( 'NONE', #15920, #21923, #79068 ) ;
#36461=ORIENTED_EDGE ( 'NONE', *, *, #23083, .T. ) ;
#36483=DIRECTION ( 'NONE',  ( 0.000000000000000000, 1.000000000000000000, 0.000000000000000000 ) ) ;
#36487=( NAMED_UNIT ( * ) SI_UNIT ( $, .STERADIAN. ) SOLID_ANGLE_UNIT ( ) );
#36492=CARTESIAN_POINT ( 'NONE',  ( -23.85899507165724032, 27.29461519911105682, -33.04201830783522809 ) ) ;
#36504=CARTESIAN_POINT ( 'NONE',  ( -1.216929526016031105, 51.81227483227483788, -8.673337395590676735 ) ) ;
#36527=CARTESIAN_POINT ( 'NONE',  ( 5.372128395027464975, 54.18872941621413730, 6.031152949374466665 ) ) ;
#36575=LINE ( 'NONE', #62939, #70136 ) ;
#36593=ORIENTED_EDGE ( 'NONE', *, *, #48124, .F. ) ;
#36611=FACE_OUTER_BOUND ( 'NONE', #100221, .T. ) ;
#36621=ORIENTED_EDGE ( 'NONE', *, *, #26556, .T. ) ;
#36622=CARTESIAN_POINT ( 'NONE',  ( 0.6238343018367229487, 8.124960217122801254, -51.58729135945497291 ) ) ;
#36639=ORIENTED_EDGE ( 'NONE', *, *, #1475, .F. ) ;
#36646=VERTEX_POINT ( 'NONE', #42242 ) ;
#36687=EDGE_CURVE ( 'NONE', #15047, #1743, #79188, .T. ) ;
#36718=SURFACE_SIDE_STYLE ('',( #44242 ) ) ;
#36744=FILL_AREA_STYLE_COLOUR ( '', #20232 ) ;
#36750=LINE ( 'NONE', #55509, #57497 ) ;
#36778=CARTESIAN_POINT ( 'NONE',  ( 23.21751746555303342, 28.11705169068991594, 30.70617127781016720 ) ) ;
#36780=PRESENTATION_STYLE_ASSIGNMENT (( #69644 ) ) ;
#36798=SURFACE_STYLE_USAGE ( .BOTH. , #94484 ) ;
#36799=ORIENTED_EDGE ( 'NONE', *, *, #62351, .T. ) ;
#36810=CARTESIAN_POINT ( 'NONE',  ( 0.3605873925011542358, 13.03538297051737338, 51.69841471560108914 ) ) ;
#36834=DIRECTION ( 'NONE',  ( -0.000000000000000000, -1.000000000000000000, -0.000000000000000000 ) ) ;
#36839=CARTESIAN_POINT ( 'NONE',  ( -0.3616048520552285206, 7.866658882532708397, -51.69814723577159299 ) ) ;
#36841=CARTESIAN_POINT ( 'NONE',  ( -17.99637020931157849, 36.53998198029804456, 22.85704674614657961 ) ) ;
#36847=CARTESIAN_POINT ( 'NONE',  ( 17.85370335554367216, 34.21381263225121216, -23.65318376138480971 ) ) ;
#36852=CARTESIAN_POINT ( 'NONE',  ( -9.648094638230798381, 46.21279293231379626, -13.07965317076984135 ) ) ;
#36881=CARTESIAN_POINT ( 'NONE',  ( -23.21751746555280249, -1.200000000000000030E-05, -33.20617127781034839 ) ) ;
#36884=( NAMED_UNIT ( * ) PLANE_ANGLE_UNIT ( ) SI_UNIT ( $, .RADIAN. ) );
#36888=ORIENTED_EDGE ( 'NONE', *, *, #24690, .F. ) ;
#36896=CARTESIAN_POINT ( 'NONE',  ( -22.81493026622527864, 25.35530515213832459, -33.14233034566358072 ) ) ;
#36897=CARTESIAN_POINT ( 'NONE',  ( -26.01151370334376978, 35.07581603598547559, -8.178615366860272573 ) ) ;
#36925=CARTESIAN_POINT ( 'NONE',  ( 8.559508646656103892, 51.55638410492932167, -4.031152949375861105 ) ) ;
#36940=CARTESIAN_POINT ( 'NONE',  ( 49.25896281664822141, 12.93370316445848900, -15.83749202751853780 ) ) ;
#36951=DIRECTION ( 'NONE',  ( -0.000000000000000000, 1.000000000000000000, -0.000000000000000000 ) ) ;
#36952=CARTESIAN_POINT ( 'NONE',  ( 0.9479484640198931888, 12.67371156664382070, 49.67349439981760639 ) ) ;
#36964=ADVANCED_FACE ( 'NONE', ( #4989 ), #29821, .T. ) ;
#36980=CARTESIAN_POINT ( 'NONE',  ( -7.465322217760688162, 54.30106466035046253, 2.153579458703050786 ) ) ;
#37002=VERTEX_POINT ( 'NONE', #17338 ) ;
#37004=CARTESIAN_POINT ( 'NONE',  ( 5.124566304833717112, 53.50649568328331185, -8.531152949374618544 ) ) ;
#37012=CARTESIAN_POINT ( 'NONE',  ( 2.761899744546835519E-15, 41.79151656018385097, 22.55262289886175608 ) ) ;
#37013=( LENGTH_UNIT ( ) NAMED_UNIT ( * ) SI_UNIT ( .MILLI., .METRE. ) );
#37026=CARTESIAN_POINT ( 'NONE',  ( -1.221877481064467252, 51.58286532492357424, -9.308967581158638538 ) ) ;
#37040=EDGE_LOOP ( 'NONE', ( #97034, #27861 ) ) ;
#37051=CARTESIAN_POINT ( 'NONE',  ( 30.10565283232790179, 7.858405490276857641, 42.03377155531566700 ) ) ;
#37085=( NAMED_UNIT ( * ) SI_UNIT ( $, .STERADIAN. ) SOLID_ANGLE_UNIT ( ) );
#37090=ADVANCED_FACE ( 'NONE', ( #72363 ), #72878, .F. ) ;
#37113=CARTESIAN_POINT ( 'NONE',  ( 2.099928008175702901E-23, 44.08548369317413318, -16.25000000000000000 ) ) ;
#37115=FACE_OUTER_BOUND ( 'NONE', #76990, .T. ) ;
#37120=LINE ( 'NONE', #103408, #93652 ) ;
#37144=MECHANICAL_DESIGN_GEOMETRIC_PRESENTATION_REPRESENTATION('',(#30187),#18197);
#37162=CARTESIAN_POINT ( 'NONE',  ( -0.5692325763115247961, 36.34704713563726131, 29.61603353372992586 ) ) ;
#37183=EDGE_CURVE ( 'NONE', #61560, #14947, #76079, .T. ) ;
#37185=CARTESIAN_POINT ( 'NONE',  ( 15.98857071195775781, 36.61411899915854917, -24.05954505250366893 ) ) ;
#37196=CARTESIAN_POINT ( 'NONE',  ( -38.33026151711676022, 27.37213072108648504, 13.20981099482207988 ) ) ;
#37203=CARTESIAN_POINT ( 'NONE',  ( -29.68315524076956180, 8.302504244945341227, 42.10535821593508388 ) ) ;
#37228=ADVANCED_FACE ( 'NONE', ( #71695 ), #71179, .F. ) ;
#37234=CARTESIAN_POINT ( 'NONE',  ( 28.30742934768286645, 36.37554873744188910, 8.455121100274956447 ) ) ;
#37263=CARTESIAN_POINT ( 'NONE',  ( 23.55048488053951417, 27.32134238698565554, 33.17259636481905005 ) ) ;
#37285=CARTESIAN_POINT ( 'NONE',  ( -9.032229468219194146, 43.92653636418285856, -14.03110142013872519 ) ) ;
#37300=CARTESIAN_POINT ( 'NONE',  ( -49.18559949472793846, 8.441045694768776642, -15.12439388195359591 ) ) ;
#37317=EDGE_LOOP ( 'NONE', ( #14957, #71560 ) ) ;
#37335=ORIENTED_EDGE ( 'NONE', *, *, #17884, .T. ) ;
#37341=CARTESIAN_POINT ( 'NONE',  ( 17.58395415724061195, 43.20953024635295492, 6.235491673352195008 ) ) ;
#37350=UNCERTAINTY_MEASURE_WITH_UNIT (LENGTH_MEASURE( 1.000000000000000082E-05 ), #105788, 'distance_accuracy_value', 'NONE');
#37407=CARTESIAN_POINT ( 'NONE',  ( -10.45066360978664122, 46.08369782028256623, 12.90779740156196986 ) ) ;
#37418=EDGE_CURVE ( 'NONE', #36282, #39760, #15935, .T. ) ;
#37452=VECTOR ( 'NONE', #101553, 1000.000000000000114 ) ;
#37454=CARTESIAN_POINT ( 'NONE',  ( -18.00372896877115636, 34.34010858039469127, 23.10073396340781215 ) ) ;
#37474=ORIENTED_EDGE ( 'NONE', *, *, #54002, .T. ) ;
#37478=CARTESIAN_POINT ( 'NONE',  ( 49.19536753089936099, 12.91488588853587061, -16.05939653828881220 ) ) ;
#37498=CARTESIAN_POINT ( 'NONE',  ( -26.10828281006072871, 37.18604047991734518, -8.034813406053556761 ) ) ;
#37502=ADVANCED_FACE ( 'NONE', ( #41998, #74877, #93214, #33945, #100232 ), #68379, .T. ) ;
#37503=CARTESIAN_POINT ( 'NONE',  ( -10.28624191511830155, 43.99263840937192782, -12.90779740156156841 ) ) ;
#37527=CARTESIAN_POINT ( 'NONE',  ( 8.718495747319281008, 53.90653400547435581, -1.531152949374520622 ) ) ;
#37546=CARTESIAN_POINT ( 'NONE',  ( -17.03955750629483745, 45.47802236175360235, -6.596165372994933662 ) ) ;
#37560=SURFACE_STYLE_USAGE ( .BOTH. , #46665 ) ;
#37572=CARTESIAN_POINT ( 'NONE',  ( -29.68315524076956891, -1.200000000000000030E-05, 42.10535821593508388 ) ) ;
#37580=ORIENTED_EDGE ( 'NONE', *, *, #7852, .T. ) ;
#37583=CARTESIAN_POINT ( 'NONE',  ( -36.95419080661243783, 25.70428587859928982, -13.30723349455869098 ) ) ;
#37584=DIRECTION ( 'NONE',  ( -0.000000000000000000, 1.000000000000000000, 0.000000000000000000 ) ) ;
#37587=CARTESIAN_POINT ( 'NONE',  ( 5.454472066463755375, 54.16644935941751271, 6.039397278010941505 ) ) ;
#37590=CARTESIAN_POINT ( 'NONE',  ( -29.68315524077004497, 8.302504244945346557, -42.10535821593474282 ) ) ;
#37604=CARTESIAN_POINT ( 'NONE',  ( -9.169258015245434379, 51.60721829683665618, 1.678621333424785700 ) ) ;
#37616=B_SPLINE_CURVE_WITH_KNOTS ( 'NONE', 3,
 ( #34175, #67053, #64921, #40634, #7204, #32040, #99930, #26105, #58962, #81091, #106420, #40112, #72988, #105894, #48713, #81601, #7728, #73519, #20132, #68658, #68097, #17973 ),
 .UNSPECIFIED., .F., .F.,
 ( 4, 2, 2, 2, 2, 2, 2, 2, 2, 2, 4 ),
 ( 0.007323666553981427081, 0.007826507932084076496, 0.008329349310186726779, 0.008580769999238053655, 0.008832190688289378797, 0.009335032066392032549, 0.009586452755443361159, 0.009837873444494689770, 0.01034071482259735220, 0.01084355620070001636, 0.01134639757880268052 ),
 .UNSPECIFIED. ) ;
#37629=FACE_BOUND ( 'NONE', #237, .T. ) ;
#37656=DIRECTION ( 'NONE',  ( 0.000000000000000000, 0.000000000000000000, 1.000000000000000000 ) ) ;
#37660=EDGE_CURVE ( 'NONE', #64333, #1743, #72116, .T. ) ;
#37668=ORIENTED_EDGE ( 'NONE', *, *, #19932, .F. ) ;
#37686=CARTESIAN_POINT ( 'NONE',  ( 0.2952253681877878844, 13.62314717402266062, -49.28328918176131879 ) ) ;
#37690=EDGE_LOOP ( 'NONE', ( #70194, #92761, #8550, #25656 ) ) ;
#37739=CARTESIAN_POINT ( 'NONE',  ( -49.13349184603291775, 7.785586125543571434, 16.19411946323684859 ) ) ;
#37777=FACE_OUTER_BOUND ( 'NONE', #40657, .T. ) ;
#37782=ADVANCED_FACE ( 'NONE', ( #55386 ), #88316, .F. ) ;
#37811=CARTESIAN_POINT ( 'NONE',  ( -1.102331679451517221, 51.47917464568522661, 9.610681418731136461 ) ) ;
#37829=CARTESIAN_POINT ( 'NONE',  ( -0.8583531473660760414, 8.496822302985666653, 51.42805900925117868 ) ) ;
#37832=ORIENTED_EDGE ( 'NONE', *, *, #43975, .T. ) ;
#37843=CARTESIAN_POINT ( 'NONE',  ( -16.34139928092842098, 35.06236595198802775, 21.87332501390299555 ) ) ;
#37855=SURFACE_SIDE_STYLE ('',( #78790 ) ) ;
#37856=AXIS2_PLACEMENT_3D ( 'NONE', #3490, #26737, #77374 ) ;
#37874=MECHANICAL_DESIGN_GEOMETRIC_PRESENTATION_REPRESENTATION('',(#80935),#44776);
#37881=AXIS2_PLACEMENT_3D ( 'NONE', #78231, #32219, #39781 ) ;
#37887=ORIENTED_EDGE ( 'NONE', *, *, #10500, .F. ) ;
#37891=ADVANCED_FACE ( 'NONE', ( #91374 ), #50351, .F. ) ;
#37898=CARTESIAN_POINT ( 'NONE',  ( -28.35175412354155355, 34.21502232083763317, 8.615583304109071250 ) ) ;
#37900=CARTESIAN_POINT ( 'NONE',  ( -48.02835407290534420, -1.200000000000000030E-05, -15.60535821593460248 ) ) ;
#37977=ADVANCED_FACE ( 'NONE', ( #3421 ), #67629, .F. ) ;
#37989=CARTESIAN_POINT ( 'NONE',  ( 9.177423055815349784, 46.16989776044872684, -13.55706802408399980 ) ) ;
#38068=FILL_AREA_STYLE ('',( #79017 ) ) ;
#38085=CARTESIAN_POINT ( 'NONE',  ( 23.54225815529381904, 28.03385386361088649, -30.74635459162673357 ) ) ;
#38088=( NAMED_UNIT ( * ) SI_UNIT ( $, .STERADIAN. ) SOLID_ANGLE_UNIT ( ) );
#38102=ORIENTED_EDGE ( 'NONE', *, *, #1086, .T. ) ;
#38105=ORIENTED_EDGE ( 'NONE', *, *, #31173, .F. ) ;
#38116=DIRECTION ( 'NONE',  ( -0.000000000000000000, 1.000000000000000000, -0.000000000000000000 ) ) ;
#38122=CARTESIAN_POINT ( 'NONE',  ( -16.64348903516521005, 43.47556584774768140, -6.657797401561535544 ) ) ;
#38179=VERTEX_POINT ( 'NONE', #97714 ) ;
#38208=CARTESIAN_POINT ( 'NONE',  ( 16.91657744243869743, 36.34978592707985712, 24.30698433968583672 ) ) ;
#38224=EDGE_CURVE ( 'NONE', #41320, #27731, #100381, .T. ) ;
#38259=CARTESIAN_POINT ( 'NONE',  ( -48.55208739724533729, 8.680497950467669810, 16.74317141725358127 ) ) ;
#38265=CARTESIAN_POINT ( 'NONE',  ( 29.68315524077034340, 13.12249633091093415, 39.60535821593451544 ) ) ;
#38289=ORIENTED_EDGE ( 'NONE', *, *, #72519, .T. ) ;
#38297=CARTESIAN_POINT ( 'NONE',  ( 7.681258945454893382E-14, -1.200000000000000030E-05, 39.50000000000000000 ) ) ;
#38312=CARTESIAN_POINT ( 'NONE',  ( 15.89370886130898164, 45.88935169965960625, -6.420701231162496470 ) ) ;
#38316=( NAMED_UNIT ( * ) PLANE_ANGLE_UNIT ( ) SI_UNIT ( $, .RADIAN. ) );
#38328=CARTESIAN_POINT ( 'NONE',  ( -30.63818566637198515, 16.09127295623279608, -40.04027533505464476 ) ) ;
#38329=ORIENTED_EDGE ( 'NONE', *, *, #31070, .F. ) ;
#38345=ORIENTED_EDGE ( 'NONE', *, *, #79970, .F. ) ;
#38368=CARTESIAN_POINT ( 'NONE',  ( 0.000000000000000000, 45.89575828009193259, 0.000000000000000000 ) ) ;
#38371=( NAMED_UNIT ( * ) SI_UNIT ( $, .STERADIAN. ) SOLID_ANGLE_UNIT ( ) );
#38374=EDGE_CURVE ( 'NONE', #20894, #68049, #98408, .T. ) ;
#38376=FACE_OUTER_BOUND ( 'NONE', #56762, .T. ) ;
#38377=VERTEX_POINT ( 'NONE', #30527 ) ;
#38385=CARTESIAN_POINT ( 'NONE',  ( 17.97922351027873589, 34.27503843121980509, 23.34624828125660656 ) ) ;
#38387=FILL_AREA_STYLE ('',( #69672 ) ) ;
#38413=SHAPE_REPRESENTATION ( '11. Strainer', ( #10728 ), #105516 ) ;
#38424=CARTESIAN_POINT ( 'NONE',  ( 16.91742856729430855, 34.95464097504886780, -21.80698433968623462 ) ) ;
#38436=CARTESIAN_POINT ( 'NONE',  ( 0.000000000000000000, 0.000000000000000000, 0.000000000000000000 ) ) ;
#38451=CARTESIAN_POINT ( 'NONE',  ( 11.48443175375249048, 45.38933445805910338, -14.52341122396187423 ) ) ;
#38453=CARTESIAN_POINT ( 'NONE',  ( 47.06916318994454684, 18.66170694578125477, -14.79344423761990512 ) ) ;
#38476=LINE ( 'NONE', #87024, #94834 ) ;
#38479=CARTESIAN_POINT ( 'NONE',  ( -48.02835407290534420, 16.78162100668604495, -14.35535821593460248 ) ) ;
#38482=CARTESIAN_POINT ( 'NONE',  ( 28.09972863518510877, 34.19584976912102547, -9.568757885759717752 ) ) ;
#38487=FACE_OUTER_BOUND ( 'NONE', #105089, .T. ) ;
#38505=CARTESIAN_POINT ( 'NONE',  ( -38.50768004163307978, 27.33171274800497130, -13.03328602146359039 ) ) ;
#38509=CARTESIAN_POINT ( 'NONE',  ( 11.24762705481944813, 45.31580660681511574, 14.96115168073759705 ) ) ;
#38526=( GEOMETRIC_REPRESENTATION_CONTEXT ( 3 ) GLOBAL_UNCERTAINTY_ASSIGNED_CONTEXT ( ( #51020 ) ) GLOBAL_UNIT_ASSIGNED_CONTEXT ( ( #22106, #56008, #54961 ) ) REPRESENTATION_CONTEXT ( 'NONE', 'WORKASPACE' ) );
#38531=CARTESIAN_POINT ( 'NONE',  ( 11.48415166351361627, 43.26076767676408963, 14.52437360466608141 ) ) ;
#38588=VERTEX_POINT ( 'NONE', #93526 ) ;
#38598=SURFACE_STYLE_FILL_AREA ( #77450 ) ;
#38643=CARTESIAN_POINT ( 'NONE',  ( 47.77471032523678218, 17.34854710534463962, 14.37330285161466392 ) ) ;
#38665=SURFACE_STYLE_FILL_AREA ( #21961 ) ;
#38680=CARTESIAN_POINT ( 'NONE',  ( 26.94507904750826555, 34.81440208126156932, 7.556984339685686614 ) ) ;
#38687=ORIENTED_EDGE ( 'NONE', *, *, #98491, .T. ) ;
#38702=EDGE_LOOP ( 'NONE', ( #44361, #8129, #51771, #58147 ) ) ;
#38719=CYLINDRICAL_SURFACE ( 'NONE', #85738, 1.249999999999999334 ) ;
#38735=CARTESIAN_POINT ( 'NONE',  ( -28.20057399694874078, 36.30547655367008275, 9.431994021286264740 ) ) ;
#38757=EDGE_CURVE ( 'NONE', #84082, #78054, #51844, .T. ) ;
#38763=LINE ( 'NONE', #72698, #14007 ) ;
#38771=CARTESIAN_POINT ( 'NONE',  ( -38.80477841475464373, 27.34308269247116741, 12.01489659479609351 ) ) ;
#38775=EDGE_CURVE ( 'NONE', #46516, #22672, #4133, .T. ) ;
#38799=VERTEX_POINT ( 'NONE', #4666 ) ;
#38810=MECHANICAL_DESIGN_GEOMETRIC_PRESENTATION_REPRESENTATION('',(#21585),#87026);
#38832=CARTESIAN_POINT ( 'NONE',  ( 1.219735312445022535, 27.62936970793004576, -39.81700975820285748 ) ) ;
#38841=CARTESIAN_POINT ( 'NONE',  ( -30.29343180852501050, 12.93058661249364327, -41.94895705695265775 ) ) ;
#38853=CARTESIAN_POINT ( 'NONE',  ( -0.3344035310850524412, 34.18675715969972373, 29.70737310419187693 ) ) ;
#38855=B_SPLINE_CURVE_WITH_KNOTS ( 'NONE', 3,
 ( #10942, #76755, #26141, #2863, #67623, #26658, #101576, #92405, #18554, #51417, #19644, #43340, #76223, #52477, #85395, #28254, #3415, #29840, #78880, #12543, #5527, #38453, #85948, #104213, #45478, #11478, #36357, #87000, #71319, #69226 ),
 .UNSPECIFIED., .F., .F.,
 ( 4, 2, 2, 2, 2, 2, 2, 2, 2, 2, 2, 2, 2, 2, 4 ),
 ( 0.002924093377768722125, 0.003854458377716627783, 0.004784823377664528671, 0.005715188377612428691, 0.006180370877586383906, 0.006645553377560339120, 0.007110735877534295202, 0.007343327127521271508, 0.007575918377508249549, 0.007808509627495227590, 0.008041100877482207365, 0.008506283377456165182, 0.008971465877430122998, 0.009436648377404082549, 0.01036701337735199818 ),
 .UNSPECIFIED. ) ;
#38874=CARTESIAN_POINT ( 'NONE',  ( -16.58664841766668019, 35.02554381010406814, 21.81514337942032355 ) ) ;
#38880=EDGE_CURVE ( 'NONE', #6938, #62849, #95800, .T. ) ;
#38908=SURFACE_STYLE_USAGE ( .BOTH. , #16737 ) ;
#38916=CARTESIAN_POINT ( 'NONE',  ( -28.45500467043791204, 17.07616014098841362, -41.11859397474302114 ) ) ;
#38917=CARTESIAN_POINT ( 'NONE',  ( 27.10511071441197117, -1.200000000000000030E-05, 7.556984339685704377 ) ) ;
#38931=DIRECTION ( 'NONE',  ( 0.000000000000000000, 0.000000000000000000, 1.000000000000000000 ) ) ;
#38937=CARTESIAN_POINT ( 'NONE',  ( 6.542049517734651154, 53.55479212070640926, -7.321410255469364081 ) ) ;
#38970=CARTESIAN_POINT ( 'NONE',  ( 11.27392099353245669, 45.76150927139935476, -13.37519430359090755 ) ) ;
#38977=CARTESIAN_POINT ( 'NONE',  ( -5.910549702781506376, 54.01482550163699869, -6.184394181519167866 ) ) ;
#38995=FACE_BOUND ( 'NONE', #33868, .T. ) ;
#39032=CARTESIAN_POINT ( 'NONE',  ( 11.38830949524109215, 45.34487012134832185, 14.75357462089488259 ) ) ;
#39036=VECTOR ( 'NONE', #84165, 1000.000000000000227 ) ;
#39049=CARTESIAN_POINT ( 'NONE',  ( 1.220787089173188678, 51.58155239968396444, -9.312747329387569550 ) ) ;
#39064=CARTESIAN_POINT ( 'NONE',  ( -26.12445749286578334, 36.99838226188546741, -9.598433884020590057 ) ) ;
#39072=DIRECTION ( 'NONE',  ( -0.000000000000000000, 1.000000000000000000, -0.000000000000000000 ) ) ;
#39099=CARTESIAN_POINT ( 'NONE',  ( 9.491091496279695579E-16, 54.30758622938872549, 7.749999999999999112 ) ) ;
#39114=SURFACE_STYLE_FILL_AREA ( #80075 ) ;
#39115=B_SPLINE_CURVE_WITH_KNOTS ( 'NONE', 3,
 ( #59306, #35050, #43112, #3184, #85163, #75999, #28554, #11250, #93255, #93792, #85715, #19419, #61437, #67915, #10722, #2636, #92176, #27505, #51180, #59845, #84101, #3725 ),
 .UNSPECIFIED., .F., .F.,
 ( 4, 2, 2, 2, 2, 2, 2, 2, 2, 2, 4 ),
 ( 0.007089767286567579853, 0.007341907183935019073, 0.007594047081302459160, 0.008098326876037337599, 0.008350466773404773349, 0.008602606670772209099, 0.009106886465507085804, 0.009611166260241964243, 0.01011544605497684095, 0.01061972584971171939, 0.01112400564444659609 ),
 .UNSPECIFIED. ) ;
#39128=CARTESIAN_POINT ( 'NONE',  ( -0.4146333384834792746, 43.19860944066726205, -18.68223018281585368 ) ) ;
#39130=PRESENTATION_STYLE_ASSIGNMENT (( #97867 ) ) ;
#39137=CARTESIAN_POINT ( 'NONE',  ( 22.19904875965656643, 26.05953402208906411, -31.21225605184647378 ) ) ;
#39145=EDGE_LOOP ( 'NONE', ( #22868, #35040, #50629, #99917 ) ) ;
#39148=CARTESIAN_POINT ( 'NONE',  ( -36.37624454313544220, 28.20756701710648784, 11.81579238979949587 ) ) ;
#39150=CARTESIAN_POINT ( 'NONE',  ( 8.559508646656349029, 51.83514083332403999, -1.531152949374623873 ) ) ;
#39169=ORIENTED_EDGE ( 'NONE', *, *, #54674, .T. ) ;
#39177=SURFACE_STYLE_USAGE ( .BOTH. , #47238 ) ;
#39178=STYLED_ITEM ( 'NONE', ( #75617 ), #66937 ) ;
#39200=( GEOMETRIC_REPRESENTATION_CONTEXT ( 3 ) GLOBAL_UNCERTAINTY_ASSIGNED_CONTEXT ( ( #6190 ) ) GLOBAL_UNIT_ASSIGNED_CONTEXT ( ( #101582, #51423, #26663 ) ) REPRESENTATION_CONTEXT ( 'NONE', 'WORKASPACE' ) );
#39212=CARTESIAN_POINT ( 'NONE',  ( 26.01891250190696425, 35.07265168611927209, 8.182742802489435974 ) ) ;
#39243=CARTESIAN_POINT ( 'NONE',  ( 3.616665348617805752E-21, 26.07813853931757464, -38.25000000000000000 ) ) ;
#39250=CARTESIAN_POINT ( 'NONE',  ( -0.08425897456643699490, 34.17188553058037570, -29.74999999999992184 ) ) ;
#39254=CARTESIAN_POINT ( 'NONE',  ( -1.106403059298377123, 17.29028464265184795, 49.90220135503628285 ) ) ;
#39255=( NAMED_UNIT ( * ) SI_UNIT ( $, .STERADIAN. ) SOLID_ANGLE_UNIT ( ) );
#39271=FACE_OUTER_BOUND ( 'NONE', #82578, .T. ) ;
#39275=EDGE_LOOP ( 'NONE', ( #58644, #98220, #43426, #62949 ) ) ;
#39302=MECHANICAL_DESIGN_GEOMETRIC_PRESENTATION_REPRESENTATION('',(#54739),#75376);
#39312=CARTESIAN_POINT ( 'NONE',  ( 29.07948315939635719, 13.68628896012809903, 39.75806671536113157 ) ) ;
#39316=CARTESIAN_POINT ( 'NONE',  ( 28.46814188645437582, 18.16755603797503937, 40.55128649371861371 ) ) ;
#39321=LINE ( 'NONE', #63053, #18995 ) ;
#39324=DIRECTION ( 'NONE',  ( -0.000000000000000000, 1.000000000000000000, -0.000000000000000000 ) ) ;
#39348=CARTESIAN_POINT ( 'NONE',  ( -7.435027261853919711, 54.30343294327740722, -2.228677732260373912 ) ) ;
#39360=( NAMED_UNIT ( * ) SI_UNIT ( $, .STERADIAN. ) SOLID_ANGLE_UNIT ( ) );
#39366=CARTESIAN_POINT ( 'NONE',  ( -0.6457708876286766264, 25.22709477130971933, 40.58338319097169489 ) ) ;
#39389=CARTESIAN_POINT ( 'NONE',  ( 4.726289671093704570, 52.17352334379410905, -6.162350474469696415 ) ) ;
#39395=CARTESIAN_POINT ( 'NONE',  ( -0.5285826653655552043, 13.43369763208850287, 49.36091062968711896 ) ) ;
#39404=DIRECTION ( 'NONE',  ( 0.000000000000000000, 0.000000000000000000, 1.000000000000000000 ) ) ;
#39405=CARTESIAN_POINT ( 'NONE',  ( 22.66566284726422964, 27.53292244466711480, 33.08065323819726444 ) ) ;
#39411=CARTESIAN_POINT ( 'NONE',  ( -16.10958011051322814, 35.08395293542164950, 21.97156943567877718 ) ) ;
#39434=B_SPLINE_CURVE_WITH_KNOTS ( 'NONE', 3,
 ( #44947, #52471, #34747, #67619, #3410, #100496, #76750, #61119, #68692, #2857, #84325, #85392, #43335, #77830, #20169, #59532, #76217, #10936, #53549, #44400 ),
 .UNSPECIFIED., .F., .F.,
 ( 4, 2, 2, 2, 2, 2, 2, 2, 2, 4 ),
 ( 0.007283033696500349971, 0.007786984348840834957, 0.008290935001181318209, 0.008794885653521803195, 0.009298836305862288182, 0.009802786958202773168, 0.01030673761054325815, 0.01081068826288374141, 0.01106266358905398303, 0.01131463891522422639 ),
 .UNSPECIFIED. ) ;
#39447=CARTESIAN_POINT ( 'NONE',  ( 1.092184909756600097, 25.84081523104171652, 38.88672836633164565 ) ) ;
#39452=CARTESIAN_POINT ( 'NONE',  ( -29.68315524077005207, 13.47185074185902209, -42.10535821593474282 ) ) ;
#39457=CARTESIAN_POINT ( 'NONE',  ( 23.62759301673245815, 25.18629740126316818, 33.13999265739832367 ) ) ;
#39478=SURFACE_SIDE_STYLE ('',( #73937 ) ) ;
#39486=PRESENTATION_STYLE_ASSIGNMENT (( #71300 ) ) ;
#39505=CARTESIAN_POINT ( 'NONE',  ( 0.000000000000000000, 29.08768991669519721, 35.82893434829263413 ) ) ;
#39512=CARTESIAN_POINT ( 'NONE',  ( -5.372766443841437756, 53.45888839938537274, -8.531152949374524397 ) ) ;
#39524=EDGE_LOOP ( 'NONE', ( #56669, #55377 ) ) ;
#39535=CARTESIAN_POINT ( 'NONE',  ( -48.48434714564471193, 13.98045800628875313, -16.77138779655891909 ) ) ;
#39563=CARTESIAN_POINT ( 'NONE',  ( -37.72547481417448978, 27.55009981184272760, -13.45617127781033417 ) ) ;
#39566=CARTESIAN_POINT ( 'NONE',  ( -0.6254118074930600235, 13.29657844059611449, -51.58631799359783798 ) ) ;
#39570=CARTESIAN_POINT ( 'NONE',  ( 11.54075930460769506, 45.44590361214169150, 14.27956357151531286 ) ) ;
#39577=LINE ( 'NONE', #95674, #92958 ) ;
#39583=CARTESIAN_POINT ( 'NONE',  ( 0.7783529810093747781, 51.35606173618085535, -9.981590251641023315 ) ) ;
#39586=CARTESIAN_POINT ( 'NONE',  ( 4.278555824747665604, 52.15500882501390123, 6.542026809210045535 ) ) ;
#39590=CARTESIAN_POINT ( 'NONE',  ( 11.38597746671299582, 43.57657614512142175, 13.48406053558915119 ) ) ;
#39624=CARTESIAN_POINT ( 'NONE',  ( -23.05251019904581611, 27.41544800856653552, 33.20617127781058286 ) ) ;
#39626=EDGE_CURVE ( 'NONE', #52941, #68169, #22192, .T. ) ;
#39630=EDGE_LOOP ( 'NONE', ( #93928, #26655 ) ) ;
#39634=DIRECTION ( 'NONE',  ( 4.738110706560371839E-17, -0.9221233147934838614, 0.3868961001538753219 ) ) ;
#39647=SURFACE_SIDE_STYLE ('',( #81644 ) ) ;
#39648=CARTESIAN_POINT ( 'NONE',  ( 1.127244920694520092, 34.38903298460757441, 29.13254641235529263 ) ) ;
#39655=CARTESIAN_POINT ( 'NONE',  ( -23.86015722654359195, 25.16617832201437110, 33.04145880079988729 ) ) ;
#39658=CARTESIAN_POINT ( 'NONE',  ( -1.249340999377952510, 43.67393701204134260, -17.33575850031895271 ) ) ;
#39664=CARTESIAN_POINT ( 'NONE',  ( 22.22683576871073186, 25.59856940243015799, -32.73475386601680270 ) ) ;
#39667=CARTESIAN_POINT ( 'NONE',  ( 47.57472544752255317, 12.59044387134409071, -14.43844179794168880 ) ) ;
#39674=CARTESIAN_POINT ( 'NONE',  ( -36.56688176566701287, 28.18335144162340811, 11.43747163042122494 ) ) ;
#39691=STYLED_ITEM ( 'NONE', ( #78058 ), #80013 ) ;
#39698=CARTESIAN_POINT ( 'NONE',  ( 46.92723468898980599, 18.82863087225951304, 15.00902207511731667 ) ) ;
#39699=CARTESIAN_POINT ( 'NONE',  ( 6.536669471946908949, 51.40519842345576507, -7.404314278401480820 ) ) ;
#39720=CYLINDRICAL_SURFACE ( 'NONE', #72206, 1.250000000000001110 ) ;
#39721=DIRECTION ( 'NONE',  ( -0.000000000000000000, 1.000000000000000000, -0.000000000000000000 ) ) ;
#39741=CARTESIAN_POINT ( 'NONE',  ( -0.7873503183212902101, 53.48327185720855681, -9.984552898249470232 ) ) ;
#39747=( NAMED_UNIT ( * ) SI_UNIT ( $, .STERADIAN. ) SOLID_ANGLE_UNIT ( ) );
#39760=VERTEX_POINT ( 'NONE', #53748 ) ;
#39769=CARTESIAN_POINT ( 'NONE',  ( 1.100317426399643139, 25.84114585796975305, -38.88560695975913006 ) ) ;
#39781=DIRECTION ( 'NONE',  ( 0.000000000000000000, 0.000000000000000000, 1.000000000000000000 ) ) ;
#39790=CARTESIAN_POINT ( 'NONE',  ( 2.470381878726035567E-14, 18.87382441218300144, 49.24999999999992184 ) ) ;
#39797=CARTESIAN_POINT ( 'NONE',  ( 23.05330517246050448, 26.02474360266739595, 30.70617127781016364 ) ) ;
#39810=CARTESIAN_POINT ( 'NONE',  ( 10.12102021413156905, 45.41888843717377000, -15.40779740156171762 ) ) ;
#39812=CARTESIAN_POINT ( 'NONE',  ( -28.18119922952890377, 34.32264690212790015, -8.150096433134891072 ) ) ;
#39826=PRESENTATION_STYLE_ASSIGNMENT (( #90490 ) ) ;
#39835=CARTESIAN_POINT ( 'NONE',  ( -16.64348903516521005, 45.88445698070336221, -4.157797401561533768 ) ) ;
#39837=CYLINDRICAL_SURFACE ( 'NONE', #4529, 1.250000000000000000 ) ;
#39862=CARTESIAN_POINT ( 'NONE',  ( 10.45316333433563649, 43.22580471055811557, -15.39941299950120523 ) ) ;
#39870=CARTESIAN_POINT ( 'NONE',  ( -17.27438113373179362, 45.65101552804006246, 4.281429632575695976 ) ) ;
#39872=ORIENTED_EDGE ( 'NONE', *, *, #66370, .F. ) ;
#39875=EDGE_CURVE ( 'NONE', #63425, #87056, #41319, .T. ) ;
#39877=SURFACE_SIDE_STYLE ('',( #31280 ) ) ;
#39885=CARTESIAN_POINT ( 'NONE',  ( -0.08410583490319520350, 26.07813853931757464, 38.25000000000002132 ) ) ;
#39892=EDGE_LOOP ( 'NONE', ( #72432, #74673 ) ) ;
#39896=CARTESIAN_POINT ( 'NONE',  ( -17.46661644397501689, 43.23536754299439622, 6.352185647016465708 ) ) ;
#39899=CARTESIAN_POINT ( 'NONE',  ( 48.91605700228181064, 13.22299455561256387, 16.49079035033173568 ) ) ;
#39915=CARTESIAN_POINT ( 'NONE',  ( 8.559508646656405872, 51.55638410492942825, 4.031152949374444461 ) ) ;
#39928=CARTESIAN_POINT ( 'NONE',  ( -16.75187969033532553, 34.25544727262118982, 24.30698433968612449 ) ) ;
#39952=CARTESIAN_POINT ( 'NONE',  ( 37.40771152851837655, 27.94111240654205730, 10.95617127780990607 ) ) ;
#39956=CARTESIAN_POINT ( 'NONE',  ( 27.10511071441176156, 34.47735702144343861, -10.05698433968637673 ) ) ;
#39959=CARTESIAN_POINT ( 'NONE',  ( -28.43259016867738609, 12.18852863928159991, -40.99039043055300624 ) ) ;
#39960=EDGE_CURVE ( 'NONE', #15279, #67879, #26358, .T. ) ;
#39961=ORIENTED_EDGE ( 'NONE', *, *, #54374, .F. ) ;
#39970=DIRECTION ( 'NONE',  ( 0.000000000000000000, 1.000000000000000000, 0.000000000000000000 ) ) ;
#39989=CARTESIAN_POINT ( 'NONE',  ( 29.68315524076926692, 13.47185074185900255, -42.10535821593530414 ) ) ;
#40021=CARTESIAN_POINT ( 'NONE',  ( -10.61653353389834464, 45.33051817006433737, 15.36625836153905489 ) ) ;
#40023=CARTESIAN_POINT ( 'NONE',  ( 11.53815258514788411, 45.46891437459016316, -14.20004885619772139 ) ) ;
#40045=FACE_OUTER_BOUND ( 'NONE', #64033, .T. ) ;
#40052=VECTOR ( 'NONE', #99099, 1000.000000000000114 ) ;
#40054=CARTESIAN_POINT ( 'NONE',  ( -16.64348903516517098, 43.47556584774767430, 6.657797401561654560 ) ) ;
#40056=ORIENTED_EDGE ( 'NONE', *, *, #42504, .F. ) ;
#40063=CARTESIAN_POINT ( 'NONE',  ( -22.57912246414728585, 28.20550200792851214, -30.87816999938245033 ) ) ;
#40085=PRESENTATION_STYLE_ASSIGNMENT (( #23395 ) ) ;
#40096=CARTESIAN_POINT ( 'NONE',  ( 0.1698589296850801789, 52.17552313485973770, -7.758756120565298176 ) ) ;
#40109=CARTESIAN_POINT ( 'NONE',  ( -26.78668668169135358, 36.71437112124606017, -10.05698433968604810 ) ) ;
#40112=CARTESIAN_POINT ( 'NONE',  ( -9.807649484915852867, 51.30023088812457388, -2.672895936288036012 ) ) ;
#40122=( GEOMETRIC_REPRESENTATION_CONTEXT ( 3 ) GLOBAL_UNCERTAINTY_ASSIGNED_CONTEXT ( ( #3909 ) ) GLOBAL_UNIT_ASSIGNED_CONTEXT ( ( #80965, #105781, #90135 ) ) REPRESENTATION_CONTEXT ( 'NONE', 'WORKASPACE' ) );
#40129=ORIENTED_EDGE ( 'NONE', *, *, #59618, .F. ) ;
#40131=ADVANCED_FACE ( 'NONE', ( #33625 ), #39720, .F. ) ;
#40148=VECTOR ( 'NONE', #56346, 1000.000000000000000 ) ;
#40150=CARTESIAN_POINT ( 'NONE',  ( 0.7831191144357741996, 34.98236821775393679, 27.51229094925169605 ) ) ;
#40159=CARTESIAN_POINT ( 'NONE',  ( 23.29992259251640263, 27.36384728240175690, -33.20617127781078892 ) ) ;
#40165=( NAMED_UNIT ( * ) SI_UNIT ( $, .STERADIAN. ) SOLID_ANGLE_UNIT ( ) );
#40176=CARTESIAN_POINT ( 'NONE',  ( 46.83547786243074285, 13.71028427728499466, -15.22387951582032528 ) ) ;
#40179=EDGE_LOOP ( 'NONE', ( #36355, #31111, #100206, #101943 ) ) ;
#40181=SURFACE_STYLE_USAGE ( .BOTH. , #81162 ) ;
#40186=LINE ( 'NONE', #31082, #10555 ) ;
#40188=CARTESIAN_POINT ( 'NONE',  ( 30.90685644053189662, 9.526079354490885720, 40.57200395206826471 ) ) ;
#40191=CARTESIAN_POINT ( 'NONE',  ( -27.10511071441183262, 36.88665068479722464, 7.556984339686156460 ) ) ;
#40207=EDGE_CURVE ( 'NONE', #95054, #56223, #77448, .T. ) ;
#40217=ADVANCED_FACE ( 'NONE', ( #77792, #76710, #28214, #101532, #35776 ), #48082, .T. ) ;
#40224=MECHANICAL_DESIGN_GEOMETRIC_PRESENTATION_REPRESENTATION('',(#7476),#85053);
#40237=CARTESIAN_POINT ( 'NONE',  ( 6.308797461351612235, 53.41353044709899933, 8.024790098550512951 ) ) ;
#40249=B_SPLINE_CURVE_WITH_KNOTS ( 'NONE', 3,
 ( #64486, #81686, #24049, #33717, #40716, #57417, #106509, #65537, #23509, #56353, #41784, #48269, #66594, #98424, #82776, #81170, #74140, #89289, #25098, #88750, #15383, #24575, #225, #47739, #16444, #49328 ),
 .UNSPECIFIED., .F., .F.,
 ( 4, 2, 2, 2, 2, 2, 2, 2, 2, 2, 2, 2, 4 ),
 ( 0.002887119676744016351, 0.003139154421792429879, 0.003391189166840843407, 0.003895258656937666125, 0.004399328147034487976, 0.004903397637131310695, 0.005155432382179719018, 0.005407467127228127342, 0.005659501872276535665, 0.005911536617324943121, 0.006415606107421763238, 0.006667640852470176765, 0.006919675597518590293 ),
 .UNSPECIFIED. ) ;
#40251=CARTESIAN_POINT ( 'NONE',  ( 15.54299285489016391, 34.77154309520251019, 23.41290371719734509 ) ) ;
#40266=ORIENTED_EDGE ( 'NONE', *, *, #20083, .F. ) ;
#40267=CONICAL_SURFACE ( 'NONE', #71222, 45.10524579772351217, 0.3972631705159501148 ) ;
#40271=CYLINDRICAL_SURFACE ( 'NONE', #89671, 1.250000000000001110 ) ;
#40284=DIRECTION ( 'NONE',  ( 0.000000000000000000, 1.000000000000000000, 0.000000000000000000 ) ) ;
#40307=EDGE_LOOP ( 'NONE', ( #20435, #101760, #106414, #49531 ) ) ;
#40318=CARTESIAN_POINT ( 'NONE',  ( 48.02835407290544367, 14.94086294439726892, 16.85535821593427386 ) ) ;
#40325=CARTESIAN_POINT ( 'NONE',  ( -27.85246203510405394, 34.47333191833108401, -7.792023951491530376 ) ) ;
#40351=CARTESIAN_POINT ( 'NONE',  ( 28.58355031030010096, 11.06033896639477732, 41.46143022647122933 ) ) ;
#40353=CARTESIAN_POINT ( 'NONE',  ( 28.62002530331290018, 18.65065574497674206, 40.19565755993141210 ) ) ;
#40358=CARTESIAN_POINT ( 'NONE',  ( -28.56372199056537298, 18.54333498561203442, 40.29094744152372698 ) ) ;
#40360=CARTESIAN_POINT ( 'NONE',  ( -28.35805447588125361, 36.30513988744195331, -8.950293267375700523 ) ) ;
#40374=B_SPLINE_CURVE_WITH_KNOTS ( 'NONE', 3,
 ( #83741, #49247, #76185, #82152, #35233, #17975, #74057, #66509, #57870, #27157, #92903, #68099, #60045, #75112, #8265, #145, #33112, #99932 ),
 .UNSPECIFIED., .F., .F.,
 ( 4, 2, 2, 2, 2, 2, 2, 2, 4 ),
 ( 0.004289890562715018008, 0.005298017633127179507, 0.005550049400730218581, 0.005802081168333258522, 0.006306144703539339272, 0.006810208238745420889, 0.007314271773951502506, 0.007818335309157584123, 0.008322398844363665740 ),
 .UNSPECIFIED. ) ;
#40378=CARTESIAN_POINT ( 'NONE',  ( 10.36885343410368243, 43.24044830979637766, -15.40779740156171940 ) ) ;
#40385=FILL_AREA_STYLE_COLOUR ( '', #45732 ) ;
#40386=CARTESIAN_POINT ( 'NONE',  ( -47.14735620107897773, 13.37129584416856964, 14.71343070694194921 ) ) ;
#40392=ADVANCED_FACE ( 'NONE', ( #14614 ), #105761, .T. ) ;
#40394=DIRECTION ( 'NONE',  ( 0.000000000000000000, 0.000000000000000000, 1.000000000000000000 ) ) ;
#40417=CARTESIAN_POINT ( 'NONE',  ( -17.89483185117538255, 43.18956583916507697, 5.468282401795739212 ) ) ;
#40419=CARTESIAN_POINT ( 'NONE',  ( -23.21751746555280249, 28.11705169068991239, -30.70617127781034839 ) ) ;
#40423=CARTESIAN_POINT ( 'NONE',  ( -8.559508646656370345, 51.55638410492942114, 4.031152949374564365 ) ) ;
#40428=CARTESIAN_POINT ( 'NONE',  ( -28.43271360265415382, 12.18326821505116619, 40.99299228862962252 ) ) ;
#40434=CARTESIAN_POINT ( 'NONE',  ( 9.181445049447248152, 51.37268433381575505, 3.877508282323112621 ) ) ;
#40438=CARTESIAN_POINT ( 'NONE',  ( 28.23197554257926711, 34.17505064455689023, -9.354563056550400546 ) ) ;
#40443=( LENGTH_UNIT ( ) NAMED_UNIT ( * ) SI_UNIT ( .MILLI., .METRE. ) );
#40444=CARTESIAN_POINT ( 'NONE',  ( 22.37441460685049677, 28.20471216883544230, 31.02949312230836298 ) ) ;
#40468=DIRECTION ( 'NONE',  ( -0.000000000000000000, 1.000000000000000000, 0.000000000000000000 ) ) ;
#40469=CARTESIAN_POINT ( 'NONE',  ( 8.559508646656398767, 51.83514083332404709, 1.531152949374243510 ) ) ;
#40477=CARTESIAN_POINT ( 'NONE',  ( -28.88581594204406144, 13.70410095367683567, -39.88976374582071571 ) ) ;
#40483=CARTESIAN_POINT ( 'NONE',  ( 38.17897261654190544, 25.52811330230706233, 11.10485842511383581 ) ) ;
#40504=CARTESIAN_POINT ( 'NONE',  ( -4.071242075002222904, 52.05516629550404417, 6.992118958553540153 ) ) ;
#40521=COLOUR_RGB ( '', 0.72549020, 0.75294118, 0.79215686) ;
#40522=ORIENTED_EDGE ( 'NONE', *, *, #37183, .T. ) ;
#40526=DIRECTION ( 'NONE',  ( 0.000000000000000000, 0.000000000000000000, -1.000000000000000000 ) ) ;
#40530=CARTESIAN_POINT ( 'NONE',  ( 0.000000000000000000, 0.000000000000000000, 0.000000000000000000 ) ) ;
#40544=DIRECTION ( 'NONE',  ( 0.000000000000000000, 1.000000000000000000, 0.000000000000000000 ) ) ;
#40551=CARTESIAN_POINT ( 'NONE',  ( -24.42523734047231798, 27.59258781593598542, -31.59665717925402006 ) ) ;
#40557=FILL_AREA_STYLE_COLOUR ( '', #20402 ) ;
#40590=CARTESIAN_POINT ( 'NONE',  ( -22.39889803669559143, 27.64071832785175786, -32.90416900124266419 ) ) ;
#40617=CARTESIAN_POINT ( 'NONE',  ( 0.6461105361034419348, 52.10944840786394394, -7.916821239980341929 ) ) ;
#40621=CARTESIAN_POINT ( 'NONE',  ( 48.90253429252455675, 9.379793601652295365, 14.70143532337736403 ) ) ;
#40634=CARTESIAN_POINT ( 'NONE',  ( -9.183473878344010188, 51.37213498224890884, -3.876623111190086846 ) ) ;
#40641=VECTOR ( 'NONE', #1639, 1000.000000000000000 ) ;
#40657=EDGE_LOOP ( 'NONE', ( #60850, #38102, #100325, #25181, #80044, #24265, #103956, #69783 ) ) ;
#40667=CARTESIAN_POINT ( 'NONE',  ( 27.42222224296737565, 34.64411886747944180, 7.587464081913322111 ) ) ;
#40675=VECTOR ( 'NONE', #69743, 1000.000000000000000 ) ;
#40677=EDGE_CURVE ( 'NONE', #32988, #44416, #31056, .T. ) ;
#40678=CARTESIAN_POINT ( 'NONE',  ( -17.85737165039477148, 45.30383319674704978, -5.717692534355175660 ) ) ;
#40680=ORIENTED_EDGE ( 'NONE', *, *, #57348, .T. ) ;
#40693=CARTESIAN_POINT ( 'NONE',  ( 0.6451975519659806091, 45.36065750478253733, 18.58354771593489474 ) ) ;
#40696=DIRECTION ( 'NONE',  ( 0.000000000000000000, 1.000000000000000000, 0.000000000000000000 ) ) ;
#40698=CARTESIAN_POINT ( 'NONE',  ( -10.61948831387139336, 45.32774727476011378, -15.37414989828182676 ) ) ;
#40716=CARTESIAN_POINT ( 'NONE',  ( -9.882256759026930126, 43.35737001761634701, 15.34350100720170218 ) ) ;
#40735=ORIENTED_EDGE ( 'NONE', *, *, #77992, .F. ) ;
#40737=CARTESIAN_POINT ( 'NONE',  ( 46.79057916015454310, 18.53868985150169024, 15.81409158839495355 ) ) ;
#40740=CARTESIAN_POINT ( 'NONE',  ( -48.26938392169753200, 11.04962899253378694, 14.37319483549275390 ) ) ;
#40759=CARTESIAN_POINT ( 'NONE',  ( -0.7852320185050503110, 43.98274617669912345, 16.51395379932535690 ) ) ;
#40764=CARTESIAN_POINT ( 'NONE',  ( 6.534168656350041182, 53.62238902978714350, 7.078273912249937183 ) ) ;
#40767=ORIENTED_EDGE ( 'NONE', *, *, #72982, .F. ) ;
#40774=VERTEX_POINT ( 'NONE', #5875 ) ;
#40796=LINE ( 'NONE', #58592, #89754 ) ;
#40800=CARTESIAN_POINT ( 'NONE',  ( 9.954785814282153922, 46.18621183893551319, 12.94079623093649190 ) ) ;
#40822=AXIS2_PLACEMENT_3D ( 'NONE', #90828, #97843, #57370 ) ;
#40828=CARTESIAN_POINT ( 'NONE',  ( 48.02835407290544367, 11.61227450977237829, 14.35535821593427386 ) ) ;
#40830=CARTESIAN_POINT ( 'NONE',  ( 24.00240153465340498, 25.16456132408722723, -32.94378638812468552 ) ) ;
#40838=EDGE_LOOP ( 'NONE', ( #41407, #48614, #59868, #95959 ) ) ;
#40840=CARTESIAN_POINT ( 'NONE',  ( 22.22836149987962528, 25.59762261593713362, 32.73686270175948465 ) ) ;
#40852=B_SPLINE_CURVE_WITH_KNOTS ( 'NONE', 3,
 ( #72742, #24764, #39870, #99688, #65197, #56557, #91615, #40921, #25858, #7469, #89483, #65735, #23704, #57612, #74341, #15578, #416, #91089 ),
 .UNSPECIFIED., .F., .F.,
 ( 4, 2, 2, 2, 2, 2, 2, 2, 4 ),
 ( 0.005148306559854647080, 0.006154786515368266056, 0.006658026493125077279, 0.006909646482003485059, 0.007161266470881893706, 0.007664506448638711000, 0.008167746426395530029, 0.008670986404152347324, 0.009174226381909166353 ),
 .UNSPECIFIED. ) ;
#40879=ORIENTED_EDGE ( 'NONE', *, *, #8277, .F. ) ;
#40882=CARTESIAN_POINT ( 'NONE',  ( 0.000000000000000000, 1.999999999999998224, -56.32976553137783782 ) ) ;
#40888=CARTESIAN_POINT ( 'NONE',  ( 28.52992520858397185, 16.51490304376833151, 41.35306031657900405 ) ) ;
#40891=DIRECTION ( 'NONE',  ( 0.000000000000000000, 1.000000000000000000, 0.000000000000000000 ) ) ;
#40895=SURFACE_SIDE_STYLE ('',( #58134 ) ) ;
#40896=CARTESIAN_POINT ( 'NONE',  ( -29.28883047145525609, 14.13190579697308813, 42.04354307362330445 ) ) ;
#40907=DIRECTION ( 'NONE',  ( 0.000000000000000000, 1.000000000000000000, 0.000000000000000000 ) ) ;
#40911=CARTESIAN_POINT ( 'NONE',  ( -26.03675119807346050, 34.91717499005247305, 9.460920673475355258 ) ) ;
#40920=SURFACE_STYLE_FILL_AREA ( #73266 ) ;
#40921=CARTESIAN_POINT ( 'NONE',  ( -17.88133836625035755, 45.34897204669928072, 5.215214262617849705 ) ) ;
#40935=CARTESIAN_POINT ( 'NONE',  ( -29.68315524076956535, 13.47185074185901499, 42.10535821593508388 ) ) ;
#40945=STYLED_ITEM ( 'NONE', ( #88541 ), #59141 ) ;
#40961=UNCERTAINTY_MEASURE_WITH_UNIT (LENGTH_MEASURE( 1.000000000000000082E-05 ), #24862, 'distance_accuracy_value', 'NONE');
#40963=CARTESIAN_POINT ( 'NONE',  ( -10.69671229097623666, 43.19294699247078739, -15.34145577127658910 ) ) ;
#40964=CARTESIAN_POINT ( 'NONE',  ( -28.49081357557760796, 13.12961590422141533, 40.46799408310435808 ) ) ;
#40967=ORIENTED_EDGE ( 'NONE', *, *, #100548, .T. ) ;
#40971=CARTESIAN_POINT ( 'NONE',  ( 36.49735890537233018, 28.04409535384628782, -12.85845504628349012 ) ) ;
#40976=CARTESIAN_POINT ( 'NONE',  ( 27.85332533969027580, 34.47293867589335292, -7.792939749169369712 ) ) ;
#40990=B_SPLINE_CURVE_WITH_KNOTS ( 'NONE', 3,
 ( #34364, #67239, #100116, #26282, #46533, #95620, #96156, #54072, #87014, #13084, #22290, #21239, #78363, #54596, #103706, #62731, #45495, #4485 ),
 .UNSPECIFIED., .F., .F.,
 ( 4, 2, 2, 2, 2, 2, 2, 2, 4 ),
 ( 0.007195729052339221166, 0.007698445262548230493, 0.008201161472757238086, 0.008703877682966246546, 0.009206593893175255006, 0.009709310103384263466, 0.01021202631359327193, 0.01071474252380228039, 0.01121745873401128885 ),
 .UNSPECIFIED. ) ;
#40992=CARTESIAN_POINT ( 'NONE',  ( -4.189032099075284066, 54.25756583020928048, 6.683507376862777072 ) ) ;
#40998=FACE_BOUND ( 'NONE', #22270, .T. ) ;
#41002=STYLED_ITEM ( 'NONE', ( #39486 ), #210 ) ;
#41015=EDGE_CURVE ( 'NONE', #86477, #12173, #105503, .T. ) ;
#41025=CARTESIAN_POINT ( 'NONE',  ( -28.56680886105565165, 18.54011861096317659, -40.29036177351430581 ) ) ;
#41036=ORIENTED_EDGE ( 'NONE', *, *, #61844, .T. ) ;
#41039=CARTESIAN_POINT ( 'NONE',  ( -5.290067270632216712, 51.34639538792298907, 8.531152949374556371 ) ) ;
#41043=B_SPLINE_CURVE_WITH_KNOTS ( 'NONE', 3,
 ( #41039, #1068, #98721, #16220, #50691, #34578, #66917, #24874, #84157, #58830, #25418, #49650, #91204, #40504, #82006, #16758, #8126, #83608, #8659, #17310, #57730, #73920, #90652, #4, #65841, #100328 ),
 .UNSPECIFIED., .F., .F.,
 ( 4, 2, 2, 2, 2, 2, 2, 2, 2, 2, 2, 2, 4 ),
 ( 0.002882682986932547098, 0.003134830279789356956, 0.003386977572646166813, 0.003891272158359783927, 0.004395566744073401907, 0.004899861329787020756, 0.005152008622643835384, 0.005404155915500650012, 0.005656303208357464640, 0.005908450501214278401, 0.006412745086927905055, 0.006664892379784719684, 0.006917039672641533445 ),
 .UNSPECIFIED. ) ;
#41045=CARTESIAN_POINT ( 'NONE',  ( 29.59231420605901519, 13.59660068169548275, -42.10535821593531836 ) ) ;
#41057=CARTESIAN_POINT ( 'NONE',  ( -8.559508646656389885, 51.55638410492942825, -4.031152949374503081 ) ) ;
#41087=CARTESIAN_POINT ( 'NONE',  ( -24.44497366060264909, 27.40106161504759186, -32.24452914909054613 ) ) ;
#41094=CARTESIAN_POINT ( 'NONE',  ( -23.54757723015235626, 27.32420764371298461, 33.16469143611122661 ) ) ;
#41099=AXIS2_PLACEMENT_3D ( 'NONE', #46776, #31160, #78600 ) ;
#41110=CARTESIAN_POINT ( 'NONE',  ( -49.26018567526330827, 7.766323692793265288, -15.83099189872090307 ) ) ;
#41115=CARTESIAN_POINT ( 'NONE',  ( 17.26510143360931693, 45.41334515577720055, 6.504361445977895784 ) ) ;
#41118=FACE_OUTER_BOUND ( 'NONE', #62422, .T. ) ;
#41147=CARTESIAN_POINT ( 'NONE',  ( 10.61203977153298439, 46.03732009579940865, 12.94024766200776888 ) ) ;
#41148=PRESENTATION_STYLE_ASSIGNMENT (( #67024 ) ) ;
#41164=CARTESIAN_POINT ( 'NONE',  ( 49.15082508851322984, 8.572194610415262872, 15.05005620232393859 ) ) ;
#41208=CARTESIAN_POINT ( 'NONE',  ( 16.64348903516523848, 43.47556584774768851, 6.657797401561421857 ) ) ;
#41212=CARTESIAN_POINT ( 'NONE',  ( -17.73803972846099697, 45.30907581182017907, -6.035033385463771438 ) ) ;
#41221=CARTESIAN_POINT ( 'NONE',  ( -0.6254647405162019336, 13.29659006857841952, 51.58631282303937837 ) ) ;
#41225=CARTESIAN_POINT ( 'NONE',  ( 0.7861120053659819140, 51.35458432871589451, 9.985568200469458588 ) ) ;
#41230=CARTESIAN_POINT ( 'NONE',  ( 1.168327726069034345, 14.76361700775325048, -50.96114577899942333 ) ) ;
#41237=CARTESIAN_POINT ( 'NONE',  ( 47.77591036386547074, 12.17665806217427971, -14.37301751662952931 ) ) ;
#41279=CARTESIAN_POINT ( 'NONE',  ( -16.64348903516517098, -1.200000000000000030E-05, 5.407797401561653672 ) ) ;
#41300=CARTESIAN_POINT ( 'NONE',  ( 0.6424216610451950471, 45.36344480451447936, -18.57546480763770802 ) ) ;
#41319=B_SPLINE_CURVE_WITH_KNOTS ( 'NONE', 3,
 ( #104561, #29661, #4286, #12888, #71655, #29145, #62015, #95958, #80275, #94910, #72202, #70617, #62531, #54393, #87339, #105106, #81860, #66226, #80813, #17169, #7443, #89978, #47907, #98590 ),
 .UNSPECIFIED., .F., .F.,
 ( 4, 2, 2, 2, 2, 2, 2, 2, 2, 2, 2, 4 ),
 ( 0.003034767923542890881, 0.003287523117834535193, 0.003540278312126179071, 0.003793033506417823383, 0.004045788700709467695, 0.004551299089292751981, 0.004804054283584394125, 0.005056809477876036268, 0.005562319866459323157, 0.006067830255042610046, 0.006573340643625896935, 0.007078851032209183824 ),
 .UNSPECIFIED. ) ;
#41320=VERTEX_POINT ( 'NONE', #15855 ) ;
#41332=CARTESIAN_POINT ( 'NONE',  ( 9.658640570150787141, 45.55801956750498505, 15.25085205539896727 ) ) ;
#41346=ADVANCED_FACE ( 'NONE', ( #33130 ), #91872, .F. ) ;
#41361=CARTESIAN_POINT ( 'NONE',  ( 47.14545574308352371, 12.03700443135207898, 16.50078943917342755 ) ) ;
#41373=VERTEX_POINT ( 'NONE', #24520 ) ;
#41376=PRESENTATION_STYLE_ASSIGNMENT (( #97471 ) ) ;
#41378=( NAMED_UNIT ( * ) SI_UNIT ( $, .STERADIAN. ) SOLID_ANGLE_UNIT ( ) );
#41388=STYLED_ITEM ( 'NONE', ( #28384 ), #70943 ) ;
#41407=ORIENTED_EDGE ( 'NONE', *, *, #29649, .F. ) ;
#41423=CARTESIAN_POINT ( 'NONE',  ( -23.21751746555244722, 25.25267828308493634, 33.20617127781060418 ) ) ;
#41441=CARTESIAN_POINT ( 'NONE',  ( -25.97802892056438040, 35.07837490203588970, 8.259914813157596569 ) ) ;
#41449=( NAMED_UNIT ( * ) PLANE_ANGLE_UNIT ( ) SI_UNIT ( $, .RADIAN. ) );
#41456=CARTESIAN_POINT ( 'NONE',  ( 16.32471966984386214, 45.71573795642332527, 6.626903219538378131 ) ) ;
#41464=CARTESIAN_POINT ( 'NONE',  ( -30.82780881727108735, 15.25261229662382512, 40.33825946679381502 ) ) ;
#41479=CARTESIAN_POINT ( 'NONE',  ( -17.83350561808738988, 43.17460513785992759, 5.799463800283817250 ) ) ;
#41486=CARTESIAN_POINT ( 'NONE',  ( -28.77725283099251641, 13.66028544304341352, 39.99080474963844267 ) ) ;
#41495=CARTESIAN_POINT ( 'NONE',  ( 36.81595939732522282, 27.89094747516896433, -13.21838899458732897 ) ) ;
#41499=ORIENTED_EDGE ( 'NONE', *, *, #37660, .F. ) ;
#41504=FILL_AREA_STYLE ('',( #49593 ) ) ;
#41510=STYLED_ITEM ( 'NONE', ( #51322 ), #81287 ) ;
#41527=ORIENTED_EDGE ( 'NONE', *, *, #5690, .T. ) ;
#41545=CARTESIAN_POINT ( 'NONE',  ( 1.128978779050344716, 25.81467378070274066, 38.95751801069041420 ) ) ;
#41549=ADVANCED_FACE ( 'NONE', ( #100228 ), #58725, .F. ) ;
#41553=( NAMED_UNIT ( * ) PLANE_ANGLE_UNIT ( ) SI_UNIT ( $, .RADIAN. ) );
#41561=CARTESIAN_POINT ( 'NONE',  ( 4.506172367774442300, 54.31195234087692825, 6.292759722430547598 ) ) ;
#41579=ORIENTED_EDGE ( 'NONE', *, *, #47308, .T. ) ;
#41585=FACE_BOUND ( 'NONE', #21615, .T. ) ;
#41587=ORIENTED_EDGE ( 'NONE', *, *, #101515, .T. ) ;
#41614=CARTESIAN_POINT ( 'NONE',  ( 0.000000000000000000, 0.000000000000000000, 24.55262289886175964 ) ) ;
#41624=CARTESIAN_POINT ( 'NONE',  ( -23.62741386766555962, 27.31466638971095406, 33.14007574073351492 ) ) ;
#41636=DIRECTION ( 'NONE',  ( 0.000000000000000000, 1.000000000000000000, 0.000000000000000000 ) ) ;
#41639=CARTESIAN_POINT ( 'NONE',  ( 16.12754063828955609, 36.56084451123473400, 24.14283378817819070 ) ) ;
#41642=CARTESIAN_POINT ( 'NONE',  ( -38.18937913013400731, 25.28116514224970146, 13.30224098674663580 ) ) ;
#41652=CARTESIAN_POINT ( 'NONE',  ( 26.16506696227845552, 37.17214248418269307, -7.978832041202565506 ) ) ;
#41655=CARTESIAN_POINT ( 'NONE',  ( -22.43989698835522262, 28.20716416251315195, -30.97385700653319773 ) ) ;
#41657=CARTESIAN_POINT ( 'NONE',  ( 16.58710573300756508, 37.15623819652538629, -21.80698433968624528 ) ) ;
#41665=VECTOR ( 'NONE', #96732, 1000.000000000000227 ) ;
#41667=CARTESIAN_POINT ( 'NONE',  ( -47.14730021652961511, 17.20087926883181240, 16.50246546963050776 ) ) ;
#41668=CARTESIAN_POINT ( 'NONE',  ( 38.32995719435926674, 27.37220640332429511, -13.21005651354133015 ) ) ;
#41684=CARTESIAN_POINT ( 'NONE',  ( 7.338420317991889874, 52.18300848749867527, 2.465250910119829442 ) ) ;
#41687=CARTESIAN_POINT ( 'NONE',  ( 48.26727629737668934, 11.05468605157633455, 14.37283805632272404 ) ) ;
#41699=SURFACE_STYLE_FILL_AREA ( #91329 ) ;
#41728=ORIENTED_EDGE ( 'NONE', *, *, #61910, .T. ) ;
#41737=CARTESIAN_POINT ( 'NONE',  ( 15.89347175675500523, 43.76110554583822676, 6.420484938539215314 ) ) ;
#41741=DIRECTION ( 'NONE',  ( -0.000000000000000000, 1.000000000000000000, 0.000000000000000000 ) ) ;
#41744=CARTESIAN_POINT ( 'NONE',  ( -17.39146662423148371, 45.59957931493300265, -4.393505531746719761 ) ) ;
#41746=VERTEX_POINT ( 'NONE', #37012 ) ;
#41748=DIRECTION ( 'NONE',  ( 0.000000000000000000, 0.000000000000000000, 1.000000000000000000 ) ) ;
#41752=CARTESIAN_POINT ( 'NONE',  ( -0.2967723360979330205, 12.99353012863888956, 51.71639748483603682 ) ) ;
#41764=CARTESIAN_POINT ( 'NONE',  ( -11.51386276761305005, 45.40501555918416443, -14.44555604779044522 ) ) ;
#41768=CARTESIAN_POINT ( 'NONE',  ( -47.14764774813726689, 18.53760837137019024, -14.71662980465877091 ) ) ;
#41770=( GEOMETRIC_REPRESENTATION_CONTEXT ( 3 ) GLOBAL_UNCERTAINTY_ASSIGNED_CONTEXT ( ( #34571 ) ) GLOBAL_UNIT_ASSIGNED_CONTEXT ( ( #84528, #99627, #17666 ) ) REPRESENTATION_CONTEXT ( 'NONE', 'WORKASPACE' ) );
#41784=CARTESIAN_POINT ( 'NONE',  ( -9.041068741337817016, 43.82601327531473601, 14.35289375551374391 ) ) ;
#41799=CARTESIAN_POINT ( 'NONE',  ( 0.000000000000000000, 52.29617335651133914, -13.27631144943088692 ) ) ;
#41808=PRESENTATION_STYLE_ASSIGNMENT (( #8906 ) ) ;
#41818=CARTESIAN_POINT ( 'NONE',  ( 38.66222440567811702, 25.17349152328067419, -12.83126464919931564 ) ) ;
#41825=CARTESIAN_POINT ( 'NONE',  ( -0.5688039300739448079, 43.22114551779936420, 18.61622414936086045 ) ) ;
#41826=FACE_OUTER_BOUND ( 'NONE', #29271, .T. ) ;
#41829=CARTESIAN_POINT ( 'NONE',  ( 1.010192736754801146, 46.02235752558536319, -16.74599088214888454 ) ) ;
#41831=VERTEX_POINT ( 'NONE', #70415 ) ;
#41832=CARTESIAN_POINT ( 'NONE',  ( 4.387778976649723378E-15, 0.000000000000000000, -35.82893434829263413 ) ) ;
#41857=ADVANCED_FACE ( 'NONE', ( #47702 ), #24011, .F. ) ;
#41879=CARTESIAN_POINT ( 'NONE',  ( 7.938522632820759206, 54.17484897284736434, 1.684095682798675497 ) ) ;
#41881=AXIS2_PLACEMENT_3D ( 'NONE', #26880, #76978, #61348 ) ;
#41885=VERTEX_POINT ( 'NONE', #63400 ) ;
#41895=COLOUR_RGB ( '', 0.09019608, 0.27058824, 0.51372549) ;
#41907=( NAMED_UNIT ( * ) PLANE_ANGLE_UNIT ( ) SI_UNIT ( $, .RADIAN. ) );
#41935=CARTESIAN_POINT ( 'NONE',  ( 17.83130206369999726, 36.70573752982816274, -22.40672895700094358 ) ) ;
#41945=CARTESIAN_POINT ( 'NONE',  ( 22.22792991547093422, 27.72626095856945128, -32.73621634624677057 ) ) ;
#41957=B_SPLINE_CURVE_WITH_KNOTS ( 'NONE', 3,
 ( #8511, #58129, #59213, #45034, #91055, #41945, #17163, #50034, #82941, #74830, #43021, #77920, #4028, #92090, #98585, #67826, #24730, #100712, #51087, #91580 ),
 .UNSPECIFIED., .F., .F.,
 ( 4, 2, 2, 2, 2, 2, 2, 2, 2, 4 ),
 ( 0.0009445086018700385531, 0.001449274952876526343, 0.001954041303883013916, 0.002458807654889501489, 0.002963574005895989495, 0.003468340356902476634, 0.003973106707908964641, 0.004225489883412212114, 0.004477873058915460454, 0.004982639409921950195 ),
 .UNSPECIFIED. ) ;
#41961=SURFACE_SIDE_STYLE ('',( #33910 ) ) ;
#41968=FACE_OUTER_BOUND ( 'NONE', #92724, .T. ) ;
#41977=CARTESIAN_POINT ( 'NONE',  ( -47.77591036386557732, 12.17665806217422286, 14.37301751662919003 ) ) ;
#41981=ORIENTED_EDGE ( 'NONE', *, *, #47308, .F. ) ;
#41987=CARTESIAN_POINT ( 'NONE',  ( 16.48350313421783753, 45.65798623861609684, 6.657797401561500017 ) ) ;
#41996=CARTESIAN_POINT ( 'NONE',  ( -30.90663305326248889, 14.69720259819712815, 40.57123681776395330 ) ) ;
#41998=FACE_BOUND ( 'NONE', #30613, .T. ) ;
#42004=ORIENTED_EDGE ( 'NONE', *, *, #42902, .F. ) ;
#42008=EDGE_LOOP ( 'NONE', ( #19933, #16191, #103666, #47926 ) ) ;
#42009=CARTESIAN_POINT ( 'NONE',  ( -17.89161720275079759, 34.22760597788447257, -23.57693812718947513 ) ) ;
#42012=CARTESIAN_POINT ( 'NONE',  ( -5.290067270632269114, 51.34639538792298907, -8.531152949374520844 ) ) ;
#42019=ADVANCED_FACE ( 'NONE', ( #104351 ), #55262, .F. ) ;
#42022=ORIENTED_EDGE ( 'NONE', *, *, #88752, .F. ) ;
#42026=CARTESIAN_POINT ( 'NONE',  ( 36.35746645901171803, 28.12773496632032533, -12.56232177387087212 ) ) ;
#42085=CARTESIAN_POINT ( 'NONE',  ( 4.063294091762369220, 54.18592360713469702, 6.990124018066343758 ) ) ;
#42091=EDGE_LOOP ( 'NONE', ( #26913, #53915, #35941, #96761 ) ) ;
#42112=PRESENTATION_STYLE_ASSIGNMENT (( #35124 ) ) ;
#42119=LINE ( 'NONE', #27589, #65722 ) ;
#42121=EDGE_CURVE ( 'NONE', #12685, #35979, #84010, .T. ) ;
#42125=DIRECTION ( 'NONE',  ( 0.000000000000000000, 0.000000000000000000, 1.000000000000000000 ) ) ;
#42134=LINE ( 'NONE', #41614, #30395 ) ;
#42145=CARTESIAN_POINT ( 'NONE',  ( -24.23707248033654693, 27.31414015027108277, 32.69896640055586090 ) ) ;
#42171=SURFACE_STYLE_USAGE ( .BOTH. , #610 ) ;
#42172=EDGE_LOOP ( 'NONE', ( #91592, #65395, #27667, #72675 ) ) ;
#42178=SURFACE_SIDE_STYLE ('',( #59450 ) ) ;
#42184=CARTESIAN_POINT ( 'NONE',  ( 30.06732394248781048, 17.62925877149445597, -39.66393268825159879 ) ) ;
#42194=( NAMED_UNIT ( * ) PLANE_ANGLE_UNIT ( ) SI_UNIT ( $, .RADIAN. ) );
#42201=ADVANCED_FACE ( 'NONE', ( #70284 ), #44960, .F. ) ;
#42210=CARTESIAN_POINT ( 'NONE',  ( 8.400221614534629566, 51.89221066646364022, 1.531152949373683958 ) ) ;
#42212=CARTESIAN_POINT ( 'NONE',  ( 49.27082696441105014, 7.795205586015218735, 15.75806003941683109 ) ) ;
#42239=CARTESIAN_POINT ( 'NONE',  ( 1.255263095696489281E-15, 51.26930509877138320, 10.24999999999999822 ) ) ;
#42242=CARTESIAN_POINT ( 'NONE',  ( -23.21751746555280249, 27.38103382803677022, -33.20617127781034839 ) ) ;
#42253=MECHANICAL_DESIGN_GEOMETRIC_PRESENTATION_REPRESENTATION('',(#18199),#52573);
#42266=CARTESIAN_POINT ( 'NONE',  ( 27.10511071441176867, -1.200000000000000030E-05, -10.05698433968634653 ) ) ;
#42274=CARTESIAN_POINT ( 'NONE',  ( 16.75187969033515145, -1.200000000000000030E-05, -23.05698433968624528 ) ) ;
#42279=CARTESIAN_POINT ( 'NONE',  ( -0.1549699029642897519, 12.93291415108713771, 51.74244959244378350 ) ) ;
#42287=CARTESIAN_POINT ( 'NONE',  ( 1.220765430959100062, 45.62969692430660018, 17.81327028958127912 ) ) ;
#42288=CARTESIAN_POINT ( 'NONE',  ( 1.231544126066453693, 16.44631351882073034, -50.25343537072281208 ) ) ;
#42293=EDGE_CURVE ( 'NONE', #104203, #92815, #34670, .T. ) ;
#42299=DIRECTION ( 'NONE',  ( 0.000000000000000000, -0.3420201433256733758, -0.9396926207859066515 ) ) ;
#42301=ORIENTED_EDGE ( 'NONE', *, *, #5690, .F. ) ;
#42308=CARTESIAN_POINT ( 'NONE',  ( 10.28624191511809371, 43.99263840937192782, -12.90779740156171407 ) ) ;
#42309=FILL_AREA_STYLE ('',( #67664 ) ) ;
#42312=ORIENTED_EDGE ( 'NONE', *, *, #61343, .T. ) ;
#42313=CARTESIAN_POINT ( 'NONE',  ( 9.554945014158674255, 51.29116508586518108, -3.541826056265481970 ) ) ;
#42337=CARTESIAN_POINT ( 'NONE',  ( -36.31864149993810287, 26.04191782070092032, 12.31453629475708667 ) ) ;
#42355=CARTESIAN_POINT ( 'NONE',  ( -9.636065190160278959, 53.53714903547604820, 2.125145488933209759 ) ) ;
#42357=CARTESIAN_POINT ( 'NONE',  ( -1.011673908906385311, 43.34673389873664462, 18.25206967576084693 ) ) ;
#42360=FACE_OUTER_BOUND ( 'NONE', #42008, .T. ) ;
#42364=ORIENTED_EDGE ( 'NONE', *, *, #80737, .T. ) ;
#42374=CARTESIAN_POINT ( 'NONE',  ( -30.06815944328915435, 12.45816842452743067, -39.66421731453383615 ) ) ;
#42384=DIRECTION ( 'NONE',  ( 0.000000000000000000, 0.000000000000000000, 1.000000000000000000 ) ) ;
#42395=COLOUR_RGB ( '', 0.40784314, 0.44705882, 0.49803922) ;
#42414=CARTESIAN_POINT ( 'NONE',  ( 7.350509712866862166, 54.21962849041422317, 3.138265851615306801 ) ) ;
#42420=CARTESIAN_POINT ( 'NONE',  ( -16.34886101041462680, 36.48569306717566008, -24.24298062968071932 ) ) ;
#42421=ORIENTED_EDGE ( 'NONE', *, *, #35152, .T. ) ;
#42426=ADVANCED_FACE ( 'NONE', ( #59418 ), #83656, .F. ) ;
#42432=ORIENTED_EDGE ( 'NONE', *, *, #29989, .F. ) ;
#42433=CARTESIAN_POINT ( 'NONE',  ( -47.03691741412927030, 13.53106325772394669, -14.84138715777564066 ) ) ;
#42457=CARTESIAN_POINT ( 'NONE',  ( 7.357155954586323432, 54.21801673151467327, -3.132771341046588720 ) ) ;
#42498=FACE_OUTER_BOUND ( 'NONE', #99043, .T. ) ;
#42504=EDGE_CURVE ( 'NONE', #83087, #65902, #101496, .T. ) ;
#42522=FILL_AREA_STYLE_COLOUR ( '', #7681 ) ;
#42545=CARTESIAN_POINT ( 'NONE',  ( 23.21751746555220564, 25.98869614573808917, -30.70617127781077116 ) ) ;
#42546=CARTESIAN_POINT ( 'NONE',  ( -28.71516359314619393, 10.50242333429326713, 41.65501769021843614 ) ) ;
#42611=SURFACE_STYLE_FILL_AREA ( #25407 ) ;
#42614=AXIS2_PLACEMENT_3D ( 'NONE', #2787, #10864, #92861 ) ;
#42619=CARTESIAN_POINT ( 'NONE',  ( 4.524538969695734991, 53.69347865467890557, 8.282048616735908197 ) ) ;
#42626=ORIENTED_EDGE ( 'NONE', *, *, #24029, .T. ) ;
#42627=EDGE_CURVE ( 'NONE', #100209, #43603, #61586, .T. ) ;
#42633=( GEOMETRIC_REPRESENTATION_CONTEXT ( 3 ) GLOBAL_UNCERTAINTY_ASSIGNED_CONTEXT ( ( #23290 ) ) GLOBAL_UNIT_ASSIGNED_CONTEXT ( ( #19208, #67711, #11042 ) ) REPRESENTATION_CONTEXT ( 'NONE', 'WORKASPACE' ) );
#42671=ORIENTED_EDGE ( 'NONE', *, *, #6324, .T. ) ;
#42683=CARTESIAN_POINT ( 'NONE',  ( -24.20637929534487398, 27.76268499971478931, 31.17501708768064717 ) ) ;
#42690=PRESENTATION_STYLE_ASSIGNMENT (( #74514 ) ) ;
#42692=EDGE_CURVE ( 'NONE', #74150, #3192, #25489, .T. ) ;
#42729=FACE_OUTER_BOUND ( 'NONE', #8316, .T. ) ;
#42732=CARTESIAN_POINT ( 'NONE',  ( -47.90297653514730314, 15.22282649863647919, 16.85535821593517269 ) ) ;
#42744=B_SPLINE_CURVE_WITH_KNOTS ( 'NONE', 3,
 ( #24962, #57816, #91806, #74538, #67535, #10336, #100415, #99885, #83171, #50780, #66457, #8744, #17927, #82644, #83692, #26580, #41652, #59448, #43252, #17394, #9269, #100947 ),
 .UNSPECIFIED., .F., .F.,
 ( 4, 2, 2, 2, 2, 2, 2, 2, 2, 2, 4 ),
 ( 0.007124701767327336864, 0.007629109439095383555, 0.008133517110863429378, 0.008385720946747459228, 0.008637924782631487344, 0.009142332454399534902, 0.009646740126167582460, 0.009898943962051603637, 0.01015114779793562655, 0.01065555546970366890, 0.01115996314147171299 ),
 .UNSPECIFIED. ) ;
#42748=CARTESIAN_POINT ( 'NONE',  ( 7.803955644651615842, 52.08656169318132356, 1.781976911754487913 ) ) ;
#42751=CARTESIAN_POINT ( 'NONE',  ( 1.101948812519610632, 43.39583042475737784, 18.11144527318901254 ) ) ;
#42763=FILL_AREA_STYLE_COLOUR ( '', #53050 ) ;
#42767=CONICAL_SURFACE ( 'NONE', #101369, 11.27631144943088337, 1.221730476396025722 ) ;
#42790=ORIENTED_EDGE ( 'NONE', *, *, #83951, .T. ) ;
#42804=CARTESIAN_POINT ( 'NONE',  ( -49.25896281664908827, 12.93370316445966317, 15.83749202751426033 ) ) ;
#42819=CARTESIAN_POINT ( 'NONE',  ( -0.9432938954576324253, 17.83686411059527899, 49.67615204089843672 ) ) ;
#42827=CARTESIAN_POINT ( 'NONE',  ( 1.115733355096011570, 14.48162342373252720, -51.08071913610608306 ) ) ;
#42831=CARTESIAN_POINT ( 'NONE',  ( -9.721687949930888806, 46.20860120156269346, 13.03939565591211469 ) ) ;
#42833=CARTESIAN_POINT ( 'NONE',  ( -47.18437091044132359, 18.47854193719484428, -14.68206053360911945 ) ) ;
#42868=CARTESIAN_POINT ( 'NONE',  ( 6.488302422815169557, 51.35002353678540743, -7.646734246321329032 ) ) ;
#42883=CARTESIAN_POINT ( 'NONE',  ( 1.250953595776213900, 10.43180450791889413, 50.60765994387645605 ) ) ;
#42888=CARTESIAN_POINT ( 'NONE',  ( 38.19004552306619615, 25.28097608663575357, -13.30190894607149055 ) ) ;
#42902=EDGE_CURVE ( 'NONE', #57955, #37002, #68640, .T. ) ;
#42905=CARTESIAN_POINT ( 'NONE',  ( 30.87886018709244240, 13.47971040000132525, 41.23243855231577015 ) ) ;
#42916=CARTESIAN_POINT ( 'NONE',  ( 0.3345852822193742804, 28.19046229938386006, 38.29267374853493777 ) ) ;
#42957=CARTESIAN_POINT ( 'NONE',  ( 7.465939481983455472, 54.30095352640775275, 2.152531556884869524 ) ) ;
#42964=CARTESIAN_POINT ( 'NONE',  ( -16.75187969033554936, 36.38380281757302015, -24.30698433968596106 ) ) ;
#42976=ORIENTED_EDGE ( 'NONE', *, *, #97411, .F. ) ;
#42978=CARTESIAN_POINT ( 'NONE',  ( -46.83715889037884494, 13.71037705486507363, -15.21858309684217936 ) ) ;
#42979=COLOUR_RGB ( '', 0.66274510, 0.83137255, 0.94901961) ;
#42981=CARTESIAN_POINT ( 'NONE',  ( -36.49061380186538628, 25.91753039342102127, -12.86327411670220222 ) ) ;
#42984=PRESENTATION_STYLE_ASSIGNMENT (( #6475 ) ) ;
#42996=CARTESIAN_POINT ( 'NONE',  ( 17.27438113373175455, 45.65101552804005536, -4.281429632575810551 ) ) ;
#42997=DIRECTION ( 'NONE',  ( -0.000000000000000000, 1.000000000000000000, 0.000000000000000000 ) ) ;
#42998=CARTESIAN_POINT ( 'NONE',  ( 48.02835407290544367, 11.61227450977237829, 14.35535821593427386 ) ) ;
#43012=CARTESIAN_POINT ( 'NONE',  ( 16.91846161659815806, 36.35180932965545253, -24.29864124313492013 ) ) ;
#43016=DIRECTION ( 'NONE',  ( 0.000000000000000000, 0.000000000000000000, 1.000000000000000000 ) ) ;
#43021=CARTESIAN_POINT ( 'NONE',  ( 21.98976603507215088, 28.09591002020466988, -31.66807300705254491 ) ) ;
#43026=EDGE_CURVE ( 'NONE', #96644, #26726, #24602, .T. ) ;
#43043=CARTESIAN_POINT ( 'NONE',  ( -0.8412040808739075226, 27.41052785484215448, 40.42819026091922296 ) ) ;
#43061=EDGE_LOOP ( 'NONE', ( #22195, #26828, #90214, #38105 ) ) ;
#43066=CARTESIAN_POINT ( 'NONE',  ( 9.803790402534414028, 53.40454157566192350, 2.927104633565267733 ) ) ;
#43072=CARTESIAN_POINT ( 'NONE',  ( -30.48723010194668603, 12.91713162683278249, 41.81530375792740983 ) ) ;
#43076=CARTESIAN_POINT ( 'NONE',  ( -7.807627842885899838, 51.84081132806975489, 3.792411731296619237 ) ) ;
#43088=CARTESIAN_POINT ( 'NONE',  ( 49.22356967707742115, 12.91018829712011140, 15.97913688295796852 ) ) ;
#43095=CARTESIAN_POINT ( 'NONE',  ( -0.7856127335827165492, 37.10997504226060784, 27.51427648435862494 ) ) ;
#43111=EDGE_CURVE ( 'NONE', #100497, #67401, #52031, .T. ) ;
#43112=CARTESIAN_POINT ( 'NONE',  ( -23.38230688380519595, 25.22066353262445304, -33.19807408660797421 ) ) ;
#43118=CARTESIAN_POINT ( 'NONE',  ( 0.4150645071567997668, 36.32396184902202663, 29.68202632210200065 ) ) ;
#43135=CYLINDRICAL_SURFACE ( 'NONE', #45254, 1.250000000000001110 ) ;
#43167=CARTESIAN_POINT ( 'NONE',  ( 27.10511071441198894, 36.88665068479745912, 7.556984339683237906 ) ) ;
#43185=DIRECTION ( 'NONE',  ( 0.000000000000000000, 1.000000000000000000, 0.000000000000000000 ) ) ;
#43186=EDGE_CURVE ( 'NONE', #86888, #55752, #95015, .T. ) ;
#43194=CARTESIAN_POINT ( 'NONE',  ( -0.6467460089013201685, 53.45139368308109340, 10.08288459130510439 ) ) ;
#43206=CARTESIAN_POINT ( 'NONE',  ( -30.04058829887638282, 13.07764605659131796, -42.05455409923744270 ) ) ;
#43213=CARTESIAN_POINT ( 'NONE',  ( 36.58606824315381800, 25.86842935218156825, -12.99751704779520267 ) ) ;
#43223=CARTESIAN_POINT ( 'NONE',  ( -15.70492864000498301, 46.17438344839472819, -4.577980962366806850 ) ) ;
#43231=CARTESIAN_POINT ( 'NONE',  ( -0.5694748022185723846, 45.34960206111118453, 18.61592841094030604 ) ) ;
#43237=CARTESIAN_POINT ( 'NONE',  ( 15.50007054317050681, 37.03005157377465650, 23.01145510268004912 ) ) ;
#43252=CARTESIAN_POINT ( 'NONE',  ( 26.48366646117538536, 37.08895952672338581, -7.710263864458167582 ) ) ;
#43259=CARTESIAN_POINT ( 'NONE',  ( 29.77121734509575290, 18.16596778899118902, -39.60535821593530414 ) ) ;
#43267=CARTESIAN_POINT ( 'NONE',  ( -47.55680477683402785, 16.06931990738296889, 16.76905664007686880 ) ) ;
#43268=CARTESIAN_POINT ( 'NONE',  ( 37.88489815392355808, 27.77121267130071303, -10.98707414366107926 ) ) ;
#43281=CARTESIAN_POINT ( 'NONE',  ( 7.465531072436692561, 52.17264765254623171, 2.153407880170176814 ) ) ;
#43291=ORIENTED_EDGE ( 'NONE', *, *, #94079, .T. ) ;
#43299=CARTESIAN_POINT ( 'NONE',  ( -1.248763605186368197, 10.99880023176083021, -50.36974636785474502 ) ) ;
#43309=FACE_OUTER_BOUND ( 'NONE', #14714, .T. ) ;
#43320=CARTESIAN_POINT ( 'NONE',  ( 28.35655838125921946, 36.31484077510918951, -8.865061771931141976 ) ) ;
#43322=CARTESIAN_POINT ( 'NONE',  ( -23.05268216894211974, 28.15323590773658680, 30.70617127781061839 ) ) ;
#43333=CARTESIAN_POINT ( 'NONE',  ( 7.312789698585915765, 52.12765650109543714, -2.970840588490396783 ) ) ;
#43335=CARTESIAN_POINT ( 'NONE',  ( -1.011124010007723006, 28.02085465524457675, -38.74700955856429374 ) ) ;
#43340=CARTESIAN_POINT ( 'NONE',  ( 46.81357782755165431, 18.41089473351597761, -15.91307620878907869 ) ) ;
#43344=CARTESIAN_POINT ( 'NONE',  ( -48.15175547875134754, 14.66334354488785507, 16.85535821593515138 ) ) ;
#43350=UNCERTAINTY_MEASURE_WITH_UNIT (LENGTH_MEASURE( 1.000000000000000082E-05 ), #81759, 'distance_accuracy_value', 'NONE');
#43356=EDGE_LOOP ( 'NONE', ( #94942, #10814, #15603, #98389 ) ) ;
#43357=CARTESIAN_POINT ( 'NONE',  ( -21.99058289103490438, 25.96809656825333334, -31.66568596923509560 ) ) ;
#43359=CARTESIAN_POINT ( 'NONE',  ( -26.10803651193542407, 35.05774228055371822, -8.035081906110033145 ) ) ;
#43360=CARTESIAN_POINT ( 'NONE',  ( -1.098016817928066491, 43.84270387359042331, -16.88143485833182922 ) ) ;
#43368=SURFACE_STYLE_FILL_AREA ( #84362 ) ;
#43370=DIRECTION ( 'NONE',  ( -0.000000000000000000, 1.000000000000000000, -0.000000000000000000 ) ) ;
#43378=ORIENTED_EDGE ( 'NONE', *, *, #31173, .T. ) ;
#43382=CARTESIAN_POINT ( 'NONE',  ( -15.90862040200999949, 35.08000091432026579, -22.13043636769250355 ) ) ;
#43389=ORIENTED_EDGE ( 'NONE', *, *, #41015, .F. ) ;
#43395=CARTESIAN_POINT ( 'NONE',  ( 5.457386620333100957, 51.31430185318657777, 8.531152949374462224 ) ) ;
#43404=ORIENTED_EDGE ( 'NONE', *, *, #40677, .F. ) ;
#43412=CARTESIAN_POINT ( 'NONE',  ( 49.26989972136220786, 12.96118195421072450, -15.76560135798010442 ) ) ;
#43415=CARTESIAN_POINT ( 'NONE',  ( -36.59134229708980257, 25.86727557889577511, 12.99205859245150840 ) ) ;
#43426=ORIENTED_EDGE ( 'NONE', *, *, #97910, .T. ) ;
#43444=FILL_AREA_STYLE ('',( #84963 ) ) ;
#43453=CARTESIAN_POINT ( 'NONE',  ( -30.93151921796016524, 9.249586871975878921, -40.69907933257887578 ) ) ;
#43477=B_SPLINE_CURVE_WITH_KNOTS ( 'NONE', 3,
 ( #52985, #85906, #29802, #53515, #11979, #4427, #37898, #44909, #103132, #46997, #30317, #79896, #54020, #3906, #69705, #86963, #13030, #28749, #61632, #45958 ),
 .UNSPECIFIED., .F., .F.,
 ( 4, 2, 2, 2, 2, 2, 2, 2, 2, 4 ),
 ( 0.006976481488830035133, 0.007983724882207922369, 0.008487346578896867721, 0.008990968275585811340, 0.009242779123930287485, 0.009494589972274761897, 0.009998211668963712453, 0.01025002251730818860, 0.01050183336565266648, 0.01100545506234161530 ),
 .UNSPECIFIED. ) ;
#43493=DIRECTION ( 'NONE',  ( -0.000000000000000000, 1.000000000000000000, -0.000000000000000000 ) ) ;
#43509=ORIENTED_EDGE ( 'NONE', *, *, #67988, .F. ) ;
#43530=CARTESIAN_POINT ( 'NONE',  ( 29.68315524076959377, 13.12249633091058243, -39.60535821593525441 ) ) ;
#43541=DIRECTION ( 'NONE',  ( 0.000000000000000000, 0.000000000000000000, 1.000000000000000000 ) ) ;
#43549=( LENGTH_UNIT ( ) NAMED_UNIT ( * ) SI_UNIT ( .MILLI., .METRE. ) );
#43569=EDGE_LOOP ( 'NONE', ( #59166, #951, #46167, #48753 ) ) ;
#43575=ORIENTED_EDGE ( 'NONE', *, *, #24802, .F. ) ;
#43595=FACE_BOUND ( 'NONE', #17600, .T. ) ;
#43599=SURFACE_STYLE_USAGE ( .BOTH. , #44683 ) ;
#43603=VERTEX_POINT ( 'NONE', #28210 ) ;
#43657=DIRECTION ( 'NONE',  ( -0.000000000000000000, 1.000000000000000000, -0.000000000000000000 ) ) ;
#43678=( NAMED_UNIT ( * ) SI_UNIT ( $, .STERADIAN. ) SOLID_ANGLE_UNIT ( ) );
#43692=MECHANICAL_DESIGN_GEOMETRIC_PRESENTATION_REPRESENTATION('',(#52080),#62659);
#43703=DIRECTION ( 'NONE',  ( 0.000000000000000000, 0.000000000000000000, 1.000000000000000000 ) ) ;
#43719=CARTESIAN_POINT ( 'NONE',  ( 23.21751746555303342, 27.38103382803677377, 33.20617127781017075 ) ) ;
#43726=ORIENTED_EDGE ( 'NONE', *, *, #82873, .F. ) ;
#43727=DIRECTION ( 'NONE',  ( -0.000000000000000000, 1.000000000000000000, -0.000000000000000000 ) ) ;
#43741=FACE_OUTER_BOUND ( 'NONE', #47458, .T. ) ;
#43749=UNCERTAINTY_MEASURE_WITH_UNIT (LENGTH_MEASURE( 1.000000000000000082E-05 ), #50172, 'distance_accuracy_value', 'NONE');
#43778=SURFACE_STYLE_USAGE ( .BOTH. , #42178 ) ;
#43783=CARTESIAN_POINT ( 'NONE',  ( 30.63784394300822100, 16.09242744237242917, -40.03992687782061921 ) ) ;
#43784=( NAMED_UNIT ( * ) SI_UNIT ( $, .STERADIAN. ) SOLID_ANGLE_UNIT ( ) );
#43791=CARTESIAN_POINT ( 'NONE',  ( 38.77519395269280267, 27.37135291505367718, -11.84730558812103141 ) ) ;
#43794=CARTESIAN_POINT ( 'NONE',  ( 17.76981297930376158, 43.17870619678550526, 5.956428682172403732 ) ) ;
#43807=CARTESIAN_POINT ( 'NONE',  ( 0.000000000000000000, 27.68727484027578356, 0.000000000000000000 ) ) ;
#43818=CARTESIAN_POINT ( 'NONE',  ( -7.923942441289230310, 51.78500681803757288, -3.904538598597388166 ) ) ;
#43821=CARTESIAN_POINT ( 'NONE',  ( -0.9432308977042356268, 12.66755915628530538, -49.67613533980958351 ) ) ;
#43832=FILL_AREA_STYLE ('',( #77272 ) ) ;
#43833=ORIENTED_EDGE ( 'NONE', *, *, #93261, .F. ) ;
#43834=CARTESIAN_POINT ( 'NONE',  ( -9.040043340647605064, 46.05340506531722866, -14.03079106125278841 ) ) ;
#43841=CARTESIAN_POINT ( 'NONE',  ( -15.39708646668728420, 44.03708262471037216, 5.599658763118309679 ) ) ;
#43843=CARTESIAN_POINT ( 'NONE',  ( 27.42641407226152594, 36.49996279467831073, -10.02585437320845863 ) ) ;
#43850=VERTEX_POINT ( 'NONE', #13556 ) ;
#43856=CARTESIAN_POINT ( 'NONE',  ( 8.239673527368280403, 51.94776582111974506, -1.561980839535718202 ) ) ;
#43865=FACE_OUTER_BOUND ( 'NONE', #44253, .T. ) ;
#43867=CARTESIAN_POINT ( 'NONE',  ( -48.49405853457024307, 15.66070211563346959, 14.43943585503378202 ) ) ;
#43869=CARTESIAN_POINT ( 'NONE',  ( 0.000000000000000000, -1.200000000000000030E-05, 9.000000000000000000 ) ) ;
#43872=FILL_AREA_STYLE ('',( #10952 ) ) ;
#43884=AXIS2_PLACEMENT_3D ( 'NONE', #33028, #6582, #31955 ) ;
#43894=SURFACE_SIDE_STYLE ('',( #61707 ) ) ;
#43899=CARTESIAN_POINT ( 'NONE',  ( 5.523799489093671039E-15, 23.58303312036771615, 45.10524579772351217 ) ) ;
#43906=CARTESIAN_POINT ( 'NONE',  ( -16.66923479943752540, 34.27251685716380791, -24.30698433968595396 ) ) ;
#43911=CARTESIAN_POINT ( 'NONE',  ( -17.97116198174659729, 34.27731494407649393, 23.34421261274562909 ) ) ;
#43917=CARTESIAN_POINT ( 'NONE',  ( 48.98802391561655867, 7.953645742799005269, -16.40821160912129173 ) ) ;
#43919=CARTESIAN_POINT ( 'NONE',  ( 5.689392408559237779, 51.96560585840138202, 6.093956388208072283 ) ) ;
#43975=EDGE_CURVE ( 'NONE', #106075, #44079, #20477, .T. ) ;
#43980=CARTESIAN_POINT ( 'NONE',  ( -30.55414771718603717, 11.21328959333581388, -39.95065846502016882 ) ) ;
#43987=ORIENTED_EDGE ( 'NONE', *, *, #55688, .T. ) ;
#43988=DIRECTION ( 'NONE',  ( 4.738110706560371839E-17, -0.9221233147934838614, 0.3868961001538753219 ) ) ;
#43996=CARTESIAN_POINT ( 'NONE',  ( 4.959124542865535723, 54.27782660535947912, -6.063864958317412679 ) ) ;
#44008=DIRECTION ( 'NONE',  ( -0.000000000000000000, 1.000000000000000000, -0.000000000000000000 ) ) ;
#44024=CARTESIAN_POINT ( 'NONE',  ( -16.66949223230251675, 36.40081923159284827, -24.30698433968597172 ) ) ;
#44029=UNCERTAINTY_MEASURE_WITH_UNIT (LENGTH_MEASURE( 1.000000000000000082E-05 ), #72237, 'distance_accuracy_value', 'NONE');
#44036=ORIENTED_EDGE ( 'NONE', *, *, #68691, .T. ) ;
#44038=CARTESIAN_POINT ( 'NONE',  ( -47.77500202626900005, 12.17856325595019307, -14.37326074422667332 ) ) ;
#44042=CARTESIAN_POINT ( 'NONE',  ( -17.39035180332607666, 43.47171372390574362, -4.392436222999140938 ) ) ;
#44051=AXIS2_PLACEMENT_3D ( 'NONE', #42274, #100514, #41748 ) ;
#44066=( NAMED_UNIT ( * ) SI_UNIT ( $, .STERADIAN. ) SOLID_ANGLE_UNIT ( ) );
#44079=VERTEX_POINT ( 'NONE', #34572 ) ;
#44085=STYLED_ITEM ( 'NONE', ( #91191 ), #99636 ) ;
#44107=ORIENTED_EDGE ( 'NONE', *, *, #67988, .T. ) ;
#44110=( LENGTH_UNIT ( ) NAMED_UNIT ( * ) SI_UNIT ( .MILLI., .METRE. ) );
#44153=CARTESIAN_POINT ( 'NONE',  ( 49.19747204248938743, 12.91412732281176545, 16.05397513442666479 ) ) ;
#44184=CARTESIAN_POINT ( 'NONE',  ( 1.220343922963510463, 36.63129049403877957, 28.81469345036448004 ) ) ;
#44204=CARTESIAN_POINT ( 'NONE',  ( -15.89370886130902427, 45.88935169965961336, 6.420701231162380118 ) ) ;
#44241=CARTESIAN_POINT ( 'NONE',  ( 30.77208753046679846, 10.36816855262256887, -40.23037088889287105 ) ) ;
#44242=SURFACE_STYLE_FILL_AREA ( #11852 ) ;
#44248=ORIENTED_EDGE ( 'NONE', *, *, #33603, .T. ) ;
#44253=EDGE_LOOP ( 'NONE', ( #75954, #47022, #64271, #33283, #40680, #71414, #2295, #41981 ) ) ;
#44276=CARTESIAN_POINT ( 'NONE',  ( -6.544565951341991372, 51.40333703996573433, 7.404642427234960245 ) ) ;
#44286=CARTESIAN_POINT ( 'NONE',  ( -9.204916576609303291, 43.65482048207726251, -14.80499302221950764 ) ) ;
#44293=CARTESIAN_POINT ( 'NONE',  ( -1.005743885764240231, 45.47705655343377629, 18.24665906407937754 ) ) ;
#44324=CARTESIAN_POINT ( 'NONE',  ( 3.840629472727446691E-14, -1.200000000000000030E-05, 28.50000000000000000 ) ) ;
#44329=( GEOMETRIC_REPRESENTATION_CONTEXT ( 3 ) GLOBAL_UNCERTAINTY_ASSIGNED_CONTEXT ( ( #101170 ) ) GLOBAL_UNIT_ASSIGNED_CONTEXT ( ( #4930, #103614, #30281 ) ) REPRESENTATION_CONTEXT ( 'NONE', 'WORKASPACE' ) );
#44333=CARTESIAN_POINT ( 'NONE',  ( 18.00630676350472115, 34.31621990238991060, 23.18203998712654368 ) ) ;
#44337=CARTESIAN_POINT ( 'NONE',  ( 17.26626608613624114, 43.28465477507130288, 6.503894573084921582 ) ) ;
#44340=B_SPLINE_CURVE_WITH_KNOTS ( 'NONE', 3,
 ( #5606, #80544, #104841, #63336, #89721, #6663, #15821, #104292, #7713, #79495, #96753, #38531, #30442, #22360, #96231, #55204, #39590, #105369, #86896, #22167, #63141, #78771, #96040, #12969, #94993, #45894 ),
 .UNSPECIFIED., .F., .F.,
 ( 4, 2, 2, 2, 2, 2, 2, 2, 2, 2, 2, 2, 4 ),
 ( 0.002320533079692624519, 0.002572382410217119615, 0.002824231740741614712, 0.003076081071266110242, 0.003327930401790605338, 0.003831629062839588592, 0.004083478393364082387, 0.004335327723888575749, 0.005342725045986517970, 0.005594574376511001791, 0.005846423707035485612, 0.006098273037559968565, 0.006350122368084452386 ),
 .UNSPECIFIED. ) ;
#44353=FILL_AREA_STYLE_COLOUR ( '', #63277 ) ;
#44361=ORIENTED_EDGE ( 'NONE', *, *, #71476, .F. ) ;
#44364=FILL_AREA_STYLE_COLOUR ( '', #93177 ) ;
#44375=CARTESIAN_POINT ( 'NONE',  ( -4.958743871765130429, 54.27777375259184822, -6.064299819695584404 ) ) ;
#44376=VECTOR ( 'NONE', #102230, 1000.000000000000000 ) ;
#44379=CARTESIAN_POINT ( 'NONE',  ( -10.12028333941253777, 45.42143084255511098, -15.39942097377737795 ) ) ;
#44400=CARTESIAN_POINT ( 'NONE',  ( -6.287528586677907235E-14, 28.20649408426966431, -38.24999999999931077 ) ) ;
#44410=CARTESIAN_POINT ( 'NONE',  ( -48.48308721883941530, 13.98293033111037964, 16.77185627386600686 ) ) ;
#44416=VERTEX_POINT ( 'NONE', #52175 ) ;
#44423=CARTESIAN_POINT ( 'NONE',  ( -23.21751746555235840, 25.25267828308461304, -33.20617127781177658 ) ) ;
#44425=CARTESIAN_POINT ( 'NONE',  ( -26.78605409122936365, 34.59012538573716711, -10.02589350699965109 ) ) ;
#44436=( NAMED_UNIT ( * ) PLANE_ANGLE_UNIT ( ) SI_UNIT ( $, .RADIAN. ) );
#44457=CARTESIAN_POINT ( 'NONE',  ( 49.07747248321130229, 8.835459238882958033, -14.91203737403161256 ) ) ;
#44458=PRESENTATION_STYLE_ASSIGNMENT (( #68192 ) ) ;
#44477=CARTESIAN_POINT ( 'NONE',  ( 48.15153125426022029, 16.50033784694704053, -14.35535821593549954 ) ) ;
#44481=MECHANICAL_DESIGN_GEOMETRIC_PRESENTATION_REPRESENTATION('',(#41002),#70266);
#44482=DIRECTION ( 'NONE',  ( 0.000000000000000000, 0.000000000000000000, 1.000000000000000000 ) ) ;
#44493=CARTESIAN_POINT ( 'NONE',  ( 0.3602828126333169623, 7.865783509256337958, 51.69852333018035750 ) ) ;
#44543=SURFACE_SIDE_STYLE ('',( #100631 ) ) ;
#44553=VERTEX_POINT ( 'NONE', #103138 ) ;
#44566=COLOUR_RGB ( '', 0.09019608, 0.27058824, 0.51372549) ;
#44581=CARTESIAN_POINT ( 'NONE',  ( -46.78712017075140039, 13.65728975790554145, -15.44288672244362282 ) ) ;
#44584=AXIS2_PLACEMENT_3D ( 'NONE', #17998, #34736, #9875 ) ;
#44601=CARTESIAN_POINT ( 'NONE',  ( 29.14716730816274293, 13.65620768952807929, -39.72410719430394010 ) ) ;
#44604=CARTESIAN_POINT ( 'NONE',  ( -9.797611831518617365, 51.31153553680866253, 2.590295869752982316 ) ) ;
#44624=SURFACE_STYLE_FILL_AREA ( #101258 ) ;
#44654=FILL_AREA_STYLE ('',( #101288 ) ) ;
#44659=ORIENTED_EDGE ( 'NONE', *, *, #35012, .T. ) ;
#44660=DIRECTION ( 'NONE',  ( -0.000000000000000000, 1.000000000000000000, 0.000000000000000000 ) ) ;
#44683=SURFACE_SIDE_STYLE ('',( #67877 ) ) ;
#44688=CARTESIAN_POINT ( 'NONE',  ( 0.5317675288997081307, 8.007226681051733408, -51.63779123901733925 ) ) ;
#44690=VECTOR ( 'NONE', #93896, 1000.000000000000000 ) ;
#44725=EDGE_CURVE ( 'NONE', #79044, #93975, #80758, .T. ) ;
#44726=CARTESIAN_POINT ( 'NONE',  ( 15.54289451413696455, 36.90012926360036261, -23.41220851048994689 ) ) ;
#44776=( GEOMETRIC_REPRESENTATION_CONTEXT ( 3 ) GLOBAL_UNCERTAINTY_ASSIGNED_CONTEXT ( ( #100647 ) ) GLOBAL_UNIT_ASSIGNED_CONTEXT ( ( #64892, #47631, #97254 ) ) REPRESENTATION_CONTEXT ( 'NONE', 'WORKASPACE' ) );
#44808=AXIS2_PLACEMENT_3D ( 'NONE', #43807, #20118, #35767 ) ;
#44818=EDGE_CURVE ( 'NONE', #52295, #86521, #60448, .T. ) ;
#44823=CARTESIAN_POINT ( 'NONE',  ( 36.32228901050014258, 26.06995930799696737, -12.06152503804560006 ) ) ;
#44831=CARTESIAN_POINT ( 'NONE',  ( -15.88324666189017442, 46.12968798971461837, -4.401569153915046329 ) ) ;
#44849=CARTESIAN_POINT ( 'NONE',  ( -1.152188841818234133E-13, -1.200000000000000030E-05, -50.50000000000000000 ) ) ;
#44875=EDGE_LOOP ( 'NONE', ( #96114, #46809, #94375, #38329 ) ) ;
#44896=CARTESIAN_POINT ( 'NONE',  ( 0.000000000000000000, 36.79151656018385097, 22.55262289886175964 ) ) ;
#44909=CARTESIAN_POINT ( 'NONE',  ( -28.35646210991579963, 34.18623537382805466, 8.867673889502601270 ) ) ;
#44912=DIRECTION ( 'NONE',  ( 0.000000000000000000, 0.000000000000000000, 1.000000000000000000 ) ) ;
#44917=CARTESIAN_POINT ( 'NONE',  ( 6.069741682797264559, 53.39713335310042908, -8.261810659904046616 ) ) ;
#44918=CARTESIAN_POINT ( 'NONE',  ( 17.99632133236754328, 34.41154148830023018, -22.85738012984803547 ) ) ;
#44921=VECTOR ( 'NONE', #71484, 1000.000000000000114 ) ;
#44931=CARTESIAN_POINT ( 'NONE',  ( 28.35143274818196346, 36.34363242571733110, -8.614219218061366590 ) ) ;
#44933=MECHANICAL_DESIGN_GEOMETRIC_PRESENTATION_REPRESENTATION('',(#20887),#88036);
#44947=CARTESIAN_POINT ( 'NONE',  ( 7.149395896920095848E-21, 27.29656849860388235, -40.75000000000000000 ) ) ;
#44953=DIRECTION ( 'NONE',  ( -0.000000000000000000, 1.000000000000000000, -0.000000000000000000 ) ) ;
#44955=CARTESIAN_POINT ( 'NONE',  ( -48.91297851735075852, 13.22767571191107194, 16.49376885358302758 ) ) ;
#44960=CYLINDRICAL_SURFACE ( 'NONE', #97779, 1.249999999999999334 ) ;
#44963=CARTESIAN_POINT ( 'NONE',  ( 4.044331601661468767, 52.01019311517404731, -7.150024461864991743 ) ) ;
#44984=DIRECTION ( 'NONE',  ( 0.000000000000000000, 0.000000000000000000, -1.000000000000000000 ) ) ;
#44996=CARTESIAN_POINT ( 'NONE',  ( 9.443129677143925704, 46.21199370134088014, -13.23108103747124353 ) ) ;
#45001=CARTESIAN_POINT ( 'NONE',  ( 48.48335035450812569, 8.813057796081539053, -16.77177117249988214 ) ) ;
#45006=MECHANICAL_DESIGN_GEOMETRIC_PRESENTATION_REPRESENTATION('',(#41510),#17431);
#45034=CARTESIAN_POINT ( 'NONE',  ( 22.59067934059547156, 27.55769764751301665, -33.04957285560310254 ) ) ;
#45035=B_SPLINE_CURVE_WITH_KNOTS ( 'NONE', 3,
 ( #60048, #26627, #83223, #1758, #18518, #50318, #34715, #100468, #9317, #51912, #58966, #99386, #2832, #68663, #17977, #92372, #76188, #1211, #25568, #27159, #51377, #10386 ),
 .UNSPECIFIED., .F., .F.,
 ( 4, 2, 2, 2, 2, 2, 2, 2, 2, 2, 4 ),
 ( 0.007115138407500913240, 0.007619047327870813284, 0.008122956248240713328, 0.008626865168610614240, 0.008878819628795569033, 0.009130774088980523825, 0.009382728549165480353, 0.009634683009350435146, 0.01013859192972034300, 0.01064250085009025085, 0.01114640977046015870 ),
 .UNSPECIFIED. ) ;
#45054=CARTESIAN_POINT ( 'NONE',  ( -7.314965114740616947, 54.29834303721024469, 2.637232812314642239 ) ) ;
#45082=CONICAL_SURFACE ( 'NONE', #26170, 11.27631144943088337, 1.221730476396025722 ) ;
#45084=ADVANCED_FACE ( 'NONE', ( #57086 ), #56006, .T. ) ;
#45088=CARTESIAN_POINT ( 'NONE',  ( -24.00351036083299761, 27.29299690957943980, -32.94270042870569881 ) ) ;
#45102=CARTESIAN_POINT ( 'NONE',  ( -1.007138393507579499, 51.97797158553648700, -8.242245250298140036 ) ) ;
#45105=ORIENTED_EDGE ( 'NONE', *, *, #36245, .T. ) ;
#45114=VERTEX_POINT ( 'NONE', #56552 ) ;
#45137=CARTESIAN_POINT ( 'NONE',  ( 28.43338544108014077, 12.59781646960430201, -40.78060993930086653 ) ) ;
#45160=B_SPLINE_CURVE_WITH_KNOTS ( 'NONE', 3,
 ( #55665, #14157, #64851, #15234, #56741, #55149, #32515, #63274, #104780, #48119, #97731, #106353, #81018, #15765, #65387, #96174, #47590, #7136, #22303, #88079 ),
 .UNSPECIFIED., .F., .F.,
 ( 4, 2, 2, 2, 2, 2, 2, 2, 2, 4 ),
 ( 0.003283110296550481328, 0.003787170202193927693, 0.004039200155015654561, 0.004291230107837381430, 0.005299349919124314925, 0.005803409824767780806, 0.006055439777589506807, 0.006307469730411232808, 0.006811529636054676137, 0.007315589541698119466 ),
 .UNSPECIFIED. ) ;
#45164=CARTESIAN_POINT ( 'NONE',  ( 10.28624191511840458, 43.25714326066859172, 15.40779740156149202 ) ) ;
#45181=CARTESIAN_POINT ( 'NONE',  ( 4.684273348644264514E-15, 28.20649408426940141, 38.25000000000000000 ) ) ;
#45194=( NAMED_UNIT ( * ) PLANE_ANGLE_UNIT ( ) SI_UNIT ( $, .RADIAN. ) );
#45240=VERTEX_POINT ( 'NONE', #101810 ) ;
#45254=AXIS2_PLACEMENT_3D ( 'NONE', #102432, #43657, #29131 ) ;
#45259=ORIENTED_EDGE ( 'NONE', *, *, #80719, .T. ) ;
#45271=CARTESIAN_POINT ( 'NONE',  ( -49.26574068698176490, 8.068653426789120786, 15.39376958037561849 ) ) ;
#45279=ADVANCED_FACE ( 'NONE', ( #4719 ), #61372, .F. ) ;
#45297=STYLED_ITEM ( 'NONE', ( #65857 ), #52510 ) ;
#45312=FACE_BOUND ( 'NONE', #89096, .T. ) ;
#45327=CARTESIAN_POINT ( 'NONE',  ( -22.65267572660740569, 28.20149222899207331, 30.83791392134356713 ) ) ;
#45347=CARTESIAN_POINT ( 'NONE',  ( -30.87886018709214397, 13.47971040000131993, -41.23243855231599042 ) ) ;
#45358=CARTESIAN_POINT ( 'NONE',  ( -10.12015569271582649, 43.29311026828216313, -15.39938930500394498 ) ) ;
#45363=CARTESIAN_POINT ( 'NONE',  ( -0.9554805223982675288, 45.45499091158017535, 18.31010292441292364 ) ) ;
#45400=B_SPLINE_CURVE_WITH_KNOTS ( 'NONE', 3,
 ( #59954, #100377, #84205, #50744, #18977, #85266, #27071, #92821, #26540, #59412, #92276, #3288, #18430, #10819, #10301, #51285, #99846, #58878, #93367, #36228 ),
 .UNSPECIFIED., .F., .F.,
 ( 4, 2, 2, 2, 2, 2, 2, 2, 2, 4 ),
 ( 0.007276925029303864083, 0.007780880140201501885, 0.008284835251099140555, 0.008788790361996777489, 0.009292745472894416159, 0.009796700583792054828, 0.01030065569468969176, 0.01080461080558733043, 0.01105658836103614803, 0.01130856591648496563 ),
 .UNSPECIFIED. ) ;
#45420=CARTESIAN_POINT ( 'NONE',  ( 0.000000000000000000, 47.77514352166374323, -11.96035173608223090 ) ) ;
#45425=VERTEX_POINT ( 'NONE', #23043 ) ;
#45442=CARTESIAN_POINT ( 'NONE',  ( 5.934563312262005397, 54.01391609258696036, -6.164477179060972034 ) ) ;
#45447=MECHANICAL_DESIGN_GEOMETRIC_PRESENTATION_REPRESENTATION('',(#71067),#95408);
#45478=CARTESIAN_POINT ( 'NONE',  ( 47.36344235967300875, 18.16811379743735344, -14.54383657267871577 ) ) ;
#45495=CARTESIAN_POINT ( 'NONE',  ( -8.717040642419030760, 53.90705534479965166, -1.531152949374502192 ) ) ;
#45497=CARTESIAN_POINT ( 'NONE',  ( 4.181903434330047631, 51.73312897152540302, -7.942462034357892442 ) ) ;
#45501=CARTESIAN_POINT ( 'NONE',  ( -22.88609270656953143, 26.05164082683736737, -30.73907939488839602 ) ) ;
#45508=CARTESIAN_POINT ( 'NONE',  ( -48.02835407290534420, 14.94086294439724227, -16.85535821593460426 ) ) ;
#45520=FILL_AREA_STYLE_COLOUR ( '', #4628 ) ;
#45545=CARTESIAN_POINT ( 'NONE',  ( 48.49405853457110283, 15.66070211563104131, -14.43943585503448723 ) ) ;
#45552=CARTESIAN_POINT ( 'NONE',  ( 4.506530263362012789, 52.18350610267697220, 6.292767562283435367 ) ) ;
#45599=CIRCLE ( 'NONE', #43884, 11.27631144943088515 ) ;
#45606=CARTESIAN_POINT ( 'NONE',  ( 4.180739497430161933, 54.25981830507254955, -6.682218162442597809 ) ) ;
#45617=ORIENTED_EDGE ( 'NONE', *, *, #23551, .F. ) ;
#45656=ORIENTED_EDGE ( 'NONE', *, *, #102133, .F. ) ;
#45661=CARTESIAN_POINT ( 'NONE',  ( -8.559508646656370345, 51.55638410492942114, 4.031152949374564365 ) ) ;
#45672=VECTOR ( 'NONE', #46621, 1000.000000000000000 ) ;
#45678=SURFACE_STYLE_USAGE ( .BOTH. , #76427 ) ;
#45684=CARTESIAN_POINT ( 'NONE',  ( 9.185096382416778837, 44.03884783307326956, 13.56034858340154337 ) ) ;
#45709=VERTEX_POINT ( 'NONE', #100086 ) ;
#45715=EDGE_CURVE ( 'NONE', #46319, #32781, #26782, .T. ) ;
#45732=COLOUR_RGB ( '', 0.09019608, 0.27058824, 0.51372549) ;
#45787=CARTESIAN_POINT ( 'NONE',  ( -49.27997219161970577, 7.868281554635428776, 15.62830927991589647 ) ) ;
#45795=CARTESIAN_POINT ( 'NONE',  ( -30.80770627799311967, 8.073552547385885347, 41.40953488888247591 ) ) ;
#45831=CARTESIAN_POINT ( 'NONE',  ( 30.23165830866633996, 7.786015354292205259, -41.98067155130507189 ) ) ;
#45836=FACE_OUTER_BOUND ( 'NONE', #44875, .T. ) ;
#45873=CARTESIAN_POINT ( 'NONE',  ( -10.28624191511816832, 43.25714326066847804, -15.40779740156204980 ) ) ;
#45883=MECHANICAL_DESIGN_GEOMETRIC_PRESENTATION_REPRESENTATION('',(#101162),#97754);
#45894=CARTESIAN_POINT ( 'NONE',  ( 10.28624191511840458, 43.99263840937192782, 12.90779740156148847 ) ) ;
#45898=SURFACE_SIDE_STYLE ('',( #14558 ) ) ;
#45903=CARTESIAN_POINT ( 'NONE',  ( -15.50566716382173738, 34.92505762992946927, 22.93027035652926315 ) ) ;
#45918=FILL_AREA_STYLE_COLOUR ( '', #97736 ) ;
#45924=CARTESIAN_POINT ( 'NONE',  ( 37.56673239365870387, 27.60449318992555945, 13.45617127780999134 ) ) ;
#45927=CARTESIAN_POINT ( 'NONE',  ( -47.57308385268305528, 17.76309546253597560, 14.43907613026821757 ) ) ;
#45950=B_SPLINE_CURVE_WITH_KNOTS ( 'NONE', 3,
 ( #556, #66947, #87910, #29191, #52879, #36213, #54439, #12935, #46385, #79274, #85806, #3273, #53420, #104073, #4330, #11880, #29704, #95462 ),
 .UNSPECIFIED., .F., .F.,
 ( 4, 2, 2, 2, 2, 2, 2, 2, 4 ),
 ( 0.007125849503216023610, 0.007630052828287927844, 0.008134256153359832944, 0.008638459478431736310, 0.009142662803503641411, 0.009646866128575546512, 0.01015106945364745161, 0.01065527277871935498, 0.01115947610379126008 ),
 .UNSPECIFIED. ) ;
#45958=CARTESIAN_POINT ( 'NONE',  ( -27.10511071441183262, 34.47735702144344572, 10.05698433968616001 ) ) ;
#45960=CARTESIAN_POINT ( 'NONE',  ( -17.15361759915034412, 37.01177862285504006, 21.87054431129721621 ) ) ;
#45961=UNCERTAINTY_MEASURE_WITH_UNIT (LENGTH_MEASURE( 1.000000000000000082E-05 ), #67594, 'distance_accuracy_value', 'NONE');
#45969=CARTESIAN_POINT ( 'NONE',  ( 5.618297568691034805, 54.12964757744262556, -6.031152949374448013 ) ) ;
#45999=CARTESIAN_POINT ( 'NONE',  ( 11.49412716574625115, 45.59192006558699006, -13.79863126508847948 ) ) ;
#46027=COLOUR_RGB ( '', 0.40784314, 0.44705882, 0.49803922) ;
#46031=COLOUR_RGB ( '', 0.31764706, 0.68627451, 0.89019608) ;
#46032=CARTESIAN_POINT ( 'NONE',  ( 27.42642194216384866, 34.37160210622304390, -10.02587544220627080 ) ) ;
#46067=DIRECTION ( 'NONE',  ( -0.000000000000000000, 1.000000000000000000, 0.000000000000000000 ) ) ;
#46072=CARTESIAN_POINT ( 'NONE',  ( 0.000000000000000000, 0.000000000000000000, 33.82893434829263413 ) ) ;
#46096=DIRECTION ( 'NONE',  ( 0.000000000000000000, 0.000000000000000000, 1.000000000000000000 ) ) ;
#46097=DIRECTION ( 'NONE',  ( 0.000000000000000000, 1.000000000000000000, 0.000000000000000000 ) ) ;
#46117=ADVANCED_FACE ( 'NONE', ( #68961 ), #67357, .F. ) ;
#46122=ORIENTED_EDGE ( 'NONE', *, *, #27480, .T. ) ;
#46129=CARTESIAN_POINT ( 'NONE',  ( 1.625879232102889042E-15, 0.000000000000000000, -13.27631144943088515 ) ) ;
#46138=CARTESIAN_POINT ( 'NONE',  ( -17.40604945778709478, 45.37707562542235706, -6.412274061844375872 ) ) ;
#46147=CARTESIAN_POINT ( 'NONE',  ( 23.38277283915452642, 28.07830159701457617, -30.71447743823567933 ) ) ;
#46148=EDGE_LOOP ( 'NONE', ( #62562, #40879, #53015, #51867 ) ) ;
#46154=EDGE_CURVE ( 'NONE', #32665, #92392, #48455, .T. ) ;
#46167=ORIENTED_EDGE ( 'NONE', *, *, #10199, .T. ) ;
#46171=LINE ( 'NONE', #102813, #10100 ) ;
#46175=ORIENTED_EDGE ( 'NONE', *, *, #102523, .F. ) ;
#46199=CARTESIAN_POINT ( 'NONE',  ( -29.68315524076956180, 8.302504244945341227, 42.10535821593508388 ) ) ;
#46269=EDGE_LOOP ( 'NONE', ( #2522, #25555, #45105, #80481 ) ) ;
#46286=EDGE_LOOP ( 'NONE', ( #7014, #53317, #78646, #13603 ) ) ;
#46289=DIRECTION ( 'NONE',  ( -0.000000000000000000, 1.000000000000000000, 0.000000000000000000 ) ) ;
#46309=CARTESIAN_POINT ( 'NONE',  ( -26.94613670386046778, 36.94238681296033633, 7.556984339686012575 ) ) ;
#46313=CARTESIAN_POINT ( 'NONE',  ( 7.808002908774420270, 53.96896602587193570, -3.792909619549702516 ) ) ;
#46319=VERTEX_POINT ( 'NONE', #14935 ) ;
#46321=CARTESIAN_POINT ( 'NONE',  ( -38.19034542652883601, 27.40923537312541214, 13.30185581998165389 ) ) ;
#46325=ORIENTED_EDGE ( 'NONE', *, *, #106511, .F. ) ;
#46358=DIRECTION ( 'NONE',  ( -0.000000000000000000, -1.000000000000000000, -0.000000000000000000 ) ) ;
#46369=VERTEX_POINT ( 'NONE', #31172 ) ;
#46385=CARTESIAN_POINT ( 'NONE',  ( -18.00631980831517609, 36.44533851663729962, -23.17937010874027237 ) ) ;
#46394=CARTESIAN_POINT ( 'NONE',  ( -30.42269336643015620, 12.90989212739755665, -41.86604079465153916 ) ) ;
#46407=EDGE_CURVE ( 'NONE', #8098, #50266, #4532, .T. ) ;
#46415=CARTESIAN_POINT ( 'NONE',  ( -1.250939209597460522, 10.43205495851956499, 50.60755518596315028 ) ) ;
#46424=AXIS2_PLACEMENT_3D ( 'NONE', #84283, #36834, #28744 ) ;
#46440=FILL_AREA_STYLE_COLOUR ( '', #90271 ) ;
#46451=EDGE_LOOP ( 'NONE', ( #35557, #34904 ) ) ;
#46453=CARTESIAN_POINT ( 'NONE',  ( 17.39415106586603343, 34.16989912227196413, 24.14244565807133469 ) ) ;
#46472=ORIENTED_EDGE ( 'NONE', *, *, #43026, .T. ) ;
#46486=SURFACE_STYLE_FILL_AREA ( #935 ) ;
#46495=EDGE_CURVE ( 'NONE', #35442, #93186, #62218, .T. ) ;
#46515=CARTESIAN_POINT ( 'NONE',  ( -11.48443175375259706, 45.38933445805909628, 14.52341122396179784 ) ) ;
#46516=VERTEX_POINT ( 'NONE', #1394 ) ;
#46533=CARTESIAN_POINT ( 'NONE',  ( -9.325077861619707420, 53.46604456964644214, -3.783146714563820012 ) ) ;
#46552=CARTESIAN_POINT ( 'NONE',  ( 27.26512758450284579, 34.42275309689889440, -10.05698433968635719 ) ) ;
#46555=DIRECTION ( 'NONE',  ( 0.000000000000000000, 1.000000000000000000, -0.000000000000000000 ) ) ;
#46559=FILL_AREA_STYLE ('',( #13647 ) ) ;
#46560=FILL_AREA_STYLE ('',( #45520 ) ) ;
#46621=DIRECTION ( 'NONE',  ( -0.000000000000000000, 1.000000000000000000, -0.000000000000000000 ) ) ;
#46625=DIRECTION ( 'NONE',  ( 0.000000000000000000, 1.000000000000000000, -0.000000000000000000 ) ) ;
#46644=CARTESIAN_POINT ( 'NONE',  ( -16.75187969033532553, 37.11970326878314808, 21.80698433968612093 ) ) ;
#46651=CARTESIAN_POINT ( 'NONE',  ( 26.02965699499564067, 37.04750560174652207, 9.465197022839127783 ) ) ;
#46655=CARTESIAN_POINT ( 'NONE',  ( -24.20499783611711564, 27.76345924012371924, -31.17339665328801246 ) ) ;
#46661=CARTESIAN_POINT ( 'NONE',  ( -23.54482684487745558, 25.90709500613124305, 30.73892193297572462 ) ) ;
#46665=SURFACE_SIDE_STYLE ('',( #38598 ) ) ;
#46674=MECHANICAL_DESIGN_GEOMETRIC_PRESENTATION_REPRESENTATION('',(#7081),#70770);
#46693=CARTESIAN_POINT ( 'NONE',  ( 30.42698073564668348, 7.740609016700362943, 41.86289218232744958 ) ) ;
#46734=CARTESIAN_POINT ( 'NONE',  ( 9.041342019628906712, 43.82558486784927965, 14.35410957973725843 ) ) ;
#46767=ORIENTED_EDGE ( 'NONE', *, *, #9943, .F. ) ;
#46768=VERTEX_POINT ( 'NONE', #59962 ) ;
#46776=CARTESIAN_POINT ( 'NONE',  ( -8.559508646656389885, -1.200000000000000030E-05, -2.781152949374503081 ) ) ;
#46795=EDGE_CURVE ( 'NONE', #10346, #1638, #31316, .T. ) ;
#46799=ORIENTED_EDGE ( 'NONE', *, *, #106174, .F. ) ;
#46808=ORIENTED_EDGE ( 'NONE', *, *, #54205, .F. ) ;
#46809=ORIENTED_EDGE ( 'NONE', *, *, #12747, .T. ) ;
#46810=CARTESIAN_POINT ( 'NONE',  ( -28.32665330097506029, 36.29719140734747640, 9.120848346371911219 ) ) ;
#46839=CARTESIAN_POINT ( 'NONE',  ( -5.290067270632269114, 51.34639538792298907, -8.531152949374520844 ) ) ;
#46842=CARTESIAN_POINT ( 'NONE',  ( -48.69302399950120019, 8.421789753111537991, 16.66702170536941807 ) ) ;
#46847=CARTESIAN_POINT ( 'NONE',  ( -30.29857313018930043, 7.759641293511166715, 41.94607130693947994 ) ) ;
#46858=STYLED_ITEM ( 'NONE', ( #92503 ), #104728 ) ;
#46890=DIRECTION ( 'NONE',  ( 0.000000000000000000, 0.000000000000000000, 1.000000000000000000 ) ) ;
#46898=CARTESIAN_POINT ( 'NONE',  ( 0.6420442155082901614, 27.35818369227503766, -40.57569272667392823 ) ) ;
#46909=CARTESIAN_POINT ( 'NONE',  ( 4.651477914329386962E-14, 52.17923068443710832, 7.749999999999496403 ) ) ;
#46928=CARTESIAN_POINT ( 'NONE',  ( -1.168375522601847960, 9.594968509503763343, 50.96085163187699152 ) ) ;
#46943=CARTESIAN_POINT ( 'NONE',  ( -16.66900757617721140, 35.00972275561253610, 21.80698433968611383 ) ) ;
#46958=CARTESIAN_POINT ( 'NONE',  ( 29.68315524076926692, 13.47185074185900255, -42.10535821593530414 ) ) ;
#46997=CARTESIAN_POINT ( 'NONE',  ( -28.31912909058650385, 34.17181180593427570, 9.116382818698859580 ) ) ;
#47005=CARTESIAN_POINT ( 'NONE',  ( 6.367454298303730553, 53.78323910253516971, -6.627674447275911263 ) ) ;
#47006=CARTESIAN_POINT ( 'NONE',  ( 17.73901682283262105, 34.63608873438791846, -22.27400293357690586 ) ) ;
#47008=ORIENTED_EDGE ( 'NONE', *, *, #52102, .F. ) ;
#47022=ORIENTED_EDGE ( 'NONE', *, *, #14085, .F. ) ;
#47056=EDGE_LOOP ( 'NONE', ( #95753, #18531, #15369, #14454 ) ) ;
#47059=CARTESIAN_POINT ( 'NONE',  ( 16.11359103326339337, 37.20915759416860169, 21.97891983235034274 ) ) ;
#47061=CARTESIAN_POINT ( 'NONE',  ( -16.64348903516517098, -1.200000000000000030E-05, 6.657797401561654560 ) ) ;
#47062=CARTESIAN_POINT ( 'NONE',  ( -48.15279758643657004, 14.66099993221198616, -16.85535821593460426 ) ) ;
#47068=DIRECTION ( 'NONE',  ( 0.000000000000000000, 1.000000000000000000, 0.000000000000000000 ) ) ;
#47085=EDGE_CURVE ( 'NONE', #49001, #106068, #74377, .T. ) ;
#47090=SURFACE_SIDE_STYLE ('',( #88105 ) ) ;
#47093=CARTESIAN_POINT ( 'NONE',  ( -0.3599032852998504395, 13.03488328047065359, -51.69862933869767829 ) ) ;
#47115=CARTESIAN_POINT ( 'NONE',  ( 38.80499884327841187, 27.34286220386137245, 12.01623411786279760 ) ) ;
#47119=COLOUR_RGB ( '', 0.40784314, 0.44705882, 0.49803922) ;
#47133=CARTESIAN_POINT ( 'NONE',  ( -6.490443738817557318, 53.67433831593452709, 6.923344696077945670 ) ) ;
#47141=ORIENTED_EDGE ( 'NONE', *, *, #21536, .F. ) ;
#47173=CARTESIAN_POINT ( 'NONE',  ( 27.10511071441176867, -1.200000000000000030E-05, -8.806984339686344754 ) ) ;
#47179=CARTESIAN_POINT ( 'NONE',  ( -4.881589094946162888, 52.15742855003398404, -6.096815929868464323 ) ) ;
#47182=UNCERTAINTY_MEASURE_WITH_UNIT (LENGTH_MEASURE( 1.000000000000000082E-05 ), #105026, 'distance_accuracy_value', 'NONE');
#47185=CARTESIAN_POINT ( 'NONE',  ( -0.08419721950864400561, 43.17555810750859990, -18.75000000000000355 ) ) ;
#47194=CARTESIAN_POINT ( 'NONE',  ( 22.00857090122901027, 25.77073524871309829, -32.31114556117190517 ) ) ;
#47204=DIRECTION ( 'NONE',  ( -0.000000000000000000, 1.000000000000000000, -0.000000000000000000 ) ) ;
#47205=DIRECTION ( 'NONE',  ( 0.000000000000000000, 0.000000000000000000, 1.000000000000000000 ) ) ;
#47218=DIRECTION ( 'NONE',  ( 0.000000000000000000, -0.3420201433256727652, -0.9396926207859068736 ) ) ;
#47231=CARTESIAN_POINT ( 'NONE',  ( 48.02835407290545078, 16.78162100668605206, 14.35535821593427386 ) ) ;
#47238=SURFACE_SIDE_STYLE ('',( #88253 ) ) ;
#47278=CARTESIAN_POINT ( 'NONE',  ( -0.5681331142220417130, 54.25170640378875220, -7.883436127774885449 ) ) ;
#47302=CARTESIAN_POINT ( 'NONE',  ( 0.000000000000000000, 0.000000000000000000, 0.000000000000000000 ) ) ;
#47303=CARTESIAN_POINT ( 'NONE',  ( 1.100366063348540591, 25.39417708419738773, -40.11413014599601468 ) ) ;
#47308=EDGE_CURVE ( 'NONE', #81828, #101117, #68928, .T. ) ;
#47316=LINE ( 'NONE', #80212, #100263 ) ;
#47354=ORIENTED_EDGE ( 'NONE', *, *, #97004, .T. ) ;
#47361=CARTESIAN_POINT ( 'NONE',  ( 7.576187751213149468, 54.08017525257882596, -3.569500874023384895 ) ) ;
#47368=CARTESIAN_POINT ( 'NONE',  ( -48.76594521878733701, 8.294242253543364640, 16.61919356891297284 ) ) ;
#47374=CARTESIAN_POINT ( 'NONE',  ( 28.79633237789232325, 10.21664471455438772, 41.74470786255320576 ) ) ;
#47378=CARTESIAN_POINT ( 'NONE',  ( 28.43956359133950684, 17.90386495480485252, 40.70637206596285296 ) ) ;
#47405=CARTESIAN_POINT ( 'NONE',  ( -7.568397567301111017, 54.27789163617485713, -2.014810990348805841 ) ) ;
#47419=EDGE_CURVE ( 'NONE', #492, #49001, #86762, .T. ) ;
#47450=EDGE_CURVE ( 'NONE', #347, #85798, #4226, .T. ) ;
#47454=CARTESIAN_POINT ( 'NONE',  ( -0.2948623160389114428, 13.62334926694027892, 49.28320643957499669 ) ) ;
#47458=EDGE_LOOP ( 'NONE', ( #40266, #23964, #44659, #101427 ) ) ;
#47464=CARTESIAN_POINT ( 'NONE',  ( 22.01999690012047495, 28.11337147615395438, 31.58836928536987187 ) ) ;
#47466=FACE_OUTER_BOUND ( 'NONE', #53968, .T. ) ;
#47471=FACE_OUTER_BOUND ( 'NONE', #30377, .T. ) ;
#47472=ORIENTED_EDGE ( 'NONE', *, *, #34970, .T. ) ;
#47493=CARTESIAN_POINT ( 'NONE',  ( 37.24829320759891971, 27.71737586852629676, 13.42523556547244290 ) ) ;
#47502=( LENGTH_UNIT ( ) NAMED_UNIT ( * ) SI_UNIT ( .MILLI., .METRE. ) );
#47513=CARTESIAN_POINT ( 'NONE',  ( -29.35512824071851057, 13.99081654327141599, -42.06953762909878947 ) ) ;
#47525=DIRECTION ( 'NONE',  ( 0.000000000000000000, 0.000000000000000000, 1.000000000000000000 ) ) ;
#47545=CARTESIAN_POINT ( 'NONE',  ( 37.56673239365841255, -1.200000000000000030E-05, -12.20617127781092215 ) ) ;
#47569=CARTESIAN_POINT ( 'NONE',  ( 0.000000000000000000, 0.000000000000000000, 0.000000000000000000 ) ) ;
#47576=DIRECTION ( 'NONE',  ( 0.000000000000000000, 0.000000000000000000, 1.000000000000000000 ) ) ;
#47588=CARTESIAN_POINT ( 'NONE',  ( 15.55441737893109355, 37.11602535008575643, 22.68899775139442099 ) ) ;
#47590=CARTESIAN_POINT ( 'NONE',  ( 0.6444792390971975093, 43.23217435222382221, -18.58392088066086600 ) ) ;
#47591=CARTESIAN_POINT ( 'NONE',  ( -38.33028772603171319, 25.24378019603273415, 13.20968585612151536 ) ) ;
#47592=CARTESIAN_POINT ( 'NONE',  ( -48.49215721461931139, 15.66554462474931420, -14.43870166537744382 ) ) ;
#47607=DIRECTION ( 'NONE',  ( 1.150791560227848544E-16, -0.3420201433256727652, 0.9396926207859068736 ) ) ;
#47616=CARTESIAN_POINT ( 'NONE',  ( -37.56673239365971284, 27.88554838446211548, -10.95617127780556466 ) ) ;
#47625=ORIENTED_EDGE ( 'NONE', *, *, #7815, .T. ) ;
#47626=FILL_AREA_STYLE ('',( #6111 ) ) ;
#47631=( NAMED_UNIT ( * ) PLANE_ANGLE_UNIT ( ) SI_UNIT ( $, .RADIAN. ) );
#47640=CARTESIAN_POINT ( 'NONE',  ( 5.290067270632321517, 52.08006895350504095, 6.031152949374479100 ) ) ;
#47687=CARTESIAN_POINT ( 'NONE',  ( 27.10511071441197117, 34.47735702144345282, 10.05698433968570704 ) ) ;
#47702=FACE_OUTER_BOUND ( 'NONE', #87819, .T. ) ;
#47713=CARTESIAN_POINT ( 'NONE',  ( 1.990040563172386960E-15, 46.21383923812596350, 16.25000000000000000 ) ) ;
#47714=CARTESIAN_POINT ( 'NONE',  ( -10.28624191511830155, -1.200000000000000030E-05, -14.15779740156157018 ) ) ;
#47716=( GEOMETRIC_REPRESENTATION_CONTEXT ( 3 ) GLOBAL_UNCERTAINTY_ASSIGNED_CONTEXT ( ( #88198 ) ) GLOBAL_UNIT_ASSIGNED_CONTEXT ( ( #21090, #38316, #4329 ) ) REPRESENTATION_CONTEXT ( 'NONE', 'WORKASPACE' ) );
#47739=CARTESIAN_POINT ( 'NONE',  ( -10.12078790316828858, 44.02769531064037523, 12.91599879790107686 ) ) ;
#47754=CARTESIAN_POINT ( 'NONE',  ( 46.89590902281800311, 18.03207604452820689, 16.16381118462976474 ) ) ;
#47755=VECTOR ( 'NONE', #9234, 1000.000000000000000 ) ;
#47781=VECTOR ( 'NONE', #103536, 1000.000000000000114 ) ;
#47782=STYLED_ITEM ( 'NONE', ( #22545 ), #37891 ) ;
#47801=CARTESIAN_POINT ( 'NONE',  ( -2.637755229554568666E-21, 53.39766064372320642, -10.24999999999999822 ) ) ;
#47807=SURFACE_SIDE_STYLE ('',( #105008 ) ) ;
#47832=ORIENTED_EDGE ( 'NONE', *, *, #46795, .T. ) ;
#47833=FACE_OUTER_BOUND ( 'NONE', #59184, .T. ) ;
#47854=CARTESIAN_POINT ( 'NONE',  ( 21.98993715557173800, 25.96775721187310637, 31.66727678396639334 ) ) ;
#47871=DIRECTION ( 'NONE',  ( -0.000000000000000000, 1.000000000000000000, 0.000000000000000000 ) ) ;
#47875=DIRECTION ( 'NONE',  ( 0.000000000000000000, 0.000000000000000000, 1.000000000000000000 ) ) ;
#47878=DIRECTION ( 'NONE',  ( 1.000000000000000000, 0.000000000000000000, 0.000000000000000000 ) ) ;
#47884=( NAMED_UNIT ( * ) PLANE_ANGLE_UNIT ( ) SI_UNIT ( $, .RADIAN. ) );
#47895=DIRECTION ( 'NONE',  ( 0.000000000000000000, 0.000000000000000000, 1.000000000000000000 ) ) ;
#47907=CARTESIAN_POINT ( 'NONE',  ( -16.48411172411860903, 43.52942502979619377, -6.657797401562040918 ) ) ;
#47908=CARTESIAN_POINT ( 'NONE',  ( 5.290067270632161645, -1.200000000000000030E-05, -7.281152949374595451 ) ) ;
#47919=MECHANICAL_DESIGN_GEOMETRIC_PRESENTATION_REPRESENTATION('',(#106526),#22187);
#47926=ORIENTED_EDGE ( 'NONE', *, *, #32464, .F. ) ;
#47939=CARTESIAN_POINT ( 'NONE',  ( 0.000000000000000000, 41.79151656018385097, 0.000000000000000000 ) ) ;
#47959=MECHANICAL_DESIGN_GEOMETRIC_PRESENTATION_REPRESENTATION('',(#56586),#91043);
#47963=CARTESIAN_POINT ( 'NONE',  ( 48.28161701412305717, 14.38519811849424990, 16.83766359355561093 ) ) ;
#47976=ORIENTED_EDGE ( 'NONE', *, *, #73557, .F. ) ;
#47989=EDGE_CURVE ( 'NONE', #59570, #96544, #18696, .T. ) ;
#47996=CARTESIAN_POINT ( 'NONE',  ( -15.50010513532795642, 34.90187412562523406, 23.01084172723449939 ) ) ;
#47997=ORIENTED_EDGE ( 'NONE', *, *, #57053, .T. ) ;
#48007=DIRECTION ( 'NONE',  ( 0.000000000000000000, 0.000000000000000000, -1.000000000000000000 ) ) ;
#48017=DIRECTION ( 'NONE',  ( 0.000000000000000000, 0.000000000000000000, -1.000000000000000000 ) ) ;
#48019=CARTESIAN_POINT ( 'NONE',  ( 25.85848788125878528, 35.03499038825931677, -8.997391814579291491 ) ) ;
#48027=CARTESIAN_POINT ( 'NONE',  ( 0.3381073927595607542, 25.18058069739937821, 40.71490780997189773 ) ) ;
#48035=CARTESIAN_POINT ( 'NONE',  ( -28.49053509030305520, 18.29756676117400005, -40.46890581211962967 ) ) ;
#48046=CARTESIAN_POINT ( 'NONE',  ( 0.000000000000000000, 0.000000000000000000, 0.000000000000000000 ) ) ;
#48061=EDGE_CURVE ( 'NONE', #62849, #41885, #66218, .T. ) ;
#48068=DIRECTION ( 'NONE',  ( 0.000000000000000000, 0.000000000000000000, 1.000000000000000000 ) ) ;
#48070=CARTESIAN_POINT ( 'NONE',  ( 27.10511071441204578, 34.75829513984540142, 7.556984339685363317 ) ) ;
#48071=CYLINDRICAL_SURFACE ( 'NONE', #15196, 1.250000000000001110 ) ;
#48074=CARTESIAN_POINT ( 'NONE',  ( 0.000000000000000000, 29.56666008184760130, -34.51297463494397988 ) ) ;
#48082=CONICAL_SURFACE ( 'NONE', #46424, 34.51297463494397988, 1.221730476396026610 ) ;
#48109=EDGE_CURVE ( 'NONE', #79581, #55752, #51979, .T. ) ;
#48119=CARTESIAN_POINT ( 'NONE',  ( 1.250250887278956835, 43.55730586753710298, -17.65695166392345428 ) ) ;
#48124=EDGE_CURVE ( 'NONE', #45709, #12173, #60642, .T. ) ;
#48148=CARTESIAN_POINT ( 'NONE',  ( -38.18740872092708827, 27.41008126919087928, -13.30320916973952627 ) ) ;
#48158=DIRECTION ( 'NONE',  ( 0.000000000000000000, 0.000000000000000000, -1.000000000000000000 ) ) ;
#48169=CARTESIAN_POINT ( 'NONE',  ( 1.250721446675217452, 51.63789146372492667, -9.152276705697273584 ) ) ;
#48173=CARTESIAN_POINT ( 'NONE',  ( 38.31552673953900268, 27.59984468902660026, 11.19255079935879849 ) ) ;
#48181=ORIENTED_EDGE ( 'NONE', *, *, #99945, .T. ) ;
#48189=CARTESIAN_POINT ( 'NONE',  ( -6.526324006461421412, 53.62377623897270240, 7.079659290374570091 ) ) ;
#48206=ORIENTED_EDGE ( 'NONE', *, *, #82117, .T. ) ;
#48218=CARTESIAN_POINT ( 'NONE',  ( 28.19101533190163522, 34.18031863878626808, 9.431734573481964645 ) ) ;
#48223=CARTESIAN_POINT ( 'NONE',  ( -22.43229796258882658, 26.08192010338115097, 30.96913259774117577 ) ) ;
#48227=SURFACE_STYLE_USAGE ( .BOTH. , #39647 ) ;
#48237=CARTESIAN_POINT ( 'NONE',  ( -24.00177444567219354, 25.16455187703150997, 32.94427520949815857 ) ) ;
#48254=EDGE_CURVE ( 'NONE', #21252, #104058, #13641, .T. ) ;
#48255=CARTESIAN_POINT ( 'NONE',  ( 46.81343110146973885, 13.24251555485277443, -15.91224400466348676 ) ) ;
#48262=FILL_AREA_STYLE ('',( #64479 ) ) ;
#48269=CARTESIAN_POINT ( 'NONE',  ( -9.034516203396696810, 43.90155024610201195, 14.11102724417178678 ) ) ;
#48286=CARTESIAN_POINT ( 'NONE',  ( 47.14583847125359739, 17.20522387600192715, 16.50112645797992528 ) ) ;
#48304=CARTESIAN_POINT ( 'NONE',  ( -37.56673239365863282, -1.200000000000000030E-05, -10.95617127781024536 ) ) ;
#48310=( NAMED_UNIT ( * ) PLANE_ANGLE_UNIT ( ) SI_UNIT ( $, .RADIAN. ) );
#48315=ADVANCED_FACE ( 'NONE', ( #38487, #71350, #30397, #78916, #61161 ), #94349, .F. ) ;
#48320=CARTESIAN_POINT ( 'NONE',  ( 29.87260017596017292, 13.22901743408738717, 42.09629626707183547 ) ) ;
#48346=COLOUR_RGB ( '', 0.72549020, 0.75294118, 0.79215686) ;
#48370=CARTESIAN_POINT ( 'NONE',  ( -0.8391198807171517116, 34.96075513128997159, -27.56988711285785953 ) ) ;
#48404=CARTESIAN_POINT ( 'NONE',  ( 9.658328022721198280, 45.55814826547295837, -15.25063005797932014 ) ) ;
#48409=VECTOR ( 'NONE', #32366, 1000.000000000000000 ) ;
#48415=UNCERTAINTY_MEASURE_WITH_UNIT (LENGTH_MEASURE( 1.000000000000000082E-05 ), #75956, 'distance_accuracy_value', 'NONE');
#48443=CARTESIAN_POINT ( 'NONE',  ( -28.09909703978631867, 36.32432838617303617, -9.569561972001043415 ) ) ;
#48455=B_SPLINE_CURVE_WITH_KNOTS ( 'NONE', 3,
 ( #77027, #101832, #60864, #10163, #43076, #93753, #75964, #96419, #5277, #55392, #102906, #94831, #29583, #54862, #79150, #14395, #20977, #53810, #86741, #88322 ),
 .UNSPECIFIED., .F., .F.,
 ( 4, 2, 2, 2, 2, 2, 2, 2, 2, 4 ),
 ( 0.002962320935262360670, 0.003468250424844080467, 0.003974179914425800264, 0.004480109404007520495, 0.004986038893589240725, 0.005491968383170961823, 0.005744933127961822372, 0.005997897872752681186, 0.006503827362334404019, 0.007009756851916126852 ),
 .UNSPECIFIED. ) ;
#48457=CARTESIAN_POINT ( 'NONE',  ( -27.10511071441183617, 34.75829513984614039, 7.556984339678626483 ) ) ;
#48460=CARTESIAN_POINT ( 'NONE',  ( 11.24754375996996991, 43.18744335144261726, -14.96124022301595424 ) ) ;
#48469=CARTESIAN_POINT ( 'NONE',  ( -46.96202111036851790, 13.62308641270877985, 14.94990935055617953 ) ) ;
#48476=SURFACE_STYLE_FILL_AREA ( #97553 ) ;
#48494=CARTESIAN_POINT ( 'NONE',  ( -17.71335089818147424, 34.18409044421883181, -23.86027278727303624 ) ) ;
#48496=DIRECTION ( 'NONE',  ( -0.000000000000000000, 1.000000000000000000, -0.000000000000000000 ) ) ;
#48508=ORIENTED_EDGE ( 'NONE', *, *, #62756, .F. ) ;
#48513=CARTESIAN_POINT ( 'NONE',  ( 8.559508646656398767, 51.83514083332404709, 1.531152949374243510 ) ) ;
#48518=CARTESIAN_POINT ( 'NONE',  ( 28.08046125550390926, 34.37078321048628737, -8.021011108984579252 ) ) ;
#48524=CARTESIAN_POINT ( 'NONE',  ( 22.65274949039523023, 28.20149500596346925, 30.83785112677286477 ) ) ;
#48555=CARTESIAN_POINT ( 'NONE',  ( 26.01059492157061115, 35.07599308518503278, -8.179937502207174305 ) ) ;
#48556=DIRECTION ( 'NONE',  ( 0.000000000000000000, 1.000000000000000000, -0.000000000000000000 ) ) ;
#48557=CARTESIAN_POINT ( 'NONE',  ( -28.45466774514982333, 11.90937068246394048, -41.11752270887390637 ) ) ;
#48561=CARTESIAN_POINT ( 'NONE',  ( 38.18636683152726619, 25.28304573692243551, 13.29490163854971385 ) ) ;
#48567=DIRECTION ( 'NONE',  ( 0.000000000000000000, 0.000000000000000000, 1.000000000000000000 ) ) ;
#48575=EDGE_CURVE ( 'NONE', #69405, #35442, #39115, .T. ) ;
#48586=CARTESIAN_POINT ( 'NONE',  ( 29.33036678664061014, 18.69950024370078978, -39.65481841613269154 ) ) ;
#48614=ORIENTED_EDGE ( 'NONE', *, *, #80414, .T. ) ;
#48627=CARTESIAN_POINT ( 'NONE',  ( -6.046331486648977460, 53.95713668298893140, -6.273411955836167841 ) ) ;
#48631=CARTESIAN_POINT ( 'NONE',  ( -24.46403792248046472, 27.44444016472271031, 32.08006538382075234 ) ) ;
#48644=CARTESIAN_POINT ( 'NONE',  ( 0.000000000000000000, 36.79151656018385097, 0.000000000000000000 ) ) ;
#48647=CARTESIAN_POINT ( 'NONE',  ( -38.56574518832086085, 25.19011887711810260, 12.97560723393621984 ) ) ;
#48654=COLOUR_RGB ( '', 0.72549020, 0.75294118, 0.79215686) ;
#48664=CARTESIAN_POINT ( 'NONE',  ( -22.81472563493007399, 27.48372958372127073, -33.14224123365035979 ) ) ;
#48690=CARTESIAN_POINT ( 'NONE',  ( 0.3382572194634697604, 34.18413605192029792, -29.71481628158403865 ) ) ;
#48713=CARTESIAN_POINT ( 'NONE',  ( -9.735143570771413124, 51.35512128393092723, -2.348594097114156565 ) ) ;
#48714=FACE_BOUND ( 'NONE', #61279, .T. ) ;
#48742=CARTESIAN_POINT ( 'NONE',  ( 28.08684260795691401, 34.36902632031492999, 8.016442903659967811 ) ) ;
#48753=ORIENTED_EDGE ( 'NONE', *, *, #15666, .T. ) ;
#48754=CARTESIAN_POINT ( 'NONE',  ( -16.64348903516521005, 45.88445698070336221, -4.157797401561533768 ) ) ;
#48764=ADVANCED_FACE ( 'NONE', ( #6314 ), #95352, .F. ) ;
#48773=CARTESIAN_POINT ( 'NONE',  ( 1.249410016421840464, 45.80241883944731995, 17.33540574942934143 ) ) ;
#48777=CARTESIAN_POINT ( 'NONE',  ( -10.12154985177026845, 46.15835141668621588, 12.90779740156129130 ) ) ;
#48785=CARTESIAN_POINT ( 'NONE',  ( 1.090085246657715112, 54.05151059601869434, 8.383057650847046460 ) ) ;
#48795=CARTESIAN_POINT ( 'NONE',  ( 30.93151921796046011, 9.249586871975902014, 40.69907933257861998 ) ) ;
#48797=CARTESIAN_POINT ( 'NONE',  ( 8.881504343373315180, 51.45494909527817384, -3.999881655714555784 ) ) ;
#48812=CARTESIAN_POINT ( 'NONE',  ( 47.78256487607184511, 15.50824688150972008, 16.83670797542556130 ) ) ;
#48821=( LENGTH_UNIT ( ) NAMED_UNIT ( * ) SI_UNIT ( .MILLI., .METRE. ) );
#48838=CARTESIAN_POINT ( 'NONE',  ( -1.218909386241671555, 43.73109126565793048, 17.18057086054097127 ) ) ;
#48842=CARTESIAN_POINT ( 'NONE',  ( 0.000000000000000000, 24.35682532067546902, -46.94949242731048145 ) ) ;
#48852=EDGE_LOOP ( 'NONE', ( #104359, #7540, #102546, #36353 ) ) ;
#48866=SURFACE_STYLE_USAGE ( .BOTH. , #91488 ) ;
#48873=COLOUR_RGB ( '', 0.40784314, 0.44705882, 0.49803922) ;
#48893=FILL_AREA_STYLE ('',( #90439 ) ) ;
#48932=B_SPLINE_CURVE_WITH_KNOTS ( 'NONE', 3,
 ( #32090, #80080, #46147, #38085, #14812, #73035, #70942, #88721, #103834, #24017, #29979, #54735, #62867, #105945, #64453, #95752, #14281, #63930, #72000, #97326, #89253, #21894, #40159, #87671 ),
 .UNSPECIFIED., .F., .F.,
 ( 4, 2, 2, 2, 2, 2, 2, 2, 2, 2, 2, 4 ),
 ( 0.004982639409921950195, 0.005234721249241282466, 0.005486803088560614737, 0.005990966767199287953, 0.006495130445837961168, 0.006999294124476635251, 0.007251375963795970991, 0.007503457803115307599, 0.008007621481753979947, 0.008511785160392651428, 0.008763866999711987169, 0.009015948839031322909 ),
 .UNSPECIFIED. ) ;
#48938=CARTESIAN_POINT ( 'NONE',  ( 7.561938253469114635, 54.28095178519542685, -2.009802758568550285 ) ) ;
#48951=STYLED_ITEM ( 'NONE', ( #98488 ), #85152 ) ;
#48954=SURFACE_STYLE_FILL_AREA ( #6378 ) ;
#48956=CARTESIAN_POINT ( 'NONE',  ( 28.56680886105595008, 18.54011861096320501, 40.29036177351405712 ) ) ;
#48983=CARTESIAN_POINT ( 'NONE',  ( -25.99577189627797935, 34.94014516354030064, 9.388825123540007311 ) ) ;
#48984=CARTESIAN_POINT ( 'NONE',  ( 11.49357173040307778, 43.46406798798316373, -13.79729247989035557 ) ) ;
#48993=CARTESIAN_POINT ( 'NONE',  ( -46.97259151695102730, 12.59255281441348728, 16.28847157548942448 ) ) ;
#49000=SURFACE_STYLE_USAGE ( .BOTH. , #39877 ) ;
#49001=VERTEX_POINT ( 'NONE', #58063 ) ;
#49020=MECHANICAL_DESIGN_GEOMETRIC_PRESENTATION_REPRESENTATION('',(#4247),#21521);
#49024=CARTESIAN_POINT ( 'NONE',  ( -17.97954184224904495, 34.27542366261327800, -23.34466436009411083 ) ) ;
#49037=VERTEX_POINT ( 'NONE', #53184 ) ;
#49041=CARTESIAN_POINT ( 'NONE',  ( 8.881086064414537518, 51.45508042954168104, 3.999917844499591535 ) ) ;
#49068=CARTESIAN_POINT ( 'NONE',  ( -38.78856572157635441, 25.16510362771173703, -12.51935735473968592 ) ) ;
#49082=CARTESIAN_POINT ( 'NONE',  ( 25.89606338949664277, 35.00197463208161963, -9.163675292473188350 ) ) ;
#49086=CARTESIAN_POINT ( 'NONE',  ( 37.72659966023548606, 25.70133307342159057, 10.95617127780997180 ) ) ;
#49087=CARTESIAN_POINT ( 'NONE',  ( 1.126303995421776394, 25.38703625300498601, 40.13366474932937678 ) ) ;
#49092=CARTESIAN_POINT ( 'NONE',  ( -28.54518584606556431, 18.48129625438333790, -40.33591358207613098 ) ) ;
#49094=SURFACE_SIDE_STYLE ('',( #42611 ) ) ;
#49099=CARTESIAN_POINT ( 'NONE',  ( 23.54214819851715390, 25.90553154796090141, 30.74632383150428083 ) ) ;
#49113=CARTESIAN_POINT ( 'NONE',  ( 29.09597697838555064, 14.54318144277619496, -41.96748357178393007 ) ) ;
#49125=DIRECTION ( 'NONE',  ( -0.000000000000000000, -1.000000000000000000, -0.000000000000000000 ) ) ;
#49127=DIRECTION ( 'NONE',  ( -0.000000000000000000, 1.000000000000000000, 0.000000000000000000 ) ) ;
#49161=CARTESIAN_POINT ( 'NONE',  ( -23.38277283915476445, 28.07830159701456907, 30.71447743823551235 ) ) ;
#49181=CARTESIAN_POINT ( 'NONE',  ( -38.66164730681681050, 25.17357370736559474, 12.83228708202576307 ) ) ;
#49190=DIRECTION ( 'NONE',  ( 0.000000000000000000, 0.000000000000000000, 1.000000000000000000 ) ) ;
#49191=EDGE_LOOP ( 'NONE', ( #2369, #11854, #68358, #42421 ) ) ;
#49210=( NAMED_UNIT ( * ) SI_UNIT ( $, .STERADIAN. ) SOLID_ANGLE_UNIT ( ) );
#49216=CARTESIAN_POINT ( 'NONE',  ( 2.845670519300376476E-15, 38.67090180175566871, 23.23666318551310539 ) ) ;
#49220=SURFACE_SIDE_STYLE ('',( #90224 ) ) ;
#49231=CARTESIAN_POINT ( 'NONE',  ( 49.22360526642682998, 7.740778690624840586, 15.97911514197205030 ) ) ;
#49247=CARTESIAN_POINT ( 'NONE',  ( 37.24678017888829373, 25.86898843256250302, 10.95617127780997535 ) ) ;
#49277=CARTESIAN_POINT ( 'NONE',  ( 28.04511907431318818, 34.20682782302920799, 9.635168561359211736 ) ) ;
#49293=CARTESIAN_POINT ( 'NONE',  ( -4.044731509663068714, 51.90665404057882881, -7.475086770086759813 ) ) ;
#49298=CARTESIAN_POINT ( 'NONE',  ( 0.6455896130745356620, 52.10958058375629776, 7.916501336716939896 ) ) ;
#49304=CARTESIAN_POINT ( 'NONE',  ( 0.8352780885855292103, 18.10189008090095797, -49.56687221457461590 ) ) ;
#49308=CARTESIAN_POINT ( 'NONE',  ( 22.65138445058343208, 26.07323991223989168, -30.83851241702902612 ) ) ;
#49312=ORIENTED_EDGE ( 'NONE', *, *, #84019, .T. ) ;
#49313=EDGE_CURVE ( 'NONE', #29960, #9249, #58394, .T. ) ;
#49319=ORIENTED_EDGE ( 'NONE', *, *, #90395, .T. ) ;
#49320=CARTESIAN_POINT ( 'NONE',  ( 0.9512138561578256102, 54.12926960197279413, 8.184984789997367116 ) ) ;
#49328=CARTESIAN_POINT ( 'NONE',  ( -10.28624191511820207, 43.99263840937192782, 12.90779740156163768 ) ) ;
#49350=DIRECTION ( 'NONE',  ( 0.000000000000000000, 1.000000000000000000, 0.000000000000000000 ) ) ;
#49362=DIRECTION ( 'NONE',  ( -0.000000000000000000, 1.000000000000000000, 0.000000000000000000 ) ) ;
#49367=CARTESIAN_POINT ( 'NONE',  ( -0.6416280306071847628, 26.01284353103483227, -38.42409783453992844 ) ) ;
#49432=EDGE_LOOP ( 'NONE', ( #80848, #53542, #63244, #42790 ) ) ;
#49444=CARTESIAN_POINT ( 'NONE',  ( 47.03691741412936267, 13.53106325772396268, 14.84138715777531381 ) ) ;
#49468=LINE ( 'NONE', #106642, #33309 ) ;
#49480=CARTESIAN_POINT ( 'NONE',  ( 7.311243580803559183, 54.26735737584581187, -2.887849316459860205 ) ) ;
#49481=UNCERTAINTY_MEASURE_WITH_UNIT (LENGTH_MEASURE( 1.000000000000000082E-05 ), #1970, 'distance_accuracy_value', 'NONE');
#49499=CARTESIAN_POINT ( 'NONE',  ( 28.56337834059337055, 13.37291324415828875, 40.29174292248561784 ) ) ;
#49528=CARTESIAN_POINT ( 'NONE',  ( 10.28624191511773844, 43.25714326066793092, -15.40779740156427202 ) ) ;
#49531=ORIENTED_EDGE ( 'NONE', *, *, #77389, .F. ) ;
#49536=CARTESIAN_POINT ( 'NONE',  ( -47.55643143940722695, 10.90089820249354879, 16.76894861493079603 ) ) ;
#49545=CARTESIAN_POINT ( 'NONE',  ( 9.539861337244017747, 53.58159379677093170, 1.989136213324401492 ) ) ;
#49552=CARTESIAN_POINT ( 'NONE',  ( -30.93146042459081002, 14.42085588385339712, 40.69811146320443385 ) ) ;
#49568=CARTESIAN_POINT ( 'NONE',  ( -17.83068241833874623, 34.57775873570747649, -22.40589842973222900 ) ) ;
#49571=CARTESIAN_POINT ( 'NONE',  ( -5.689124116752916294, 51.96569795582090734, -6.093860943101484295 ) ) ;
#49593=FILL_AREA_STYLE_COLOUR ( '', #53831 ) ;
#49598=EDGE_CURVE ( 'NONE', #41885, #62849, #100784, .T. ) ;
#49613=AXIS2_PLACEMENT_3D ( 'NONE', #12302, #20469, #28534 ) ;
#49614=LINE ( 'NONE', #89558, #63877 ) ;
#49627=FACE_OUTER_BOUND ( 'NONE', #75238, .T. ) ;
#49632=CARTESIAN_POINT ( 'NONE',  ( 0.6448156900331544206, 25.22696244642840924, 40.58375750131497028 ) ) ;
#49639=FACE_OUTER_BOUND ( 'NONE', #55375, .T. ) ;
#49642=CARTESIAN_POINT ( 'NONE',  ( 23.29962249077899727, 25.97067266342275715, 30.70617127781015654 ) ) ;
#49645=CARTESIAN_POINT ( 'NONE',  ( 5.290067270632397012, 54.20842449845690680, 6.031152949374294359 ) ) ;
#49650=CARTESIAN_POINT ( 'NONE',  ( -4.038444544431111893, 51.98515651805179516, 7.232149228015535947 ) ) ;
#49657=CARTESIAN_POINT ( 'NONE',  ( 28.61312531052607255, 18.65874454358747769, -40.19656138064517137 ) ) ;
#49669=FACE_BOUND ( 'NONE', #5288, .T. ) ;
#49684=ORIENTED_EDGE ( 'NONE', *, *, #31393, .F. ) ;
#49691=STYLED_ITEM ( 'NONE', ( #10562 ), #1263 ) ;
#49697=CARTESIAN_POINT ( 'NONE',  ( 0.000000000000000000, 57.12835554495183032, 0.000000000000000000 ) ) ;
#49708=CARTESIAN_POINT ( 'NONE',  ( -23.97799606807676298, 27.87796489320411197, 30.95132209396226486 ) ) ;
#49721=CARTESIAN_POINT ( 'NONE',  ( 16.42611686831694939, 36.46285186709819470, 24.26654634025072355 ) ) ;
#49744=AXIS2_PLACEMENT_3D ( 'NONE', #32774, #65647, #57530 ) ;
#49751=( NAMED_UNIT ( * ) PLANE_ANGLE_UNIT ( ) SI_UNIT ( $, .RADIAN. ) );
#49752=ORIENTED_EDGE ( 'NONE', *, *, #38224, .T. ) ;
#49755=CARTESIAN_POINT ( 'NONE',  ( 38.66172427885771157, 27.30186337571333155, -12.83265428641589523 ) ) ;
#49758=CARTESIAN_POINT ( 'NONE',  ( 10.28624191511840280, 46.12099395432375104, 12.90779740156148847 ) ) ;
#49775=CARTESIAN_POINT ( 'NONE',  ( 49.02741474918247633, 7.901513937033938895, 16.35941288907570623 ) ) ;
#49782=CARTESIAN_POINT ( 'NONE',  ( -8.559508646656381003, 51.83514083332404709, -1.531152949374265049 ) ) ;
#49809=EDGE_CURVE ( 'NONE', #55752, #32781, #92842, .T. ) ;
#49821=MECHANICAL_DESIGN_GEOMETRIC_PRESENTATION_REPRESENTATION('',(#96353),#103200);
#49829=( LENGTH_UNIT ( ) NAMED_UNIT ( * ) SI_UNIT ( .MILLI., .METRE. ) );
#49835=PRESENTATION_STYLE_ASSIGNMENT (( #50358 ) ) ;
#49839=CARTESIAN_POINT ( 'NONE',  ( -1.168166114424086244, 14.76304312983176104, 50.96139025757861418 ) ) ;
#49847=CARTESIAN_POINT ( 'NONE',  ( 1.944839216437187431E-15, 45.30391365246044444, 18.75000000000001066 ) ) ;
#49850=( GEOMETRIC_REPRESENTATION_CONTEXT ( 3 ) GLOBAL_UNCERTAINTY_ASSIGNED_CONTEXT ( ( #67742 ) ) GLOBAL_UNIT_ASSIGNED_CONTEXT ( ( #44110, #67848, #60315 ) ) REPRESENTATION_CONTEXT ( 'NONE', 'WORKASPACE' ) );
#49852=CARTESIAN_POINT ( 'NONE',  ( -10.92801675053744148, 45.30201443972634934, -15.24347305256524088 ) ) ;
#49858=CARTESIAN_POINT ( 'NONE',  ( -36.32210038707830790, 28.19822729005272421, 12.06285977509587859 ) ) ;
#49871=CARTESIAN_POINT ( 'NONE',  ( 30.93386089603002986, 8.839832930400802979, 40.91297150549235084 ) ) ;
#49906=CARTESIAN_POINT ( 'NONE',  ( 38.77611916830803551, 25.24244599302587844, -11.84947842017332320 ) ) ;
#49909=DIRECTION ( 'NONE',  ( -0.000000000000000000, 1.000000000000000000, -0.000000000000000000 ) ) ;
#49923=SURFACE_STYLE_FILL_AREA ( #43444 ) ;
#49982=CARTESIAN_POINT ( 'NONE',  ( 24.23033468520214484, 25.18874691648631270, -32.69349562522533859 ) ) ;
#49987=ADVANCED_FACE ( 'NONE', ( #47466 ), #62104, .F. ) ;
#50008=( GEOMETRIC_REPRESENTATION_CONTEXT ( 3 ) GLOBAL_UNCERTAINTY_ASSIGNED_CONTEXT ( ( #93618 ) ) GLOBAL_UNIT_ASSIGNED_CONTEXT ( ( #68278, #18145, #36487 ) ) REPRESENTATION_CONTEXT ( 'NONE', 'WORKASPACE' ) );
#50034=CARTESIAN_POINT ( 'NONE',  ( 22.00868112945000021, 27.89883671455867287, -32.31191507115346440 ) ) ;
#50038=ADVANCED_FACE ( 'NONE', ( #91541 ), #23229, .F. ) ;
#50058=CARTESIAN_POINT ( 'NONE',  ( -26.78645834884456178, 34.58995912366707159, 10.02611660484962819 ) ) ;
#50070=CARTESIAN_POINT ( 'NONE',  ( -48.02835407290516656, 9.771516447483513446, 16.85535821593516559 ) ) ;
#50086=CARTESIAN_POINT ( 'NONE',  ( -30.92872287337569048, 13.87446774603009558, 40.98770496732624480 ) ) ;
#50089=AXIS2_PLACEMENT_3D ( 'NONE', #61680, #101578, #77302 ) ;
#50101=CARTESIAN_POINT ( 'NONE',  ( -17.84561098364271459, 43.24919059263760346, 5.055340749336767026 ) ) ;
#50104=CARTESIAN_POINT ( 'NONE',  ( -5.454857745093078414, 51.31478691690154648, -8.531152949374575911 ) ) ;
#50117=CARTESIAN_POINT ( 'NONE',  ( 9.812372088291331451, 51.27357729035378497, 2.926662531446465820 ) ) ;
#50141=CARTESIAN_POINT ( 'NONE',  ( -37.56673239365863282, 25.47613764497371847, -13.45617127781024891 ) ) ;
#50148=CARTESIAN_POINT ( 'NONE',  ( 16.64348903516496492, 43.47556584774762456, -6.657797401562562278 ) ) ;
#50159=FILL_AREA_STYLE_COLOUR ( '', #16110 ) ;
#50162=B_SPLINE_CURVE_WITH_KNOTS ( 'NONE', 3,
 ( #67669, #98940, #67135, #90881, #59049, #7812, #33720, #73609, #75202, #66596, #58514, #50394, #9397, #100549, #32668, #42313, #26712, #91933, #83835, #48797, #65539, #36925 ),
 .UNSPECIFIED., .F., .F.,
 ( 4, 2, 2, 2, 2, 2, 2, 2, 2, 2, 4 ),
 ( 0.003168291407922112484, 0.003670795193784145982, 0.004173298979646179047, 0.004675802765508212111, 0.004927054658439226908, 0.005178306551370240839, 0.005680810337232268699, 0.005932062230163284364, 0.006183314123094299161, 0.006685817908956327021, 0.007188321694818354882 ),
 .UNSPECIFIED. ) ;
#50172=( LENGTH_UNIT ( ) NAMED_UNIT ( * ) SI_UNIT ( .MILLI., .METRE. ) );
#50206=FACE_OUTER_BOUND ( 'NONE', #97232, .T. ) ;
#50217=AXIS2_PLACEMENT_3D ( 'NONE', #76295, #2405, #18083 ) ;
#50261=CARTESIAN_POINT ( 'NONE',  ( 17.71951158999540610, 45.45134770963999671, 4.750929343604541444 ) ) ;
#50266=VERTEX_POINT ( 'NONE', #73064 ) ;
#50272=CARTESIAN_POINT ( 'NONE',  ( -22.19982010036164866, 28.18804608458828653, -31.21118039878593464 ) ) ;
#50275=FILL_AREA_STYLE_COLOUR ( '', #46031 ) ;
#50300=CARTESIAN_POINT ( 'NONE',  ( 48.91516379432449924, 8.057663746602608867, 16.48802948946137548 ) ) ;
#50302=CARTESIAN_POINT ( 'NONE',  ( 10.28624191511840458, 45.38549880562042205, 15.40779740156149202 ) ) ;
#50318=CARTESIAN_POINT ( 'NONE',  ( 9.293831213271754876, 43.59774867130855824, -14.93437611856834835 ) ) ;
#50321=ORIENTED_EDGE ( 'NONE', *, *, #98491, .F. ) ;
#50329=CARTESIAN_POINT ( 'NONE',  ( -15.88225526726033365, 44.00162778657170293, 4.402143696494996483 ) ) ;
#50351=CYLINDRICAL_SURFACE ( 'NONE', #77067, 1.250000000000001110 ) ;
#50358=SURFACE_STYLE_USAGE ( .BOTH. , #84344 ) ;
#50362=CARTESIAN_POINT ( 'NONE',  ( -0.3597645216197892792, 13.03473291421858704, 51.69869386382899989 ) ) ;
#50376=CARTESIAN_POINT ( 'NONE',  ( -47.50596275964301185, 17.89684634806518915, -14.46697959672336609 ) ) ;
#50378=ORIENTED_EDGE ( 'NONE', *, *, #76130, .T. ) ;
#50394=CARTESIAN_POINT ( 'NONE',  ( 9.812626099621477138, 51.27376982094347824, -2.923931248734654709 ) ) ;
#50396=CARTESIAN_POINT ( 'NONE',  ( 5.856054662371438901, 51.27348195240095663, 8.398858895281488657 ) ) ;
#50405=EDGE_LOOP ( 'NONE', ( #17405, #98050 ) ) ;
#50409=CARTESIAN_POINT ( 'NONE',  ( -36.49045618873069685, 28.04599723762765606, -12.86279510840584095 ) ) ;
#50424=AXIS2_PLACEMENT_3D ( 'NONE', #76192, #10913, #70769 ) ;
#50428=CARTESIAN_POINT ( 'NONE',  ( 37.56673239365841255, 25.47613764497371136, -13.45617127781092215 ) ) ;
#50436=CYLINDRICAL_SURFACE ( 'NONE', #51238, 1.250000000000001110 ) ;
#50444=FACE_OUTER_BOUND ( 'NONE', #89464, .T. ) ;
#50446=AXIS2_PLACEMENT_3D ( 'NONE', #86556, #12614, #87598 ) ;
#50453=CARTESIAN_POINT ( 'NONE',  ( 15.67156894839903991, 34.65681240932962481, 23.70584078379189563 ) ) ;
#50456=EDGE_CURVE ( 'NONE', #45240, #103131, #40186, .T. ) ;
#50469=UNCERTAINTY_MEASURE_WITH_UNIT (LENGTH_MEASURE( 1.000000000000000082E-05 ), #4783, 'distance_accuracy_value', 'NONE');
#50486=ADVANCED_FACE ( 'NONE', ( #55812 ), #98422, .F. ) ;
#50490=CARTESIAN_POINT ( 'NONE',  ( 8.239113808047395793, 53.79488085724082680, 3.999741343929974935 ) ) ;
#50495=CARTESIAN_POINT ( 'NONE',  ( 8.559508646656407649, 53.68473964988125857, 4.031152949374444461 ) ) ;
#50509=VERTEX_POINT ( 'NONE', #2905 ) ;
#50525=CARTESIAN_POINT ( 'NONE',  ( -27.42597638825734663, 34.37175190012616355, -10.02588870074117366 ) ) ;
#50541=CARTESIAN_POINT ( 'NONE',  ( 16.83415698846517117, 37.10146012410931604, -21.80698433968623817 ) ) ;
#50545=EDGE_CURVE ( 'NONE', #33697, #21252, #96782, .T. ) ;
#50572=ORIENTED_EDGE ( 'NONE', *, *, #95294, .T. ) ;
#50581=DIRECTION ( 'NONE',  ( -0.000000000000000000, 1.000000000000000000, -0.000000000000000000 ) ) ;
#50582=CARTESIAN_POINT ( 'NONE',  ( -46.81343110146983122, 13.24251555485282239, 15.91224400466310307 ) ) ;
#50590=CARTESIAN_POINT ( 'NONE',  ( 15.39661048887591299, 46.16593794825683261, 5.596966726905939105 ) ) ;
#50599=CARTESIAN_POINT ( 'NONE',  ( -30.06732394248810536, 17.62925877149443821, 39.66393268825138563 ) ) ;
#50613=CARTESIAN_POINT ( 'NONE',  ( -6.510243396850508901, 51.36750486090217294, -7.564727007839853634 ) ) ;
#50619=CARTESIAN_POINT ( 'NONE',  ( -29.08094203968506974, 13.68582110885884440, 39.75724343093563107 ) ) ;
#50626=CARTESIAN_POINT ( 'NONE',  ( 37.40728451038606295, 27.65912829610039125, -13.45617127781095590 ) ) ;
#50629=ORIENTED_EDGE ( 'NONE', *, *, #100634, .T. ) ;
#50652=CARTESIAN_POINT ( 'NONE',  ( 15.56598648174122346, 43.92012149713269054, -6.062017361296271112 ) ) ;
#50655=CARTESIAN_POINT ( 'NONE',  ( -37.72538228492555135, 27.83011398562653227, 10.95617127781058464 ) ) ;
#50691=CARTESIAN_POINT ( 'NONE',  ( -4.884983410653892300, 51.44234778147703935, 8.466500073338718124 ) ) ;
#50696=CARTESIAN_POINT ( 'NONE',  ( 30.00229752355648571, 12.60065794652348359, -39.63915577993689965 ) ) ;
#50710=FILL_AREA_STYLE_COLOUR ( '', #47119 ) ;
#50722=CARTESIAN_POINT ( 'NONE',  ( -0.4142949201392615577, 54.27908600331601718, 7.817690266341844385 ) ) ;
#50744=CARTESIAN_POINT ( 'NONE',  ( -0.6458512730941106117, 36.35850673702802283, -29.58327430845546147 ) ) ;
#50767=DIRECTION ( 'NONE',  ( -0.000000000000000000, 1.000000000000000000, -0.000000000000000000 ) ) ;
#50780=CARTESIAN_POINT ( 'NONE',  ( 25.89579718936635544, 37.13050443889593311, -9.162997211423999033 ) ) ;
#50797=FILL_AREA_STYLE_COLOUR ( '', #103976 ) ;
#50801=DIRECTION ( 'NONE',  ( 0.000000000000000000, 0.000000000000000000, 1.000000000000000000 ) ) ;
#50809=ORIENTED_EDGE ( 'NONE', *, *, #82271, .T. ) ;
#50833=B_SPLINE_CURVE_WITH_KNOTS ( 'NONE', 3,
 ( #39956, #6502, #15137, #96605, #88512, #90091, #89035, #49082, #48019, #65284, #105733, #15662, #31876, #48555, #71248, #97634, #96071, #73355, #106254, #32415 ),
 .UNSPECIFIED., .F., .F.,
 ( 4, 2, 2, 2, 2, 2, 2, 2, 2, 4 ),
 ( 0.007218903764951243446, 0.007723284340237460133, 0.008227664915523676820, 0.008732045490809895241, 0.009236426066096111928, 0.009488616353739223741, 0.009740806641382337289, 0.01024518721666855745, 0.01074956779195477760, 0.01125394836724099949 ),
 .UNSPECIFIED. ) ;
#50834=CARTESIAN_POINT ( 'NONE',  ( -1.231305719443886781, 11.27890317915398022, -50.25262848319923847 ) ) ;
#50841=B_SPLINE_CURVE_WITH_KNOTS ( 'NONE', 3,
 ( #77727, #69636, #10313, #61557, #3839, #35705, #94453, #59426, #20610, #53449, #93382, #12435, #18994, #44293, #45363, #92290, #35162, #84220, #43231, #2212, #68028, #100921 ),
 .UNSPECIFIED., .F., .F.,
 ( 4, 2, 2, 2, 2, 2, 2, 2, 2, 2, 4 ),
 ( 0.007250106599135532071, 0.007754025997590315369, 0.008257945396045098668, 0.008761864794499881967, 0.009265784192954665266, 0.009769703591409448565, 0.01002166329063684802, 0.01027362298986424748, 0.01052558268909164693, 0.01077754238831904639, 0.01128146178677384009 ),
 .UNSPECIFIED. ) ;
#50848=( GEOMETRIC_REPRESENTATION_CONTEXT ( 3 ) GLOBAL_UNCERTAINTY_ASSIGNED_CONTEXT ( ( #102229 ) ) GLOBAL_UNIT_ASSIGNED_CONTEXT ( ( #7662, #91801, #32521 ) ) REPRESENTATION_CONTEXT ( 'NONE', 'WORKASPACE' ) );
#50857=CARTESIAN_POINT ( 'NONE',  ( -23.21751746555244722, 28.11705169068991594, 30.70617127781060418 ) ) ;
#50863=EDGE_LOOP ( 'NONE', ( #17982, #69568 ) ) ;
#50871=AXIS2_PLACEMENT_3D ( 'NONE', #99266, #57217, #48068 ) ;
#50882=SURFACE_SIDE_STYLE ('',( #18016 ) ) ;
#50889=CARTESIAN_POINT ( 'NONE',  ( -4.080371711542015056, 51.84956781351371546, -7.633648114451180966 ) ) ;
#50893=ORIENTED_EDGE ( 'NONE', *, *, #34477, .T. ) ;
#50901=EDGE_LOOP ( 'NONE', ( #81400, #12619, #35022, #36888, #2387, #4227, #91616, #42432 ) ) ;
#50903=CARTESIAN_POINT ( 'NONE',  ( -9.032223969890592841, 46.05502784614109402, 14.03066199895137345 ) ) ;
#50914=CARTESIAN_POINT ( 'NONE',  ( -15.49777008014214275, 34.92648659974615555, -22.93096364591211866 ) ) ;
#50926=CARTESIAN_POINT ( 'NONE',  ( 6.308322377852634055, 51.28511537930989306, 8.025364867616824327 ) ) ;
#50937=VECTOR ( 'NONE', #43493, 1000.000000000000000 ) ;
#50939=CARTESIAN_POINT ( 'NONE',  ( 5.619944455633341995, 51.29440671850761646, -8.489742679686163029 ) ) ;
#50960=CARTESIAN_POINT ( 'NONE',  ( 37.88407777523421061, 25.64317711490430085, -10.98674666298723324 ) ) ;
#50972=DIRECTION ( 'NONE',  ( 1.150791560227848297E-16, -0.3420201433256725987, 0.9396926207859068736 ) ) ;
#50980=ORIENTED_EDGE ( 'NONE', *, *, #3822, .T. ) ;
#50982=CARTESIAN_POINT ( 'NONE',  ( 0.6419155526175454041, 28.14113459593094291, 38.42427017686829060 ) ) ;
#50983=CARTESIAN_POINT ( 'NONE',  ( -30.00061906993008876, 12.59382690271829652, -39.64398720750899230 ) ) ;
#50999=( GEOMETRIC_REPRESENTATION_CONTEXT ( 3 ) GLOBAL_UNCERTAINTY_ASSIGNED_CONTEXT ( ( #81764 ) ) GLOBAL_UNIT_ASSIGNED_CONTEXT ( ( #56235, #5068, #32013 ) ) REPRESENTATION_CONTEXT ( 'NONE', 'WORKASPACE' ) );
#51001=ORIENTED_EDGE ( 'NONE', *, *, #100888, .F. ) ;
#51005=STYLED_ITEM ( 'NONE', ( #18778 ), #64164 ) ;
#51020=UNCERTAINTY_MEASURE_WITH_UNIT (LENGTH_MEASURE( 1.000000000000000082E-05 ), #22106, 'distance_accuracy_value', 'NONE');
#51026=CARTESIAN_POINT ( 'NONE',  ( 7.945173694731215264, 53.90995037661843270, 3.881245261317305406 ) ) ;
#51031=CARTESIAN_POINT ( 'NONE',  ( -15.50560966020059617, 37.05331456527880363, -22.93063681418762911 ) ) ;
#51034=CARTESIAN_POINT ( 'NONE',  ( 47.90468627969811166, 11.89467801380305545, 14.35535821593427919 ) ) ;
#51043=CARTESIAN_POINT ( 'NONE',  ( -47.18533784750982107, 13.30762177597462781, -14.68117529621423145 ) ) ;
#51044=CARTESIAN_POINT ( 'NONE',  ( -36.35681509222002461, 25.99976016919919886, -12.56101700226311024 ) ) ;
#51045=DIRECTION ( 'NONE',  ( -0.000000000000000000, 1.000000000000000000, -0.000000000000000000 ) ) ;
#51077=ORIENTED_EDGE ( 'NONE', *, *, #63608, .T. ) ;
#51080=CARTESIAN_POINT ( 'NONE',  ( 15.97317602965549277, 35.08246898966388727, -22.07552446507282795 ) ) ;
#51081=FACE_OUTER_BOUND ( 'NONE', #46286, .T. ) ;
#51083=ADVANCED_FACE ( 'NONE', ( #106242, #40998, #8622, #58237, #64747 ), #45082, .F. ) ;
#51085=COLOUR_RGB ( '', 0.09019608, 0.27058824, 0.51372549) ;
#51087=CARTESIAN_POINT ( 'NONE',  ( 23.05268216894187105, 28.15323590773658324, -30.70617127781077471 ) ) ;
#51095=CARTESIAN_POINT ( 'NONE',  ( -22.59034450229749424, 25.42945400995673921, 33.04942977596110154 ) ) ;
#51110=( NAMED_UNIT ( * ) SI_UNIT ( $, .STERADIAN. ) SOLID_ANGLE_UNIT ( ) );
#51120=CARTESIAN_POINT ( 'NONE',  ( -8.398759976699373908, 53.73767103463583084, -4.031152949374835259 ) ) ;
#51127=ORIENTED_EDGE ( 'NONE', *, *, #19932, .T. ) ;
#51133=CARTESIAN_POINT ( 'NONE',  ( 8.875371311763096571, 53.84840360445480911, 1.561291615688902956 ) ) ;
#51154=CARTESIAN_POINT ( 'NONE',  ( 48.80488232270386106, 14.82891652079634426, 14.61828285348437007 ) ) ;
#51167=EDGE_LOOP ( 'NONE', ( #61541, #26989 ) ) ;
#51180=CARTESIAN_POINT ( 'NONE',  ( -23.84258101729975365, 25.80558521616085699, -30.86173856011716055 ) ) ;
#51236=CARTESIAN_POINT ( 'NONE',  ( 2.845670519300376476E-15, 38.67090180175566871, 23.23666318551310539 ) ) ;
#51238=AXIS2_PLACEMENT_3D ( 'NONE', #100064, #33764, #34840 ) ;
#51245=PRESENTATION_STYLE_ASSIGNMENT (( #10784 ) ) ;
#51263=CARTESIAN_POINT ( 'NONE',  ( -0.3343798466136014835, 53.41130560517088810, 10.20736967772077186 ) ) ;
#51282=CARTESIAN_POINT ( 'NONE',  ( 36.95318979654836511, 25.70470319923920854, -13.30662917248846178 ) ) ;
#51285=CARTESIAN_POINT ( 'NONE',  ( -0.4138703915521824706, 37.18449757264020406, -27.31749840197732127 ) ) ;
#51291=CARTESIAN_POINT ( 'NONE',  ( -15.51806636169574993, 46.21009754484515497, -4.857304170327880755 ) ) ;
#51293=UNCERTAINTY_MEASURE_WITH_UNIT (LENGTH_MEASURE( 1.000000000000000082E-05 ), #29240, 'distance_accuracy_value', 'NONE');
#51315=ORIENTED_EDGE ( 'NONE', *, *, #100472, .T. ) ;
#51322=PRESENTATION_STYLE_ASSIGNMENT (( #43778 ) ) ;
#51340=DIRECTION ( 'NONE',  ( 0.000000000000000000, 1.000000000000000000, -0.000000000000000000 ) ) ;
#51343=( LENGTH_UNIT ( ) NAMED_UNIT ( * ) SI_UNIT ( .MILLI., .METRE. ) );
#51360=CARTESIAN_POINT ( 'NONE',  ( 7.306639711237237655, 52.17338899348808212, 2.636058739605869228 ) ) ;
#51365=CARTESIAN_POINT ( 'NONE',  ( -4.237512335919120849E-14, 43.17555810750860701, 18.75000000000000355 ) ) ;
#51377=CARTESIAN_POINT ( 'NONE',  ( 10.12027680424187714, 44.03028463990052899, -12.90779740156171940 ) ) ;
#51388=B_SPLINE_CURVE_WITH_KNOTS ( 'NONE', 3,
 ( #42012, #50104, #90034, #33417, #26414, #99722, #17757, #73847, #92155, #24795, #50613, #35025, #16680, #8045, #83009, #16140, #75444, #49571, #81925, #58197, #1537, #18300 ),
 .UNSPECIFIED., .F., .F.,
 ( 4, 2, 2, 2, 2, 2, 2, 2, 2, 2, 4 ),
 ( 0.006827920940005929341, 0.007331585277004999505, 0.007583417445504535455, 0.007835249614004072272, 0.008338913951003144170, 0.008590746119502681855, 0.008842578288002221273, 0.009849906962000365071, 0.01035357129899943870, 0.01060540346749897986, 0.01085723563599851928 ),
 .UNSPECIFIED. ) ;
#51395=CARTESIAN_POINT ( 'NONE',  ( 28.18083109848378598, 36.45116722329852621, -8.149727080479747698 ) ) ;
#51402=ADVANCED_FACE ( 'NONE', ( #19318 ), #26862, .T. ) ;
#51417=CARTESIAN_POINT ( 'NONE',  ( 46.90314054034891456, 18.02221697236495501, -16.15497048139741665 ) ) ;
#51421=CARTESIAN_POINT ( 'NONE',  ( -49.15269216906030181, 13.73471152902511072, 15.05374764291914857 ) ) ;
#51423=( NAMED_UNIT ( * ) PLANE_ANGLE_UNIT ( ) SI_UNIT ( $, .RADIAN. ) );
#51445=VECTOR ( 'NONE', #71485, 1000.000000000000000 ) ;
#51448=CYLINDRICAL_SURFACE ( 'NONE', #104949, 1.250000000000001110 ) ;
#51469=CARTESIAN_POINT ( 'NONE',  ( 49.24306615471292758, 8.188742177551262102, -15.29695692017807396 ) ) ;
#51484=CARTESIAN_POINT ( 'NONE',  ( 5.701517186572424123, 51.28557980447222064, -8.464474017692539931 ) ) ;
#51489=CARTESIAN_POINT ( 'NONE',  ( -36.45744830273498138, 25.93793769161023022, 12.78814307577592402 ) ) ;
#51512=FILL_AREA_STYLE ('',( #18652 ) ) ;
#51517=CARTESIAN_POINT ( 'NONE',  ( 30.77392345931262341, 15.52887250063909441, 40.23353194602682237 ) ) ;
#51564=ORIENTED_EDGE ( 'NONE', *, *, #27936, .T. ) ;
#51565=LINE ( 'NONE', #75306, #26834 ) ;
#51573=CARTESIAN_POINT ( 'NONE',  ( -16.12754063828937490, 36.56084451123471979, -24.14283378817831860 ) ) ;
#51580=ORIENTED_EDGE ( 'NONE', *, *, #73188, .F. ) ;
#51584=CARTESIAN_POINT ( 'NONE',  ( -46.86466781827400041, 13.70365495135298772, -15.14281811549651913 ) ) ;
#51586=LINE ( 'NONE', #85032, #99940 ) ;
#51587=DIRECTION ( 'NONE',  ( 0.000000000000000000, 0.000000000000000000, 1.000000000000000000 ) ) ;
#51601=CARTESIAN_POINT ( 'NONE',  ( 29.35771261243655061, 8.827287181787172088, -42.06472072717370736 ) ) ;
#51602=CARTESIAN_POINT ( 'NONE',  ( 17.62428443205140383, 45.49731502040738462, -4.616218165346110958 ) ) ;
#51618=CARTESIAN_POINT ( 'NONE',  ( 17.08200492518409774, 36.32755554593313008, -24.26548702208093999 ) ) ;
#51627=ADVANCED_FACE ( 'NONE', ( #34146 ), #25534, .F. ) ;
#51665=ORIENTED_EDGE ( 'NONE', *, *, #66250, .F. ) ;
#51670=CARTESIAN_POINT ( 'NONE',  ( 15.42241126771897086, 46.21736870922993035, 5.091656527549089262 ) ) ;
#51702=ORIENTED_EDGE ( 'NONE', *, *, #1562, .T. ) ;
#51706=CARTESIAN_POINT ( 'NONE',  ( 0.000000000000000000, 38.67090180175566871, -23.23666318551310539 ) ) ;
#51709=B_SPLINE_CURVE_WITH_KNOTS ( 'NONE', 3,
 ( #33453, #26971, #59855, #66328, #25375, #92725, #18885, #58231, #81961, #66869, #8087, #74934, #40992, #73881, #106776, #32927, #98678, #11797, #78652, #61447 ),
 .UNSPECIFIED., .F., .F.,
 ( 4, 2, 2, 2, 2, 2, 2, 2, 2, 4 ),
 ( 0.003076783614208158761, 0.003581015465326142094, 0.004085247316444126295, 0.004589479167562109628, 0.005093711018680092961, 0.005597942869798077162, 0.005850058795357066660, 0.006102174720916056158, 0.006606406572034035155, 0.007110638423152015018 ),
 .UNSPECIFIED. ) ;
#51725=CARTESIAN_POINT ( 'NONE',  ( 0.3345949520953953593, 37.19393312596059786, 27.29267445124407843 ) ) ;
#51762=EDGE_CURVE ( 'NONE', #101, #66410, #55991, .T. ) ;
#51771=ORIENTED_EDGE ( 'NONE', *, *, #46495, .T. ) ;
#51796=CARTESIAN_POINT ( 'NONE',  ( 7.715274834628325378E-15, 0.000000000000000000, -63.00000000000000000 ) ) ;
#51798=VECTOR ( 'NONE', #63003, 1000.000000000000000 ) ;
#51819=CARTESIAN_POINT ( 'NONE',  ( 37.40542853975937732, 25.53140870284743613, -13.45617127781092215 ) ) ;
#51828=CARTESIAN_POINT ( 'NONE',  ( -16.02154979717254335, 46.08966533359959072, -4.311187973113333349 ) ) ;
#51839=EDGE_CURVE ( 'NONE', #88140, #60788, #80284, .T. ) ;
#51842=DIRECTION ( 'NONE',  ( 0.000000000000000000, 1.000000000000000000, 0.000000000000000000 ) ) ;
#51844=B_SPLINE_CURVE_WITH_KNOTS ( 'NONE', 3,
 ( #28990, #102288, #85050, #51601, #76403, #94753, #52132, #86135, #84522, #20374, #28434, #77491, #11668, #45137, #35465, #2516, #69930, #36008, #92596, #60268, #12208, #60789, #103360, #11129, #44601, #94205, #10608, #93677, #19830, #43530 ),
 .UNSPECIFIED., .F., .F.,
 ( 4, 2, 2, 2, 2, 2, 2, 2, 2, 2, 2, 2, 2, 2, 4 ),
 ( 0.0004001071830457286088, 0.0008634720163662153516, 0.001326836849686701932, 0.002253566516327680080, 0.003180296182968658011, 0.004107025849609637243, 0.005033755516250615174, 0.005497120349571107609, 0.005960485182891598309, 0.006423850016212089876, 0.006655532432872336528, 0.006887214849532581444, 0.007118897266192828095, 0.007350579682853073012, 0.007813944516173556773 ),
 .UNSPECIFIED. ) ;
#51847=CARTESIAN_POINT ( 'NONE',  ( -48.02835407290533709, 9.771516447483559631, -16.85535821593460426 ) ) ;
#51867=ORIENTED_EDGE ( 'NONE', *, *, #72982, .T. ) ;
#51874=CARTESIAN_POINT ( 'NONE',  ( 38.64245533733815563, 27.44901796531306459, -11.54891632625754028 ) ) ;
#51877=CARTESIAN_POINT ( 'NONE',  ( 0.9891189538826573591, 17.70032527776562858, 49.73254565116481984 ) ) ;
#51888=DIRECTION ( 'NONE',  ( 0.000000000000000000, 1.000000000000000000, 0.000000000000000000 ) ) ;
#51889=CARTESIAN_POINT ( 'NONE',  ( 5.290067270632158980, 51.34639538792298197, -8.531152949374604333 ) ) ;
#51896=LINE ( 'NONE', #86430, #26817 ) ;
#51909=CARTESIAN_POINT ( 'NONE',  ( -0.9991018963761647553, 8.903979680119203266, -51.25442813699677913 ) ) ;
#51912=CARTESIAN_POINT ( 'NONE',  ( 9.048917774133558467, 43.82457158262040053, -14.35241448611411919 ) ) ;
#51923=CARTESIAN_POINT ( 'NONE',  ( -16.48255526477243293, 43.52995101198734318, 6.657797401561652784 ) ) ;
#51937=EDGE_LOOP ( 'NONE', ( #95735, #67112 ) ) ;
#51938=CARTESIAN_POINT ( 'NONE',  ( 8.559508646656349029, 51.83514083332403999, -1.531152949374623873 ) ) ;
#51941=ORIENTED_EDGE ( 'NONE', *, *, #90598, .F. ) ;
#51962=ADVANCED_FACE ( 'NONE', ( #82958 ), #24222, .F. ) ;
#51965=CARTESIAN_POINT ( 'NONE',  ( -25.85238267732653128, 35.07671371647713698, -8.660559307860188127 ) ) ;
#51973=FILL_AREA_STYLE_COLOUR ( '', #84294 ) ;
#51975=( LENGTH_UNIT ( ) NAMED_UNIT ( * ) SI_UNIT ( .MILLI., .METRE. ) );
#51979=LINE ( 'NONE', #43899, #52987 ) ;
#51986=CARTESIAN_POINT ( 'NONE',  ( -15.97423913551834040, 35.08248256844603219, -22.07470797814806929 ) ) ;
#51994=ORIENTED_EDGE ( 'NONE', *, *, #76989, .T. ) ;
#52000=CARTESIAN_POINT ( 'NONE',  ( 6.542048114965975714, 51.42613907887827196, 7.322510233794829126 ) ) ;
#52015=CARTESIAN_POINT ( 'NONE',  ( 6.392325331821059109, 51.30797053396300100, -7.876575602207272375 ) ) ;
#52031=LINE ( 'NONE', #26219, #99710 ) ;
#52056=CARTESIAN_POINT ( 'NONE',  ( 0.08491295131515702588, 27.29656849860388235, 40.75000000000002132 ) ) ;
#52057=CARTESIAN_POINT ( 'NONE',  ( -30.90161637171721765, 8.443258198712127793, -41.14563328228313566 ) ) ;
#52063=CARTESIAN_POINT ( 'NONE',  ( 8.559508646656350805, 53.96349637827587031, -1.531152949374623651 ) ) ;
#52074=CARTESIAN_POINT ( 'NONE',  ( 5.290067270632161645, 53.47475093287481229, -8.531152949374595451 ) ) ;
#52080=STYLED_ITEM ( 'NONE', ( #71908 ), #95383 ) ;
#52102=EDGE_CURVE ( 'NONE', #34913, #54018, #65584, .T. ) ;
#52116=FACE_OUTER_BOUND ( 'NONE', #65350, .T. ) ;
#52119=CARTESIAN_POINT ( 'NONE',  ( -16.64348903516526335, 43.75610143575153899, -4.157797401561264650 ) ) ;
#52132=CARTESIAN_POINT ( 'NONE',  ( 28.98676785243906906, 9.652684557211529182, -41.90074509620651355 ) ) ;
#52151=CARTESIAN_POINT ( 'NONE',  ( 17.97174518249911657, 36.40624878439879808, -23.34175835912210317 ) ) ;
#52175=CARTESIAN_POINT ( 'NONE',  ( 27.10511071441198894, 36.88665068479745912, 7.556984339683237906 ) ) ;
#52176=CARTESIAN_POINT ( 'NONE',  ( 48.02835407290504577, -1.200000000000000030E-05, -15.60535821593549954 ) ) ;
#52178=SURFACE_SIDE_STYLE ('',( #77532 ) ) ;
#52179=CARTESIAN_POINT ( 'NONE',  ( 1.093414209075683985, 36.52532583549212575, -29.11109415026225378 ) ) ;
#52180=ORIENTED_EDGE ( 'NONE', *, *, #59396, .T. ) ;
#52198=ORIENTED_EDGE ( 'NONE', *, *, #49809, .F. ) ;
#52200=EDGE_CURVE ( 'NONE', #49037, #46369, #7723, .T. ) ;
#52215=ORIENTED_EDGE ( 'NONE', *, *, #52412, .F. ) ;
#52222=ORIENTED_EDGE ( 'NONE', *, *, #47085, .T. ) ;
#52233=CARTESIAN_POINT ( 'NONE',  ( -0.6447519515824183811, 37.14707136400079435, 27.41619501522666269 ) ) ;
#52249=CARTESIAN_POINT ( 'NONE',  ( -0.7867783998819701807, 45.39444483141824094, -18.48491233039627701 ) ) ;
#52268=EDGE_LOOP ( 'NONE', ( #52492, #77889, #40522, #88344 ) ) ;
#52272=ORIENTED_EDGE ( 'NONE', *, *, #10240, .T. ) ;
#52295=VERTEX_POINT ( 'NONE', #94112 ) ;
#52313=CARTESIAN_POINT ( 'NONE',  ( 30.63612296757489517, 10.92940684821786590, -40.03790167141658429 ) ) ;
#52324=CARTESIAN_POINT ( 'NONE',  ( 10.28624191511809371, -1.200000000000000030E-05, -15.40779740156171762 ) ) ;
#52327=SURFACE_SIDE_STYLE ('',( #19490 ) ) ;
#52334=CARTESIAN_POINT ( 'NONE',  ( 2.761899744546835519E-15, 36.79151656018385097, -22.55262289886175964 ) ) ;
#52341=ORIENTED_EDGE ( 'NONE', *, *, #30862, .F. ) ;
#52342=CARTESIAN_POINT ( 'NONE',  ( 0.000000000000000000, 23.58303312036771615, -45.10524579772351217 ) ) ;
#52359=EDGE_CURVE ( 'NONE', #100497, #24510, #93588, .T. ) ;
#52387=STYLED_ITEM ( 'NONE', ( #95521 ), #16251 ) ;
#52403=CARTESIAN_POINT ( 'NONE',  ( -47.77442396816168468, 17.34920168383065686, 14.37330342454805177 ) ) ;
#52404=DIRECTION ( 'NONE',  ( 0.000000000000000000, 0.000000000000000000, 1.000000000000000000 ) ) ;
#52406=CARTESIAN_POINT ( 'NONE',  ( 0.5305815910617995845, 18.60106106186565356, 49.36172356568721398 ) ) ;
#52412=EDGE_CURVE ( 'NONE', #95973, #20227, #84926, .T. ) ;
#52417=AXIS2_PLACEMENT_3D ( 'NONE', #67670, #100550, #26713 ) ;
#52431=CARTESIAN_POINT ( 'NONE',  ( -7.312621643696487261, 52.12777849912266248, -2.970404147433324482 ) ) ;
#52434=ADVANCED_FACE ( 'NONE', ( #43309 ), #92375, .F. ) ;
#52435=CARTESIAN_POINT ( 'NONE',  ( -0.7804241024683111760, 8.373447173740549587, -51.48088908221409099 ) ) ;
#52437=PRESENTATION_STYLE_ASSIGNMENT (( #9315 ) ) ;
#52445=CARTESIAN_POINT ( 'NONE',  ( -4.272532768864641284, 54.28699348431178606, -6.535710695638695888 ) ) ;
#52455=LINE ( 'NONE', #27709, #37452 ) ;
#52471=CARTESIAN_POINT ( 'NONE',  ( -0.1682124922453071825, 27.29656849860387879, -40.75000000000001421 ) ) ;
#52477=CARTESIAN_POINT ( 'NONE',  ( 46.77788840983939878, 18.69141115048694957, -15.65052543522692652 ) ) ;
#52479=CARTESIAN_POINT ( 'NONE',  ( -10.61825212277778796, 43.91732780493584443, 12.90779740156163768 ) ) ;
#52481=CARTESIAN_POINT ( 'NONE',  ( -49.13304414347859250, 12.95525746345744622, 16.19504546972465064 ) ) ;
#52490=CARTESIAN_POINT ( 'NONE',  ( 5.290067270632160756, 52.08006895350504806, -6.031152949374595451 ) ) ;
#52492=ORIENTED_EDGE ( 'NONE', *, *, #33895, .F. ) ;
#52494=CARTESIAN_POINT ( 'NONE',  ( -23.05170650452966186, 25.28969635687047202, -33.19779254177406358 ) ) ;
#52496=CARTESIAN_POINT ( 'NONE',  ( -26.55974056404284767, 34.93710072687599677, -7.679312300194466978 ) ) ;
#52508=SURFACE_STYLE_USAGE ( .BOTH. , #2361 ) ;
#52510=ADVANCED_FACE ( 'NONE', ( #4980 ), #72870, .F. ) ;
#52514=CARTESIAN_POINT ( 'NONE',  ( -46.77759138928167459, 18.69812886098191385, -15.64253076101933537 ) ) ;
#52529=SURFACE_STYLE_FILL_AREA ( #61179 ) ;
#52530=CARTESIAN_POINT ( 'NONE',  ( 6.528903126310523497, 51.53956178974399904, 6.914479967639524993 ) ) ;
#52544=CARTESIAN_POINT ( 'NONE',  ( -37.40764580657506855, 27.65900449730653321, -13.45617127781033595 ) ) ;
#52548=CARTESIAN_POINT ( 'NONE',  ( -37.40563201180869868, 25.53133898278100133, 13.45617127781066102 ) ) ;
#52555=ORIENTED_EDGE ( 'NONE', *, *, #74999, .F. ) ;
#52563=ORIENTED_EDGE ( 'NONE', *, *, #106328, .F. ) ;
#52564=CARTESIAN_POINT ( 'NONE',  ( -26.94608050197553695, 36.94240651728468805, -7.556984339685585361 ) ) ;
#52573=( GEOMETRIC_REPRESENTATION_CONTEXT ( 3 ) GLOBAL_UNCERTAINTY_ASSIGNED_CONTEXT ( ( #85006 ) ) GLOBAL_UNIT_ASSIGNED_CONTEXT ( ( #82207, #55790, #40165 ) ) REPRESENTATION_CONTEXT ( 'NONE', 'WORKASPACE' ) );
#52576=ORIENTED_EDGE ( 'NONE', *, *, #102166, .F. ) ;
#52577=CARTESIAN_POINT ( 'NONE',  ( 30.82851008854570196, 15.24887380073564280, 40.33969805263195241 ) ) ;
#52595=ORIENTED_EDGE ( 'NONE', *, *, #50456, .T. ) ;
#52614=CARTESIAN_POINT ( 'NONE',  ( -23.21751746555280249, 27.38103382803677022, -33.20617127781034839 ) ) ;
#52620=ADVANCED_FACE ( 'NONE', ( #35658 ), #84702, .F. ) ;
#52645=DIRECTION ( 'NONE',  ( 0.000000000000000000, 0.000000000000000000, -1.000000000000000000 ) ) ;
#52680=CARTESIAN_POINT ( 'NONE',  ( 17.99637020931140441, 36.53998198029805877, -22.85704674614672172 ) ) ;
#52683=LINE ( 'NONE', #34949, #106695 ) ;
#52705=ORIENTED_EDGE ( 'NONE', *, *, #1475, .T. ) ;
#52707=( LENGTH_UNIT ( ) NAMED_UNIT ( * ) SI_UNIT ( .MILLI., .METRE. ) );
#52710=CARTESIAN_POINT ( 'NONE',  ( -0.6415267897369668626, 27.35808064800162853, 40.57598378311829634 ) ) ;
#52712=MECHANICAL_DESIGN_GEOMETRIC_PRESENTATION_REPRESENTATION('',(#69971),#81958);
#52732=ORIENTED_EDGE ( 'NONE', *, *, #101530, .T. ) ;
#52734=ORIENTED_EDGE ( 'NONE', *, *, #22258, .T. ) ;
#52758=CARTESIAN_POINT ( 'NONE',  ( 0.000000000000000000, 36.79151656018385097, 0.000000000000000000 ) ) ;
#52768=FACE_OUTER_BOUND ( 'NONE', #32374, .T. ) ;
#52792=CARTESIAN_POINT ( 'NONE',  ( -16.64348903516526335, 43.75610143575153899, -4.157797401561264650 ) ) ;
#52814=CARTESIAN_POINT ( 'NONE',  ( -16.32302039041868724, 45.99487210642904955, 4.188696036803978728 ) ) ;
#52855=CARTESIAN_POINT ( 'NONE',  ( -27.10511071441183262, -1.200000000000000030E-05, 10.05698433968616001 ) ) ;
#52859=VECTOR ( 'NONE', #31505, 1000.000000000000114 ) ;
#52862=ORIENTED_EDGE ( 'NONE', *, *, #52359, .F. ) ;
#52876=CARTESIAN_POINT ( 'NONE',  ( 24.47192364801414755, 27.44308780173428985, 32.07880713850987320 ) ) ;
#52879=CARTESIAN_POINT ( 'NONE',  ( -17.53793833829797322, 36.29671191971048927, -24.04345926538308831 ) ) ;
#52886=FACE_OUTER_BOUND ( 'NONE', #25222, .T. ) ;
#52892=CARTESIAN_POINT ( 'NONE',  ( -5.855392133367304908, 51.27352836932585944, 8.399161085123857617 ) ) ;
#52923=CIRCLE ( 'NONE', #6393, 22.55262289886175964 ) ;
#52941=VERTEX_POINT ( 'NONE', #60203 ) ;
#52950=CARTESIAN_POINT ( 'NONE',  ( -29.27049653814488295, 13.57913911089069003, -39.67351191892544193 ) ) ;
#52961=LINE ( 'NONE', #13012, #84313 ) ;
#52985=CARTESIAN_POINT ( 'NONE',  ( -27.10511071441183617, 34.75829513984614039, 7.556984339678626483 ) ) ;
#52987=VECTOR ( 'NONE', #59569, 1000.000000000000000 ) ;
#53000=CARTESIAN_POINT ( 'NONE',  ( -9.960122430517547087, 45.46309208840077076, -15.36726729605914166 ) ) ;
#53015=ORIENTED_EDGE ( 'NONE', *, *, #73268, .T. ) ;
#53018=AXIS2_PLACEMENT_3D ( 'NONE', #14350, #39721, #72073 ) ;
#53027=FACE_BOUND ( 'NONE', #75591, .T. ) ;
#53029=CARTESIAN_POINT ( 'NONE',  ( -48.15153125426052583, 16.50033784694647920, 14.35535821593516204 ) ) ;
#53032=CARTESIAN_POINT ( 'NONE',  ( 37.56673239365870387, -1.200000000000000030E-05, 12.20617127780998956 ) ) ;
#53042=CARTESIAN_POINT ( 'NONE',  ( 5.290067270632158980, 51.34639538792298197, -8.531152949374604333 ) ) ;
#53047=CARTESIAN_POINT ( 'NONE',  ( -21.96336593612924659, 25.92439649894939890, -31.83037853264628225 ) ) ;
#53048=CARTESIAN_POINT ( 'NONE',  ( -27.10511071441193565, 34.75829513984539432, -7.556984339685824281 ) ) ;
#53050=COLOUR_RGB ( '', 0.72549020, 0.75294118, 0.79215686) ;
#53068=FACE_OUTER_BOUND ( 'NONE', #84709, .T. ) ;
#53072=CARTESIAN_POINT ( 'NONE',  ( -17.39904316874586598, 34.80796549191882150, 21.94102072422699123 ) ) ;
#53077=EDGE_CURVE ( 'NONE', #34913, #100497, #7532, .T. ) ;
#53078=CARTESIAN_POINT ( 'NONE',  ( 48.55208739724518807, 8.680497950467705337, -16.74317141725391878 ) ) ;
#53094=CARTESIAN_POINT ( 'NONE',  ( 49.27914886956165930, 13.08292563505449024, -15.56788460764872717 ) ) ;
#53128=ORIENTED_EDGE ( 'NONE', *, *, #35573, .T. ) ;
#53133=CARTESIAN_POINT ( 'NONE',  ( -8.239589396826303869, 54.07616056299237073, 1.561881609672474136 ) ) ;
#53143=B_SPLINE_CURVE_WITH_KNOTS ( 'NONE', 3,
 ( #79814, #72257, #8041, #72771, #25330, #976, #105677, #48494, #83006, #58746, #42009, #49024, #64700, #74366, #99720, #49568, #32357, #91641, #98121, #17229, #89511, #31815 ),
 .UNSPECIFIED., .F., .F.,
 ( 4, 2, 2, 2, 2, 2, 2, 2, 2, 2, 4 ),
 ( 0.007084402336705432693, 0.007336525902261045382, 0.007588649467816658070, 0.008092896598927895591, 0.008345020164483511749, 0.008597143730039126172, 0.009101390861150355019, 0.009605637992261582131, 0.01010988512337281098, 0.01061413225448403982, 0.01111837938559526694 ),
 .UNSPECIFIED. ) ;
#53159=CARTESIAN_POINT ( 'NONE',  ( 4.063874237994596683, 54.18639730106497865, -6.988267930799597849 ) ) ;
#53162=ORIENTED_EDGE ( 'NONE', *, *, #93261, .T. ) ;
#53166=CARTESIAN_POINT ( 'NONE',  ( 26.78649824955473235, 36.71831459666817210, 10.02601051567788204 ) ) ;
#53184=CARTESIAN_POINT ( 'NONE',  ( 29.68315524077033629, 13.47185074185905584, 42.10535821593451544 ) ) ;
#53195=B_SPLINE_CURVE_WITH_KNOTS ( 'NONE', 3,
 ( #60194, #52056, #34856, #68805, #34326, #100078, #11056, #10535, #18126, #84442, #35390, #67724, #60714, #93600, #100610, #50982, #83895, #19752, #42916, #75807, #26771, #1903 ),
 .UNSPECIFIED., .F., .F.,
 ( 4, 2, 2, 2, 2, 2, 2, 2, 2, 2, 4 ),
 ( 0.003192110316504342005, 0.003444089597595979216, 0.003696068878687615994, 0.004200027440870891283, 0.004703986003054166573, 0.005207944565237442730, 0.006215861689604012391, 0.006467840970695656541, 0.006719820251787300691, 0.006971799532878944841, 0.007223778813970588991 ),
 .UNSPECIFIED. ) ;
#53199=CARTESIAN_POINT ( 'NONE',  ( 8.377077475354079672E-17, 56.87938524157181774, 0.6840402866513453084 ) ) ;
#53201=DIRECTION ( 'NONE',  ( -0.000000000000000000, 1.000000000000000000, -0.000000000000000000 ) ) ;
#53202=CARTESIAN_POINT ( 'NONE',  ( 6.045898094491907848, 53.95739701478677119, 6.272836224203895306 ) ) ;
#53245=CARTESIAN_POINT ( 'NONE',  ( 9.295649250257604024, 43.59667780448855723, 14.93671105746132710 ) ) ;
#53260=CARTESIAN_POINT ( 'NONE',  ( -1.011534475481120854, 28.02053069269880226, 38.74788564449888639 ) ) ;
#53262=ORIENTED_EDGE ( 'NONE', *, *, #100548, .F. ) ;
#53265=SURFACE_SIDE_STYLE ('',( #10136 ) ) ;
#53302=CARTESIAN_POINT ( 'NONE',  ( 17.53793833829814375, 36.29671191971048927, 24.04345926538296396 ) ) ;
#53305=VERTEX_POINT ( 'NONE', #36219 ) ;
#53313=CARTESIAN_POINT ( 'NONE',  ( -0.7774258472507343809, 36.39397619591250788, 29.48229727820018553 ) ) ;
#53315=EDGE_CURVE ( 'NONE', #6418, #653, #92808, .T. ) ;
#53317=ORIENTED_EDGE ( 'NONE', *, *, #82466, .T. ) ;
#53326=ORIENTED_EDGE ( 'NONE', *, *, #98199, .T. ) ;
#53351=CARTESIAN_POINT ( 'NONE',  ( -48.15129163819138824, 9.495040186444070329, 16.85535821593516559 ) ) ;
#53357=CARTESIAN_POINT ( 'NONE',  ( -30.90717084365936529, 9.524046525575998956, 40.57283699552785095 ) ) ;
#53370=ADVANCED_FACE ( 'NONE', ( #52886 ), #18967, .F. ) ;
#53375=DIRECTION ( 'NONE',  ( -0.000000000000000000, 1.000000000000000000, -0.000000000000000000 ) ) ;
#53388=COLOUR_RGB ( '', 0.08235294, 0.09019608, 0.10196078) ;
#53389=CARTESIAN_POINT ( 'NONE',  ( 27.26394779839380433, 36.55151123035060579, 10.05698433968587580 ) ) ;
#53392=CARTESIAN_POINT ( 'NONE',  ( 29.68315524076926337, 8.302504244945327017, -42.10535821593530414 ) ) ;
#53402=FILL_AREA_STYLE_COLOUR ( '', #70215 ) ;
#53418=CARTESIAN_POINT ( 'NONE',  ( 24.29659155877487464, 27.70505434333144379, 31.30545107321081133 ) ) ;
#53420=CARTESIAN_POINT ( 'NONE',  ( -17.73901163440277884, 36.76451030150755628, -22.27377543627849121 ) ) ;
#53431=CARTESIAN_POINT ( 'NONE',  ( -30.90725857724320846, 14.69157187025842859, -40.57373053090537240 ) ) ;
#53436=FACE_OUTER_BOUND ( 'NONE', #103233, .T. ) ;
#53440=CARTESIAN_POINT ( 'NONE',  ( -9.176942142885224030, 44.04119814292888435, -13.55851898737775052 ) ) ;
#53449=CARTESIAN_POINT ( 'NONE',  ( -1.250293961483907923, 45.68606392481615330, 17.65583989057408587 ) ) ;
#53460=FACE_OUTER_BOUND ( 'NONE', #93622, .T. ) ;
#53477=CARTESIAN_POINT ( 'NONE',  ( 30.90153257058524972, 13.61190038887009024, -41.14606609713278118 ) ) ;
#53489=CARTESIAN_POINT ( 'NONE',  ( 0.9986426376963660756, 14.07186834901433770, 51.25504895071563283 ) ) ;
#53498=EDGE_CURVE ( 'NONE', #73607, #20227, #36750, .T. ) ;
#53515=CARTESIAN_POINT ( 'NONE',  ( -28.08610930860416843, 34.36935600744033792, 8.015707762699872063 ) ) ;
#53523=CARTESIAN_POINT ( 'NONE',  ( 17.71323538867952152, 34.18408009164598127, -23.86039338639478302 ) ) ;
#53527=( GEOMETRIC_REPRESENTATION_CONTEXT ( 3 ) GLOBAL_UNCERTAINTY_ASSIGNED_CONTEXT ( ( #18215 ) ) GLOBAL_UNIT_ASSIGNED_CONTEXT ( ( #20619, #26312, #25783 ) ) REPRESENTATION_CONTEXT ( 'NONE', 'WORKASPACE' ) );
#53542=ORIENTED_EDGE ( 'NONE', *, *, #67974, .F. ) ;
#53549=CARTESIAN_POINT ( 'NONE',  ( -0.08440048694455513922, 28.20649408426940496, -38.25000000000000000 ) ) ;
#53568=CARTESIAN_POINT ( 'NONE',  ( 4.959933632926892599, 51.41894395452099786, -8.497788349702878108 ) ) ;
#53579=CARTESIAN_POINT ( 'NONE',  ( -48.90276556242077532, 14.54846953981632396, -14.70164374843202992 ) ) ;
#53622=CARTESIAN_POINT ( 'NONE',  ( 4.297616547240164842, 51.67621034708934502, 8.057714428547381402 ) ) ;
#53682=CARTESIAN_POINT ( 'NONE',  ( 10.28624191511840458, 45.38549880562042205, 15.40779740156149202 ) ) ;
#53701=CARTESIAN_POINT ( 'NONE',  ( 27.10511071441176867, 34.75829513984540142, -7.556984339686343866 ) ) ;
#53708=LINE ( 'NONE', #37572, #78949 ) ;
#53741=ORIENTED_EDGE ( 'NONE', *, *, #102806, .T. ) ;
#53748=CARTESIAN_POINT ( 'NONE',  ( -5.580966921651770022E-13, 25.16821295365027211, 40.75000000000505906 ) ) ;
#53752=B_SPLINE_CURVE_WITH_KNOTS ( 'NONE', 3,
 ( #12681, #30496, #54196, #63922, #54727, #13743, #63399, #78486, #104350, #71451, #21887, #62860, #87662, #46651, #79551, #5144, #6182, #53166, #87135, #4614 ),
 .UNSPECIFIED., .F., .F.,
 ( 4, 2, 2, 2, 2, 2, 2, 2, 2, 4 ),
 ( 0.007145084556283989689, 0.007649977546646419616, 0.008154870537008848674, 0.008659763527371279468, 0.009164656517733708527, 0.009417103012914925658, 0.009669549508096141055, 0.01017444249845856838, 0.01067933548882099570, 0.01118422847918342303 ),
 .UNSPECIFIED. ) ;
#53754=CYLINDRICAL_SURFACE ( 'NONE', #32682, 1.250000000000000222 ) ;
#53777=CARTESIAN_POINT ( 'NONE',  ( 0.9545024399685089200, 36.45430134163607505, -29.31124438187364234 ) ) ;
#53804=DIRECTION ( 'NONE',  ( 0.000000000000000000, 0.000000000000000000, -1.000000000000000000 ) ) ;
#53810=CARTESIAN_POINT ( 'NONE',  ( -8.239512452575834089, 51.94782406950919551, 1.561983666614737309 ) ) ;
#53816=DIRECTION ( 'NONE',  ( -0.000000000000000000, 1.000000000000000000, -0.000000000000000000 ) ) ;
#53829=CARTESIAN_POINT ( 'NONE',  ( -1.130607513584494406, 36.55099619479304351, 29.03907309283103544 ) ) ;
#53831=COLOUR_RGB ( '', 0.66274510, 0.83137255, 0.94901961) ;
#53856=CARTESIAN_POINT ( 'NONE',  ( 16.41900535493345359, 37.18348077072297997, -21.84048156163012067 ) ) ;
#53857=STYLED_ITEM ( 'NONE', ( #33869 ), #89702 ) ;
#53874=CARTESIAN_POINT ( 'NONE',  ( -30.90131729786687842, 8.441056540751493031, 41.14701368050880603 ) ) ;
#53890=AXIS2_PLACEMENT_3D ( 'NONE', #93160, #68362, #4155 ) ;
#53903=FACE_BOUND ( 'NONE', #88741, .T. ) ;
#53912=EDGE_LOOP ( 'NONE', ( #66059, #47354, #103564, #73067 ) ) ;
#53915=ORIENTED_EDGE ( 'NONE', *, *, #90343, .F. ) ;
#53936=CARTESIAN_POINT ( 'NONE',  ( -30.77392345931232143, 15.52887250063908731, -40.23353194602704264 ) ) ;
#53946=CARTESIAN_POINT ( 'NONE',  ( -0.7775020681061201033, 34.26564639408222490, 29.48222419693123797 ) ) ;
#53953=CARTESIAN_POINT ( 'NONE',  ( -1.248974075102163850, 10.99431765185030052, 50.37162249473301756 ) ) ;
#53967=CARTESIAN_POINT ( 'NONE',  ( -15.65011139837766230, 35.03623782845583889, 22.46068017020301255 ) ) ;
#53968=EDGE_LOOP ( 'NONE', ( #74361, #86134, #97301, #52180 ) ) ;
#53981=CARTESIAN_POINT ( 'NONE',  ( 30.22873954704373745, 12.95661247755295875, -41.98212759391220317 ) ) ;
#53989=CARTESIAN_POINT ( 'NONE',  ( -46.86052085224959995, 18.87480283624657673, 15.15319613412692590 ) ) ;
#53991=( NAMED_UNIT ( * ) SI_UNIT ( $, .STERADIAN. ) SOLID_ANGLE_UNIT ( ) );
#53993=COLOUR_RGB ( '', 0.31764706, 0.68627451, 0.89019608) ;
#53994=CARTESIAN_POINT ( 'NONE',  ( 17.27446834819473054, 43.52264201582065084, 4.281299067926229718 ) ) ;
#53999=CARTESIAN_POINT ( 'NONE',  ( 37.56673239365870387, 25.47613764497372557, 13.45617127780999134 ) ) ;
#54002=EDGE_CURVE ( 'NONE', #85904, #92815, #60868, .T. ) ;
#54007=FACE_BOUND ( 'NONE', #79988, .T. ) ;
#54009=DIRECTION ( 'NONE',  ( -0.000000000000000000, 1.000000000000000000, 0.000000000000000000 ) ) ;
#54018=VERTEX_POINT ( 'NONE', #78612 ) ;
#54020=CARTESIAN_POINT ( 'NONE',  ( -28.10445496912546659, 34.19346676493858439, 9.576006629673763371 ) ) ;
#54025=CARTESIAN_POINT ( 'NONE',  ( -7.681258945454893382E-14, -1.200000000000000030E-05, -39.50000000000000000 ) ) ;
#54071=ORIENTED_EDGE ( 'NONE', *, *, #58333, .F. ) ;
#54072=CARTESIAN_POINT ( 'NONE',  ( -9.781128050978084687, 53.39489088403298211, -3.094517574441575380 ) ) ;
#54086=CARTESIAN_POINT ( 'NONE',  ( -49.15106604892663711, 13.74065395669281919, -15.05054071407247740 ) ) ;
#54091=CARTESIAN_POINT ( 'NONE',  ( 27.86890485335036871, 34.24656432884084722, -9.810347930556213569 ) ) ;
#54101=SURFACE_STYLE_FILL_AREA ( #46560 ) ;
#54131=CARTESIAN_POINT ( 'NONE',  ( 5.290067270632455632, 51.34639538792298197, 8.531152949374481764 ) ) ;
#54134=CARTESIAN_POINT ( 'NONE',  ( 37.72563823326647992, 27.83002455384509233, 10.95617127780987410 ) ) ;
#54137=DIRECTION ( 'NONE',  ( 0.000000000000000000, 1.000000000000000000, 0.000000000000000000 ) ) ;
#54150=CARTESIAN_POINT ( 'NONE',  ( -5.290067270632282437, 54.20842449845790867, 6.031152949371105798 ) ) ;
#54182=UNCERTAINTY_MEASURE_WITH_UNIT (LENGTH_MEASURE( 1.000000000000000082E-05 ), #85424, 'distance_accuracy_value', 'NONE');
#54196=CARTESIAN_POINT ( 'NONE',  ( 26.78538857523856720, 36.99571777491210867, 7.587731473697932216 ) ) ;
#54198=CARTESIAN_POINT ( 'NONE',  ( 17.62275466961044401, 43.36964291604525812, -4.614633819576646978 ) ) ;
#54205=EDGE_CURVE ( 'NONE', #15279, #49001, #68115, .T. ) ;
#54211=EDGE_LOOP ( 'NONE', ( #81406, #55287 ) ) ;
#54242=CARTESIAN_POINT ( 'NONE',  ( -9.383347720677482684, 51.32558664833128148, 3.724917079647517948 ) ) ;
#54268=CARTESIAN_POINT ( 'NONE',  ( 10.12220134229128732, 44.02984809270889599, 12.90779740156146538 ) ) ;
#54271=CARTESIAN_POINT ( 'NONE',  ( 2.848917157793759055E-13, 44.08548369317517768, 16.24999999999732836 ) ) ;
#54301=VERTEX_POINT ( 'NONE', #101190 ) ;
#54314=AXIS2_PLACEMENT_3D ( 'NONE', #86097, #93640, #19789 ) ;
#54321=CARTESIAN_POINT ( 'NONE',  ( 1.248924154308308054, 10.99719009875376230, -50.37041816597272259 ) ) ;
#54341=CARTESIAN_POINT ( 'NONE',  ( -27.85348497893874509, 36.60125607490498112, 7.792768389110043437 ) ) ;
#54373=CARTESIAN_POINT ( 'NONE',  ( -37.72638201607069419, 27.54978895746880951, 13.45617127781066813 ) ) ;
#54374=EDGE_CURVE ( 'NONE', #10253, #92720, #40990, .T. ) ;
#54382=CARTESIAN_POINT ( 'NONE',  ( 29.59409995734579368, 13.24979100942362109, 39.60535821593451544 ) ) ;
#54393=CARTESIAN_POINT ( 'NONE',  ( -15.39919601875319444, 44.07709767825076597, -5.261523372194803372 ) ) ;
#54397=MECHANICAL_DESIGN_GEOMETRIC_PRESENTATION_REPRESENTATION('',(#83680),#81971);
#54419=SURFACE_SIDE_STYLE ('',( #21584 ) ) ;
#54427=MECHANICAL_DESIGN_GEOMETRIC_PRESENTATION_REPRESENTATION('',(#981),#9707);
#54439=CARTESIAN_POINT ( 'NONE',  ( -17.86230688873610006, 36.34004572609662631, -23.65428218925779902 ) ) ;
#54447=CARTESIAN_POINT ( 'NONE',  ( -0.7854097470862259067, 51.35442182215429341, 9.986069114443392181 ) ) ;
#54458=CARTESIAN_POINT ( 'NONE',  ( -1.100320091651754373, 34.84262691055438665, 27.88550462674917796 ) ) ;
#54487=( NAMED_UNIT ( * ) SI_UNIT ( $, .STERADIAN. ) SOLID_ANGLE_UNIT ( ) );
#54499=CARTESIAN_POINT ( 'NONE',  ( 5.290067270632322405, -1.200000000000000030E-05, 7.281152949374479100 ) ) ;
#54512=CARTESIAN_POINT ( 'NONE',  ( -46.77666182531606154, 18.74137236369755755, 15.58806238567861158 ) ) ;
#54530=EDGE_LOOP ( 'NONE', ( #23820, #27378, #69918, #72584 ) ) ;
#54555=B_SPLINE_CURVE_WITH_KNOTS ( 'NONE', 3,
 ( #64254, #16741, #48027, #49632, #73363, #49087, #63725, #22746, #105227, #41545, #39447, #30840, #31373, #89577, #55583, #15146, #81989, #80937, #72836, #105747 ),
 .UNSPECIFIED., .F., .F.,
 ( 4, 2, 2, 2, 2, 2, 2, 2, 2, 4 ),
 ( 0.002407757697027169443, 0.002911641504507399801, 0.003415525311987630593, 0.004423292926948105622, 0.004927176734428342919, 0.005179118638168462435, 0.005431060541908580216, 0.005683002445648699733, 0.005934944349388818381, 0.006438828156869064352 ),
 .UNSPECIFIED. ) ;
#54576=VERTEX_POINT ( 'NONE', #35637 ) ;
#54595=ORIENTED_EDGE ( 'NONE', *, *, #84019, .F. ) ;
#54596=CARTESIAN_POINT ( 'NONE',  ( -9.306447067397133566, 53.68077726991365495, -1.766059074214993974 ) ) ;
#54600=ORIENTED_EDGE ( 'NONE', *, *, #1884, .F. ) ;
#54608=CARTESIAN_POINT ( 'NONE',  ( -49.24259736700098244, 13.36037099746783596, -15.29523612018324741 ) ) ;
#54621=SURFACE_STYLE_FILL_AREA ( #46559 ) ;
#54636=( GEOMETRIC_REPRESENTATION_CONTEXT ( 3 ) GLOBAL_UNCERTAINTY_ASSIGNED_CONTEXT ( ( #67505 ) ) GLOBAL_UNIT_ASSIGNED_CONTEXT ( ( #27572, #18392, #93327 ) ) REPRESENTATION_CONTEXT ( 'NONE', 'WORKASPACE' ) );
#54674=EDGE_CURVE ( 'NONE', #84521, #5811, #55633, .T. ) ;
#54675=EDGE_LOOP ( 'NONE', ( #53262, #11387 ) ) ;
#54691=VERTEX_POINT ( 'NONE', #10117 ) ;
#54700=ORIENTED_EDGE ( 'NONE', *, *, #66250, .T. ) ;
#54720=CARTESIAN_POINT ( 'NONE',  ( 15.70480526265250987, 44.04604958794632807, 4.578183157293787886 ) ) ;
#54727=CARTESIAN_POINT ( 'NONE',  ( 26.34246982073403487, 37.12886783033192728, 7.802669617497731913 ) ) ;
#54730=CARTESIAN_POINT ( 'NONE',  ( 17.26604493211178593, 43.28473347087221157, -6.503856858636642535 ) ) ;
#54735=CARTESIAN_POINT ( 'NONE',  ( 24.46939029779937158, 27.46660112286070188, -31.99934855281030721 ) ) ;
#54737=ORIENTED_EDGE ( 'NONE', *, *, #60022, .F. ) ;
#54739=STYLED_ITEM ( 'NONE', ( #103182 ), #42201 ) ;
#54759=VERTEX_POINT ( 'NONE', #104981 ) ;
#54761=LINE ( 'NONE', #53199, #44921 ) ;
#54770=ORIENTED_EDGE ( 'NONE', *, *, #57320, .F. ) ;
#54775=B_SPLINE_CURVE_WITH_KNOTS ( 'NONE', 3,
 ( #34744, #76214, #58455, #2321, #92936, #67082, #99965, #25598, #43333, #67616, #68135, #66541, #35809, #84322, #35265, #43856, #101029, #51938 ),
 .UNSPECIFIED., .F., .F.,
 ( 4, 2, 2, 2, 2, 2, 2, 2, 4 ),
 ( 0.007188321694818354014, 0.007693711742174220297, 0.008199101789530087447, 0.008704491836885952863, 0.009209881884241818278, 0.009715271931597681959, 0.01022066197895354737, 0.01072605202630941626, 0.01123144207366528168 ),
 .UNSPECIFIED. ) ;
#54809=CARTESIAN_POINT ( 'NONE',  ( -0.1699383547153779650, 25.17130188398262192, -40.74124215288320272 ) ) ;
#54816=SURFACE_STYLE_USAGE ( .BOTH. , #103906 ) ;
#54842=DIRECTION ( 'NONE',  ( 0.000000000000000000, 0.000000000000000000, 1.000000000000000000 ) ) ;
#54862=CARTESIAN_POINT ( 'NONE',  ( -7.566827944241370396, 52.14989601952419207, 2.016859383240065196 ) ) ;
#54873=VERTEX_POINT ( 'NONE', #37503 ) ;
#54880=CARTESIAN_POINT ( 'NONE',  ( -0.3375650005721265723, 36.31234776228274086, 29.71522679684275658 ) ) ;
#54884=ORIENTED_EDGE ( 'NONE', *, *, #84729, .T. ) ;
#54923=CARTESIAN_POINT ( 'NONE',  ( -49.27018817646332849, 7.792903869376758053, 15.76322754694117378 ) ) ;
#54926=EDGE_LOOP ( 'NONE', ( #46175, #54770 ) ) ;
#54956=CARTESIAN_POINT ( 'NONE',  ( 30.04470542674661360, 7.904892719711591020, -42.05337092467530624 ) ) ;
#54961=( NAMED_UNIT ( * ) SI_UNIT ( $, .STERADIAN. ) SOLID_ANGLE_UNIT ( ) );
#54973=CARTESIAN_POINT ( 'NONE',  ( 15.43446081147247106, 46.13172121994917063, -5.765148793919847137 ) ) ;
#54989=CARTESIAN_POINT ( 'NONE',  ( -30.00306714711500433, 17.76853250946121676, -39.63934773235520481 ) ) ;
#55000=CARTESIAN_POINT ( 'NONE',  ( -0.8400705922950577609, 34.28427440775693924, 29.42928587081339487 ) ) ;
#55007=CARTESIAN_POINT ( 'NONE',  ( 8.455951367436818379E-15, 13.70447791526914294, 49.24999999999998579 ) ) ;
#55019=CARTESIAN_POINT ( 'NONE',  ( 22.88936581297007677, 28.17682283790767173, 30.74716342950124570 ) ) ;
#55025=CARTESIAN_POINT ( 'NONE',  ( -16.12403420814926491, 34.43109856403526692, 24.14991543090281567 ) ) ;
#55038=SURFACE_SIDE_STYLE ('',( #35188 ) ) ;
#55044=CARTESIAN_POINT ( 'NONE',  ( 30.64177940627106977, 12.99790429510469281, -41.66010176663461095 ) ) ;
#55090=CARTESIAN_POINT ( 'NONE',  ( 5.290067270632157204, 54.20842449845687838, -6.031152949374584793 ) ) ;
#55109=EDGE_CURVE ( 'NONE', #80390, #52295, #43477, .T. ) ;
#55119=CARTESIAN_POINT ( 'NONE',  ( -11.07117956952426319, 45.30041971330288675, 15.14528042430103660 ) ) ;
#55147=CARTESIAN_POINT ( 'NONE',  ( 16.42383576958776814, 37.18011179812619105, 21.84794872343109517 ) ) ;
#55149=CARTESIAN_POINT ( 'NONE',  ( 0.7775032979944270783, 43.98141867996192644, -16.51775870502402910 ) ) ;
#55192=DIRECTION ( 'NONE',  ( 0.000000000000000000, -0.3420201433256725987, -0.9396926207859068736 ) ) ;
#55198=DIRECTION ( 'NONE',  ( -0.000000000000000000, 1.000000000000000000, -0.000000000000000000 ) ) ;
#55204=CARTESIAN_POINT ( 'NONE',  ( 11.52549757438868028, 43.45827012614538631, 13.79275970915428218 ) ) ;
#55209=AXIS2_PLACEMENT_3D ( 'NONE', #91014, #56068, #31334 ) ;
#55215=CARTESIAN_POINT ( 'NONE',  ( -25.85826872225150552, 37.16337633890192649, -8.997803431316897971 ) ) ;
#55221=CARTESIAN_POINT ( 'NONE',  ( -6.308454306367740294, 53.41350920378196321, 8.025121516174188230 ) ) ;
#55247=DIRECTION ( 'NONE',  ( 0.000000000000000000, 0.000000000000000000, -1.000000000000000000 ) ) ;
#55252=EDGE_LOOP ( 'NONE', ( #74599, #77551 ) ) ;
#55262=CYLINDRICAL_SURFACE ( 'NONE', #11699, 1.250000000000001110 ) ;
#55264=CARTESIAN_POINT ( 'NONE',  ( -24.29659155877464372, 27.70505434333144379, -31.30545107321098541 ) ) ;
#55272=EDGE_LOOP ( 'NONE', ( #105284, #34883, #83490, #99529 ) ) ;
#55273=CARTESIAN_POINT ( 'NONE',  ( 1.013458338643688394, 51.43252368279713238, 9.749812615651872960 ) ) ;
#55276=CARTESIAN_POINT ( 'NONE',  ( -0.4154390169121289778, 51.29111456655304124, -10.18190877321939958 ) ) ;
#55287=ORIENTED_EDGE ( 'NONE', *, *, #90040, .T. ) ;
#55293=CARTESIAN_POINT ( 'NONE',  ( 5.290067270632161645, -1.200000000000000030E-05, -6.031152949374595451 ) ) ;
#55298=MECHANICAL_DESIGN_GEOMETRIC_PRESENTATION_REPRESENTATION('',(#24320),#17444);
#55325=FILL_AREA_STYLE ('',( #24069 ) ) ;
#55338=CARTESIAN_POINT ( 'NONE',  ( 9.502264916438665665, 44.08945810161099388, 13.16974031357852226 ) ) ;
#55344=PRESENTATION_STYLE_ASSIGNMENT (( #54816 ) ) ;
#55365=CARTESIAN_POINT ( 'NONE',  ( -1.251035332617614015, 53.76709749943464089, -9.149874701752242601 ) ) ;
#55375=EDGE_LOOP ( 'NONE', ( #56989, #101305, #86519, #1855 ) ) ;
#55377=ORIENTED_EDGE ( 'NONE', *, *, #55109, .T. ) ;
#55383=AXIS2_PLACEMENT_3D ( 'NONE', #59936, #101437, #85250 ) ;
#55386=FACE_OUTER_BOUND ( 'NONE', #69732, .T. ) ;
#55392=CARTESIAN_POINT ( 'NONE',  ( -7.306464488495704401, 52.17307787027569788, 2.638989770206940477 ) ) ;
#55396=CARTESIAN_POINT ( 'NONE',  ( 1.167761364413894221, 9.591040725253717980, -50.96251430281557049 ) ) ;
#55398=FACE_OUTER_BOUND ( 'NONE', #21896, .T. ) ;
#55431=PRESENTATION_STYLE_ASSIGNMENT (( #80778 ) ) ;
#55435=CARTESIAN_POINT ( 'NONE',  ( -26.12491014859622851, 36.99816777972599624, 9.598909272560698369 ) ) ;
#55439=CARTESIAN_POINT ( 'NONE',  ( 8.559508646656350805, 53.68473964988125857, -4.031152949374623873 ) ) ;
#55454=SURFACE_SIDE_STYLE ('',( #48954 ) ) ;
#55467=STYLED_ITEM ( 'NONE', ( #79453 ), #10508 ) ;
#55485=CARTESIAN_POINT ( 'NONE',  ( 0.000000000000000000, 55.00000000000000000, 0.000000000000000000 ) ) ;
#55509=CARTESIAN_POINT ( 'NONE',  ( -5.290067270632269114, -1.200000000000000030E-05, -8.531152949374520844 ) ) ;
#55512=CARTESIAN_POINT ( 'NONE',  ( -30.93371285580958130, 14.00361151752278666, -40.91601221254722276 ) ) ;
#55546=FILL_AREA_STYLE ('',( #80362 ) ) ;
#55550=( NAMED_UNIT ( * ) PLANE_ANGLE_UNIT ( ) SI_UNIT ( $, .RADIAN. ) );
#55562=CARTESIAN_POINT ( 'NONE',  ( -27.10511071441192144, 36.60571256639527604, -10.05698433968589178 ) ) ;
#55565=LINE ( 'NONE', #16186, #68 ) ;
#55570=CARTESIAN_POINT ( 'NONE',  ( 36.32012801257089052, 28.16013746738074630, 12.39738870050804209 ) ) ;
#55579=CARTESIAN_POINT ( 'NONE',  ( -28.49094055106828449, 13.12977990610419532, -40.46781900651360075 ) ) ;
#55582=CARTESIAN_POINT ( 'NONE',  ( 38.38780340174425731, 25.23068935580986150, 13.15235269662653828 ) ) ;
#55583=CARTESIAN_POINT ( 'NONE',  ( 0.7775251346576579348, 25.97784539287345851, 38.51776489545537885 ) ) ;
#55588=CARTESIAN_POINT ( 'NONE',  ( -28.88579667808738805, 18.87341229088492511, -39.88979553324844574 ) ) ;
#55603=SURFACE_SIDE_STYLE ('',( #46486 ) ) ;
#55633=CIRCLE ( 'NONE', #41881, 33.82893434829264123 ) ;
#55663=CARTESIAN_POINT ( 'NONE',  ( 15.73424097804762489, 37.19149822104526493, 22.31191215652642867 ) ) ;
#55665=CARTESIAN_POINT ( 'NONE',  ( 2.099928008175702901E-23, 44.08548369317413318, -16.25000000000000000 ) ) ;
#55667=CARTESIAN_POINT ( 'NONE',  ( -49.28001195564456083, 13.04047724765254301, -15.62422648184040064 ) ) ;
#55688=EDGE_CURVE ( 'NONE', #60190, #36049, #102700, .T. ) ;
#55720=CARTESIAN_POINT ( 'NONE',  ( 38.66062501847530086, 27.30206768824636754, 12.83416379226657789 ) ) ;
#55721=ORIENTED_EDGE ( 'NONE', *, *, #106116, .T. ) ;
#55731=CARTESIAN_POINT ( 'NONE',  ( -25.89567525304408946, 37.13054467105123280, -9.163018210787793549 ) ) ;
#55736=CARTESIAN_POINT ( 'NONE',  ( -5.290067270632215823, 53.47475093287481229, 8.531152949374556371 ) ) ;
#55742=VECTOR ( 'NONE', #100565, 1000.000000000000000 ) ;
#55752=VERTEX_POINT ( 'NONE', #90941 ) ;
#55767=EDGE_LOOP ( 'NONE', ( #78150, #35264 ) ) ;
#55768=CARTESIAN_POINT ( 'NONE',  ( -22.57534922171806357, 26.08024732591615802, 30.87069056292416391 ) ) ;
#55772=CARTESIAN_POINT ( 'NONE',  ( -15.90864490579666679, 37.20836975595027241, 22.13037531087898557 ) ) ;
#55777=CARTESIAN_POINT ( 'NONE',  ( 0.1684925962546267031, 35.08181111624586634, 27.25000000000001066 ) ) ;
#55784=CARTESIAN_POINT ( 'NONE',  ( -4.506590204516032649, 52.18349789241705139, -6.292748301456810189 ) ) ;
#55790=( NAMED_UNIT ( * ) PLANE_ANGLE_UNIT ( ) SI_UNIT ( $, .RADIAN. ) );
#55801=CARTESIAN_POINT ( 'NONE',  ( 47.24160628166276865, 11.75468494072138625, -16.58444347056465062 ) ) ;
#55812=FACE_OUTER_BOUND ( 'NONE', #68751, .T. ) ;
#55833=CARTESIAN_POINT ( 'NONE',  ( 46.77678417914661679, 18.74709138458479529, 15.58010501040359586 ) ) ;
#55896=FILL_AREA_STYLE ('',( #95873 ) ) ;
#55901=CARTESIAN_POINT ( 'NONE',  ( 1.219713087837473786, 25.73165379248329998, -39.18301856506552383 ) ) ;
#55907=CARTESIAN_POINT ( 'NONE',  ( -0.3346257469825759667, 34.18677894913321325, -29.70731069098821209 ) ) ;
#55908=ORIENTED_EDGE ( 'NONE', *, *, #90598, .T. ) ;
#55911=CARTESIAN_POINT ( 'NONE',  ( -0.3586102644459059907, 18.74914751208079267, 49.30103893526906234 ) ) ;
#55956=CARTESIAN_POINT ( 'NONE',  ( -25.85875814313400411, 37.16303024043016023, 8.999254728584531904 ) ) ;
#55967=FILL_AREA_STYLE_COLOUR ( '', #88038 ) ;
#55976=FACE_OUTER_BOUND ( 'NONE', #19118, .T. ) ;
#55991=LINE ( 'NONE', #87349, #91716 ) ;
#56001=CARTESIAN_POINT ( 'NONE',  ( 11.51372298711423880, 43.27656282359909312, -14.44600693944211933 ) ) ;
#56006=CYLINDRICAL_SURFACE ( 'NONE', #6689, 63.00000000000000000 ) ;
#56007=AXIS2_PLACEMENT_3D ( 'NONE', #47714, #106480, #64974 ) ;
#56008=( NAMED_UNIT ( * ) PLANE_ANGLE_UNIT ( ) SI_UNIT ( $, .RADIAN. ) );
#56024=SURFACE_SIDE_STYLE ('',( #48476 ) ) ;
#56032=CARTESIAN_POINT ( 'NONE',  ( -0.7841117270647198767, 25.97962594934760716, 38.51284013075863299 ) ) ;
#56051=CARTESIAN_POINT ( 'NONE',  ( -1.249981344408581885, 34.67482971135811454, 28.34062085008046949 ) ) ;
#56066=CARTESIAN_POINT ( 'NONE',  ( 23.21751746555303342, 27.38103382803677377, 33.20617127781017075 ) ) ;
#56068=DIRECTION ( 'NONE',  ( -0.000000000000000000, 1.000000000000000000, -0.000000000000000000 ) ) ;
#56095=CARTESIAN_POINT ( 'NONE',  ( 36.56751284714513872, 28.18319525971078576, 11.43687960009742177 ) ) ;
#56107=CARTESIAN_POINT ( 'NONE',  ( 38.69245764546075605, 25.17153636228211511, 12.75614855080256405 ) ) ;
#56113=CARTESIAN_POINT ( 'NONE',  ( -29.07939586085774408, 18.85565742903569486, -39.75811902752995763 ) ) ;
#56116=CARTESIAN_POINT ( 'NONE',  ( 24.06092750555239590, 25.16990051853040811, 32.88256764606778404 ) ) ;
#56122=ADVANCED_FACE ( 'NONE', ( #30333 ), #12518, .F. ) ;
#56137=FILL_AREA_STYLE_COLOUR ( '', #91800 ) ;
#56164=ORIENTED_EDGE ( 'NONE', *, *, #24690, .T. ) ;
#56173=CARTESIAN_POINT ( 'NONE',  ( -5.620533092652015839, 53.42269982616544866, -8.489555698183893995 ) ) ;
#56222=CARTESIAN_POINT ( 'NONE',  ( -38.17830846319614579, 27.65673431820511752, -11.10453014817443318 ) ) ;
#56223=VERTEX_POINT ( 'NONE', #41057 ) ;
#56235=( LENGTH_UNIT ( ) NAMED_UNIT ( * ) SI_UNIT ( .MILLI., .METRE. ) );
#56244=COLOUR_RGB ( '', 0.72549020, 0.75294118, 0.79215686) ;
#56255=VECTOR ( 'NONE', #60205, 1000.000000000000114 ) ;
#56260=CARTESIAN_POINT ( 'NONE',  ( 4.226620391573794039E-15, 29.56666008184760130, 34.51297463494397988 ) ) ;
#56276=ADVANCED_FACE ( 'NONE', ( #50206 ), #27041, .F. ) ;
#56303=CARTESIAN_POINT ( 'NONE',  ( -16.58679117417358739, 36.41790041698920533, 24.30698433968611383 ) ) ;
#56306=( NAMED_UNIT ( * ) PLANE_ANGLE_UNIT ( ) SI_UNIT ( $, .RADIAN. ) );
#56307=CARTESIAN_POINT ( 'NONE',  ( 1.098919214070069206, 34.84343022423479397, 27.88335111672935795 ) ) ;
#56309=( NAMED_UNIT ( * ) PLANE_ANGLE_UNIT ( ) SI_UNIT ( $, .RADIAN. ) );
#56314=CYLINDRICAL_SURFACE ( 'NONE', #44051, 1.250000000000001110 ) ;
#56316=CARTESIAN_POINT ( 'NONE',  ( -5.290067270634260410, 52.08006895350597176, -6.031152949369843697 ) ) ;
#56324=CARTESIAN_POINT ( 'NONE',  ( 1.248999938734115744, 51.75291198392519476, 8.833461820030818146 ) ) ;
#56339=CARTESIAN_POINT ( 'NONE',  ( 47.55643143940710615, 10.90089820249353636, -16.76894861493112643 ) ) ;
#56341=EDGE_LOOP ( 'NONE', ( #12629, #3667 ) ) ;
#56342=VERTEX_POINT ( 'NONE', #51796 ) ;
#56346=DIRECTION ( 'NONE',  ( 0.000000000000000000, 1.000000000000000000, -0.000000000000000000 ) ) ;
#56353=CARTESIAN_POINT ( 'NONE',  ( -9.076500669139843325, 43.77048081941054392, 14.51057422361543559 ) ) ;
#56366=ORIENTED_EDGE ( 'NONE', *, *, #62756, .T. ) ;
#56367=CARTESIAN_POINT ( 'NONE',  ( 47.50596275964315396, 17.89684634806513230, 14.46697959672304101 ) ) ;
#56370=CARTESIAN_POINT ( 'NONE',  ( 6.542037336788293800, 51.42598268746419876, -7.323096805894091510 ) ) ;
#56401=B_SPLINE_CURVE_WITH_KNOTS ( 'NONE', 3,
 ( #31020, #39624, #32066, #72496, #64427, #23452, #83763, #91355, #17469, #86332, #4324, #1229, #84311, #26642, #91870, #26128, #45327, #17996, #43322, #50857 ),
 .UNSPECIFIED., .F., .F.,
 ( 4, 2, 2, 2, 2, 2, 2, 2, 2, 4 ),
 ( 0.0009445086018700379026, 0.001449274952876525692, 0.001954041303883013482, 0.002458807654889501055, 0.002963574005895989062, 0.003468340356902477068, 0.003973106707908964641, 0.004225489883412212114, 0.004477873058915459586, 0.004982639409921949328 ),
 .UNSPECIFIED. ) ;
#56416=CARTESIAN_POINT ( 'NONE',  ( -29.68315524077004497, 8.302504244945346557, -42.10535821593474282 ) ) ;
#56430=VERTEX_POINT ( 'NONE', #62565 ) ;
#56433=ORIENTED_EDGE ( 'NONE', *, *, #93296, .F. ) ;
#56455=CARTESIAN_POINT ( 'NONE',  ( -0.4139970039192563123, 35.05610801426639966, -27.31758834064758190 ) ) ;
#56481=CARTESIAN_POINT ( 'NONE',  ( 22.43351772994257587, 26.08195184212913276, 30.96814220329011746 ) ) ;
#56528=CARTESIAN_POINT ( 'NONE',  ( -27.71646321558792536, 36.65781963206741523, -7.705227733214372599 ) ) ;
#56531=( GEOMETRIC_REPRESENTATION_CONTEXT ( 3 ) GLOBAL_UNCERTAINTY_ASSIGNED_CONTEXT ( ( #22218 ) ) GLOBAL_UNIT_ASSIGNED_CONTEXT ( ( #37013, #102775, #19258 ) ) REPRESENTATION_CONTEXT ( 'NONE', 'WORKASPACE' ) );
#56543=CARTESIAN_POINT ( 'NONE',  ( -26.12980120306467313, 34.86887208967902296, 9.592984429938166357 ) ) ;
#56552=CARTESIAN_POINT ( 'NONE',  ( -6.287528586677907235E-14, 28.20649408426966431, -38.24999999999931077 ) ) ;
#56557=CARTESIAN_POINT ( 'NONE',  ( -17.81928184698856654, 45.39461501854592740, 4.975624619099529689 ) ) ;
#56564=DIRECTION ( 'NONE',  ( -0.000000000000000000, 1.000000000000000000, -0.000000000000000000 ) ) ;
#56586=STYLED_ITEM ( 'NONE', ( #41376 ), #31006 ) ;
#56588=CARTESIAN_POINT ( 'NONE',  ( -16.80185364056168140, 43.70017998952184968, 4.157797401561232675 ) ) ;
#56598=CARTESIAN_POINT ( 'NONE',  ( -28.52985215182788892, 11.34625443571976078, 41.35275482200152197 ) ) ;
#56600=STYLED_ITEM ( 'NONE', ( #75254 ), #76497 ) ;
#56635=CARTESIAN_POINT ( 'NONE',  ( 0.000000000000000000, 45.89575828009193259, 0.000000000000000000 ) ) ;
#56638=VECTOR ( 'NONE', #101272, 1000.000000000000000 ) ;
#56650=CARTESIAN_POINT ( 'NONE',  ( -28.71655383515105697, 10.49725697686257675, -41.65669210871969597 ) ) ;
#56660=SURFACE_SIDE_STYLE ('',( #14603 ) ) ;
#56669=ORIENTED_EDGE ( 'NONE', *, *, #72727, .T. ) ;
#56681=CARTESIAN_POINT ( 'NONE',  ( 28.49074715056170959, 18.29855530143743181, -40.46824935483557795 ) ) ;
#56706=( GEOMETRIC_REPRESENTATION_CONTEXT ( 3 ) GLOBAL_UNCERTAINTY_ASSIGNED_CONTEXT ( ( #83983 ) ) GLOBAL_UNIT_ASSIGNED_CONTEXT ( ( #9844, #34706, #25009 ) ) REPRESENTATION_CONTEXT ( 'NONE', 'WORKASPACE' ) );
#56711=CARTESIAN_POINT ( 'NONE',  ( -5.290067270632216712, 52.08006895350504095, 6.031152949374556371 ) ) ;
#56721=CARTESIAN_POINT ( 'NONE',  ( -6.075342555560988345, 53.39437066006075838, -8.268384239318029572 ) ) ;
#56732=( NAMED_UNIT ( * ) PLANE_ANGLE_UNIT ( ) SI_UNIT ( $, .RADIAN. ) );
#56741=CARTESIAN_POINT ( 'NONE',  ( 0.6416334532436100968, 44.01761382017788549, -16.42407442096259729 ) ) ;
#56742=CARTESIAN_POINT ( 'NONE',  ( -38.78071457445877712, 25.16813833650925503, 12.51568302197794047 ) ) ;
#56757=CARTESIAN_POINT ( 'NONE',  ( -23.21751746555280249, 28.11705169068991239, -30.70617127781034839 ) ) ;
#56762=EDGE_LOOP ( 'NONE', ( #68141, #71185, #41579, #84640 ) ) ;
#56766=VERTEX_POINT ( 'NONE', #4196 ) ;
#56785=SURFACE_STYLE_FILL_AREA ( #22348 ) ;
#56804=STYLED_ITEM ( 'NONE', ( #92681 ), #46117 ) ;
#56824=ORIENTED_EDGE ( 'NONE', *, *, #7044, .F. ) ;
#56831=CARTESIAN_POINT ( 'NONE',  ( 27.85367641560119978, 36.60113970943790918, -7.793258884886260951 ) ) ;
#56841=CARTESIAN_POINT ( 'NONE',  ( 27.26539850557486844, 34.42266064818549864, 10.05698433968570704 ) ) ;
#56849=CARTESIAN_POINT ( 'NONE',  ( 16.48304798889096290, 43.52978450323011117, 6.657797401561433404 ) ) ;
#56872=CARTESIAN_POINT ( 'NONE',  ( -9.443129677144035838, 46.21199370134087303, 13.23108103747117070 ) ) ;
#56882=( NAMED_UNIT ( * ) PLANE_ANGLE_UNIT ( ) SI_UNIT ( $, .RADIAN. ) );
#56887=( NAMED_UNIT ( * ) PLANE_ANGLE_UNIT ( ) SI_UNIT ( $, .RADIAN. ) );
#56890=CARTESIAN_POINT ( 'NONE',  ( 29.68315524077034340, 13.12249633091093415, 39.60535821593451544 ) ) ;
#56917=FILL_AREA_STYLE ('',( #90365 ) ) ;
#56926=CARTESIAN_POINT ( 'NONE',  ( -9.170934695443028417, 53.73492620751849813, 1.679349929019868570 ) ) ;
#56935=CARTESIAN_POINT ( 'NONE',  ( 5.622453258321459479, 53.42013071948692016, 8.498021148331359242 ) ) ;
#56951=CARTESIAN_POINT ( 'NONE',  ( 15.73414724454982583, 35.06317813786103699, 22.31186484002455472 ) ) ;
#56960=DIRECTION ( 'NONE',  ( 0.000000000000000000, 1.000000000000000000, -0.000000000000000000 ) ) ;
#56985=CARTESIAN_POINT ( 'NONE',  ( 0.5686146804203622285, 53.44061092886668973, -10.11633179230661206 ) ) ;
#56989=ORIENTED_EDGE ( 'NONE', *, *, #7455, .F. ) ;
#57002=CARTESIAN_POINT ( 'NONE',  ( 47.14858110737401375, 13.36679009520640093, 14.71571165017371463 ) ) ;
#57025=CARTESIAN_POINT ( 'NONE',  ( -27.26426147078658602, 34.70249704477448205, -7.556984339685874019 ) ) ;
#57033=DIRECTION ( 'NONE',  ( 0.000000000000000000, 0.000000000000000000, 1.000000000000000000 ) ) ;
#57036=UNCERTAINTY_MEASURE_WITH_UNIT (LENGTH_MEASURE( 1.000000000000000082E-05 ), #22561, 'distance_accuracy_value', 'NONE');
#57043=CARTESIAN_POINT ( 'NONE',  ( 0.07794078601782293558, 18.87382441218279538, 49.24999999999998579 ) ) ;
#57050=CARTESIAN_POINT ( 'NONE',  ( 28.77610217197986486, 13.65956388957901524, 39.99200581488069872 ) ) ;
#57053=EDGE_CURVE ( 'NONE', #13222, #88217, #24128, .T. ) ;
#57055=CARTESIAN_POINT ( 'NONE',  ( 28.45500467043821047, 17.07616014098844559, 41.11859397474279376 ) ) ;
#57061=MECHANICAL_DESIGN_GEOMETRIC_PRESENTATION_REPRESENTATION('',(#58792),#67414);
#57074=CARTESIAN_POINT ( 'NONE',  ( 5.290067270632397012, 54.20842449845690680, 6.031152949374294359 ) ) ;
#57086=FACE_OUTER_BOUND ( 'NONE', #97487, .T. ) ;
#57105=CARTESIAN_POINT ( 'NONE',  ( -30.42537733501908548, 12.90981014178662001, 41.86413436173241820 ) ) ;
#57115=CARTESIAN_POINT ( 'NONE',  ( -0.08513827788200560576, 51.26930509877139031, 10.24999999999999822 ) ) ;
#57117=CARTESIAN_POINT ( 'NONE',  ( -17.81989518783386828, 43.26589036823222045, 4.977204039784022704 ) ) ;
#57122=AXIS2_PLACEMENT_3D ( 'NONE', #29255, #94493, #52404 ) ;
#57129=CARTESIAN_POINT ( 'NONE',  ( -10.45127858233877127, 43.22611363095290216, -15.39966633374197258 ) ) ;
#57130=CARTESIAN_POINT ( 'NONE',  ( -28.79545026039450661, 10.21913446882438059, 41.74404769594809039 ) ) ;
#57136=CARTESIAN_POINT ( 'NONE',  ( 36.62653249502783126, 28.16896743844737472, -11.37818750331463669 ) ) ;
#57141=CARTESIAN_POINT ( 'NONE',  ( 28.17375089705461377, 34.32482771417988232, -8.153477830591306486 ) ) ;
#57144=CARTESIAN_POINT ( 'NONE',  ( -36.34588046138484430, 26.08150859950978528, -11.88946398838879936 ) ) ;
#57151=B_SPLINE_CURVE_WITH_KNOTS ( 'NONE', 3,
 ( #24287, #50626, #16694, #105693, #41495, #8593, #90585, #40971, #15622, #42026, #74383, #73859, #81405, #24810, #98136, #66305, #57136, #7516, #9117, #106754, #74909, #106210 ),
 .UNSPECIFIED., .F., .F.,
 ( 4, 2, 2, 2, 2, 2, 2, 2, 2, 2, 4 ),
 ( 0.007135418818287256673, 0.007639688340070102668, 0.008143957861852950397, 0.008396092622744374262, 0.008648227383635799861, 0.009152496905418661469, 0.009656766427201524811, 0.009908901188092952145, 0.01016103594898437948, 0.01066530547076722027, 0.01116957499255006279 ),
 .UNSPECIFIED. ) ;
#57182=CARTESIAN_POINT ( 'NONE',  ( 38.64309545302648274, 25.32034139323217303, 11.54985948942248442 ) ) ;
#57192=CARTESIAN_POINT ( 'NONE',  ( 23.21751746555303342, 25.25267828308493989, 33.20617127781017075 ) ) ;
#57196=CARTESIAN_POINT ( 'NONE',  ( 4.660622226121999390, 53.64064877316351954, 8.373216872651239484 ) ) ;
#57217=DIRECTION ( 'NONE',  ( 0.000000000000000000, 1.000000000000000000, 0.000000000000000000 ) ) ;
#57240=ORIENTED_EDGE ( 'NONE', *, *, #1332, .T. ) ;
#57248=CARTESIAN_POINT ( 'NONE',  ( 17.89152967391262905, 43.20852219665771088, -5.298485905622539072 ) ) ;
#57266=CARTESIAN_POINT ( 'NONE',  ( -49.13582233779567332, 7.783546568855187253, -16.18978396958260646 ) ) ;
#57275=CYLINDRICAL_SURFACE ( 'NONE', #14667, 1.250000000000000222 ) ;
#57277=B_SPLINE_CURVE_WITH_KNOTS ( 'NONE', 3,
 ( #101772, #50541, #34423, #1461, #19845, #101254, #10624, #67295, #41935, #76961, #52680, #99640, #9026, #52151, #17678, #27408, #19323, #58669, #59735, #100173, #51618, #43012, #83456, #85066 ),
 .UNSPECIFIED., .F., .F.,
 ( 4, 2, 2, 2, 2, 2, 2, 2, 2, 2, 2, 4 ),
 ( 0.004982501964703167467, 0.005234564667989247827, 0.005486627371275329054, 0.005990752777847501917, 0.006494878184419674780, 0.006999003590991847643, 0.007251066294277925400, 0.007503128997564004893, 0.008007254404136165613, 0.008511379810708326332, 0.008763442513994402355, 0.009015505217280478378 ),
 .UNSPECIFIED. ) ;
#57302=FACE_OUTER_BOUND ( 'NONE', #63819, .T. ) ;
#57314=CARTESIAN_POINT ( 'NONE',  ( 1.250068677369559955, 34.55937372842163313, -28.65813469251532908 ) ) ;
#57320=EDGE_CURVE ( 'NONE', #50509, #85798, #75345, .T. ) ;
#57323=CARTESIAN_POINT ( 'NONE',  ( 49.07509721567211614, 8.836758769845308947, 14.91787708872405993 ) ) ;
#57325=CARTESIAN_POINT ( 'NONE',  ( 1.220516205144134947, 43.50113954421431117, 17.81384183994350678 ) ) ;
#57330=CARTESIAN_POINT ( 'NONE',  ( 0.000000000000000000, -1.200000000000000030E-05, -9.000000000000000000 ) ) ;
#57348=EDGE_CURVE ( 'NONE', #67879, #54018, #97704, .T. ) ;
#57370=DIRECTION ( 'NONE',  ( 0.000000000000000000, 0.000000000000000000, -1.000000000000000000 ) ) ;
#57383=CARTESIAN_POINT ( 'NONE',  ( -16.80328583523074570, 45.82802980027265960, -4.157797401561525774 ) ) ;
#57387=EDGE_LOOP ( 'NONE', ( #51001, #64951, #79576, #20086 ) ) ;
#57399=CARTESIAN_POINT ( 'NONE',  ( 1.009888436704913683, 46.02255095878446411, 16.74547954875638567 ) ) ;
#57403=CARTESIAN_POINT ( 'NONE',  ( -11.29905645152040350, 45.32368457861270628, -14.89516444794125860 ) ) ;
#57406=CARTESIAN_POINT ( 'NONE',  ( 46.78648606410028066, 13.65508681559503223, -15.44775621776510732 ) ) ;
#57408=CARTESIAN_POINT ( 'NONE',  ( -37.56673239365849781, 27.60449318992554169, 13.45617127781067168 ) ) ;
#57417=CARTESIAN_POINT ( 'NONE',  ( -9.657190910579735998, 43.43017001567654489, 15.25012657391256354 ) ) ;
#57434=CARTESIAN_POINT ( 'NONE',  ( 5.615901427346222441, 51.99194348808828181, -6.063755289240993385 ) ) ;
#57454=MECHANICAL_DESIGN_GEOMETRIC_PRESENTATION_REPRESENTATION('',(#14421),#10958);
#57457=CARTESIAN_POINT ( 'NONE',  ( -1.010512028542145835, 25.89279316576818601, -38.74621732557902476 ) ) ;
#57465=CARTESIAN_POINT ( 'NONE',  ( 1.220421971816566309, 45.62918557654543861, -17.81470306399649672 ) ) ;
#57467=B_SPLINE_CURVE_WITH_KNOTS ( 'NONE', 3,
 ( #36778, #69643, #71218, #55019, #87950, #48524, #30798, #73324, #40444, #15631, #72798, #47464, #73869, #106222, #105703, #6473, #23768, #23227, #98146, #89008, #39405, #31846, #106764, #81415, #7526, #56066 ),
 .UNSPECIFIED., .F., .F.,
 ( 4, 2, 2, 2, 2, 2, 2, 2, 2, 2, 2, 2, 4 ),
 ( 0.003090214743966921036, 0.003342416748342327739, 0.003594618752717734442, 0.003846820757093141578, 0.004099022761468547847, 0.004603426770219354314, 0.004855628774594765787, 0.005107830778970177260, 0.006116638796471883868, 0.006368840800847312689, 0.006621042805222741509, 0.006873244809598170330, 0.007125446813973600017 ),
 .UNSPECIFIED. ) ;
#57486=ORIENTED_EDGE ( 'NONE', *, *, #103889, .F. ) ;
#57494=MECHANICAL_DESIGN_GEOMETRIC_PRESENTATION_REPRESENTATION('',(#19615),#38526);
#57497=VECTOR ( 'NONE', #87394, 1000.000000000000000 ) ;
#57503=CARTESIAN_POINT ( 'NONE',  ( 9.182151393623465552, 45.78138532639618319, 14.82507784383104621 ) ) ;
#57530=DIRECTION ( 'NONE',  ( 0.000000000000000000, 0.000000000000000000, 1.000000000000000000 ) ) ;
#57540=ORIENTED_EDGE ( 'NONE', *, *, #5146, .F. ) ;
#57543=B_SPLINE_CURVE_WITH_KNOTS ( 'NONE', 3,
 ( #59867, #11270, #28053, #100821, #44204, #60403, #70065, #77090, #93811, #93283, #69019, #67938, #18897, #78149, #102967, #3209, #36149, #52814, #84658, #77628 ),
 .UNSPECIFIED., .F., .F.,
 ( 4, 2, 2, 2, 2, 2, 2, 2, 2, 4 ),
 ( 0.001107850312301168066, 0.001612907343245352943, 0.002117964374189537820, 0.002623021405133722696, 0.003128078436077907573, 0.003380606951549999795, 0.003633135467022092450, 0.004138192497966277326, 0.004643249528910462637, 0.005148306559854647080 ),
 .UNSPECIFIED. ) ;
#57558=CARTESIAN_POINT ( 'NONE',  ( 7.941476738584017703, 54.17312961474247857, -1.691542695135636043 ) ) ;
#57563=STYLED_ITEM ( 'NONE', ( #44458 ), #87330 ) ;
#57566=VERTEX_POINT ( 'NONE', #17885 ) ;
#57576=CARTESIAN_POINT ( 'NONE',  ( 28.43345358725029115, 12.59863739772601399, 40.78014218160711124 ) ) ;
#57584=CARTESIAN_POINT ( 'NONE',  ( -10.28624191511816832, 43.25714326066847804, -15.40779740156204980 ) ) ;
#57597=CYLINDRICAL_SURFACE ( 'NONE', #96647, 11.27631144943088515 ) ;
#57600=ORIENTED_EDGE ( 'NONE', *, *, #26804, .F. ) ;
#57602=( LENGTH_UNIT ( ) NAMED_UNIT ( * ) SI_UNIT ( .MILLI., .METRE. ) );
#57611=SURFACE_SIDE_STYLE ('',( #40920 ) ) ;
#57612=CARTESIAN_POINT ( 'NONE',  ( -17.40646473312639841, 45.37698912868007284, 6.411815653116708091 ) ) ;
#57620=CARTESIAN_POINT ( 'NONE',  ( 16.02154979717257177, 46.08966533359958362, 4.311187973113217886 ) ) ;
#57623=CARTESIAN_POINT ( 'NONE',  ( 15.45347762069375008, 46.21495662470461241, -5.015962831654205090 ) ) ;
#57629=CARTESIAN_POINT ( 'NONE',  ( -0.6457802288624886478, 26.01561404131637900, 38.41666353100805509 ) ) ;
#57645=CARTESIAN_POINT ( 'NONE',  ( -17.64329793883007014, 43.19648771793908537, 6.176246302466131155 ) ) ;
#57648=CARTESIAN_POINT ( 'NONE',  ( 48.48434714564498194, 13.98045800628846536, 16.77138779655850342 ) ) ;
#57655=CARTESIAN_POINT ( 'NONE',  ( -29.50913623581989143, 8.560131685753201936, 42.09559527950047197 ) ) ;
#57661=CARTESIAN_POINT ( 'NONE',  ( 9.646529840909229492, 51.27688607554693334, 3.403973221859950549 ) ) ;
#57666=CARTESIAN_POINT ( 'NONE',  ( 27.71631011201982275, 34.52951940293964128, -7.705211021039788832 ) ) ;
#57681=ADVANCED_FACE ( 'NONE', ( #7982 ), #81858, .F. ) ;
#57688=CARTESIAN_POINT ( 'NONE',  ( -38.19782146056491712, 25.52416208525854913, -11.07986758502889835 ) ) ;
#57701=FILL_AREA_STYLE ('',( #50159 ) ) ;
#57702=SURFACE_STYLE_FILL_AREA ( #73899 ) ;
#57705=CARTESIAN_POINT ( 'NONE',  ( 38.54706409169610026, 25.36787315721333869, 11.41424143689304316 ) ) ;
#57712=CYLINDRICAL_SURFACE ( 'NONE', #2713, 1.250000000000001110 ) ;
#57730=CARTESIAN_POINT ( 'NONE',  ( -4.648081478759306329, 52.18157122484780075, 6.195523926019952832 ) ) ;
#57735=CARTESIAN_POINT ( 'NONE',  ( 28.98629307556451096, 14.82330134267482968, -41.90042541400673315 ) ) ;
#57746=ORIENTED_EDGE ( 'NONE', *, *, #80719, .F. ) ;
#57755=CARTESIAN_POINT ( 'NONE',  ( -0.08408805189534301894, 54.30758622938873259, 7.749999999999999112 ) ) ;
#57792=STYLED_ITEM ( 'NONE', ( #29983 ), #9182 ) ;
#57793=CYLINDRICAL_SURFACE ( 'NONE', #98901, 1.250000000000001110 ) ;
#57797=ORIENTED_EDGE ( 'NONE', *, *, #35011, .T. ) ;
#57816=CARTESIAN_POINT ( 'NONE',  ( 26.94560983199210469, 36.66014041605558305, -10.05698433968642291 ) ) ;
#57820=CARTESIAN_POINT ( 'NONE',  ( -23.13516888326535081, 27.39820858062317654, -33.20617127781034839 ) ) ;
#57832=CARTESIAN_POINT ( 'NONE',  ( 38.78087356411477060, 27.29650668150768666, -12.51507624832616195 ) ) ;
#57844=CARTESIAN_POINT ( 'NONE',  ( 1.130275170373804983, 34.42238785691029079, -29.03978118008791398 ) ) ;
#57856=CARTESIAN_POINT ( 'NONE',  ( 0.1691482177511390850, 43.17849576545665258, 18.74134708137945537 ) ) ;
#57870=CARTESIAN_POINT ( 'NONE',  ( 36.31401350675979245, 26.07298798432232090, 12.06078247660970071 ) ) ;
#57917=B_SPLINE_CURVE_WITH_KNOTS ( 'NONE', 3,
 ( #56316, #96817, #22949, #81140, #47179, #6188, #55784, #7249, #17499, #8315, #100516, #81654, #67638, #49293, #50889, #82199, #57923, #65505, #24542, #74105, #9907, #716 ),
 .UNSPECIFIED., .F., .F.,
 ( 4, 2, 2, 2, 2, 2, 2, 2, 2, 2, 4 ),
 ( 0.002790526113034574960, 0.003042863289720283172, 0.003295200466405991818, 0.003799874819777412146, 0.004052211996463120358, 0.004304549173148828137, 0.004809223526520248898, 0.005313897879891668792, 0.005818572233263088686, 0.006323246586634508580, 0.006827920940005928474 ),
 .UNSPECIFIED. ) ;
#57921=( NAMED_UNIT ( * ) PLANE_ANGLE_UNIT ( ) SI_UNIT ( $, .RADIAN. ) );
#57923=CARTESIAN_POINT ( 'NONE',  ( -4.298373348636018498, 51.67582542842902171, -8.058508091860746347 ) ) ;
#57937=CARTESIAN_POINT ( 'NONE',  ( -10.45113867624388071, 45.35217484112028075, -15.40779740156158084 ) ) ;
#57946=CARTESIAN_POINT ( 'NONE',  ( -15.99012395148572629, 34.48504170391973389, -24.06089424805132992 ) ) ;
#57948=AXIS2_PLACEMENT_3D ( 'NONE', #100333, #26498, #84693 ) ;
#57954=CARTESIAN_POINT ( 'NONE',  ( 30.59731729458148664, 7.793314453875814785, 41.71112871039118630 ) ) ;
#57955=VERTEX_POINT ( 'NONE', #73241 ) ;
#57960=MECHANICAL_DESIGN_GEOMETRIC_PRESENTATION_REPRESENTATION('',(#4541),#80357);
#57966=B_SPLINE_CURVE_WITH_KNOTS ( 'NONE', 3,
 ( #1142, #83157, #66988, #76122, #90725, #99869, #65911, #16839, #2218, #35168, #26042, #68035, #57266, #82080, #8199, #41110, #74, #33045, #36251, #4904, #28679, #37300, #70166, #3845, #19537, #92837, #10838, #29225, #27625, #94459, #19001, #61563 ),
 .UNSPECIFIED., .F., .F.,
 ( 4, 2, 2, 2, 2, 2, 2, 2, 2, 2, 2, 2, 2, 2, 2, 4 ),
 ( 0.01223842624040716656, 0.01316182229273517301, 0.01362352031889916930, 0.01408521834506316732, 0.01431606735814517500, 0.01454691637122718442, 0.01477776538430919037, 0.01500861439739119979, 0.01523946341047320747, 0.01547031242355521342, 0.01593201044971922359, 0.01639370847588323202, 0.01685540650204724045, 0.01777880255437524690, 0.01870219860670325335, 0.01962559465903125980 ),
 .UNSPECIFIED. ) ;
#57995=CARTESIAN_POINT ( 'NONE',  ( 37.72580964046798613, 25.70160911691909433, -10.95617127781097899 ) ) ;
#58000=CARTESIAN_POINT ( 'NONE',  ( -0.3334083441215401900, 43.18996287760407427, 18.70763396291626179 ) ) ;
#58016=CARTESIAN_POINT ( 'NONE',  ( 15.52452758388592535, 34.97031437783925867, 22.76750761962476233 ) ) ;
#58043=CARTESIAN_POINT ( 'NONE',  ( 9.882762594765912567, 45.48558064014432745, 15.34364832776098275 ) ) ;
#58058=ORIENTED_EDGE ( 'NONE', *, *, #101530, .F. ) ;
#58063=CARTESIAN_POINT ( 'NONE',  ( 2.985641311035224431E-22, 35.08181111624585213, -27.25000000000000000 ) ) ;
#58067=ORIENTED_EDGE ( 'NONE', *, *, #21101, .F. ) ;
#58077=EDGE_LOOP ( 'NONE', ( #69898, #94226 ) ) ;
#58079=CARTESIAN_POINT ( 'NONE',  ( 22.07915843411224444, 26.01897790090626827, 31.43308708091262105 ) ) ;
#58081=CYLINDRICAL_SURFACE ( 'NONE', #18771, 1.249999999999999334 ) ;
#58103=UNCERTAINTY_MEASURE_WITH_UNIT (LENGTH_MEASURE( 1.000000000000000082E-05 ), #75743, 'distance_accuracy_value', 'NONE');
#58129=CARTESIAN_POINT ( 'NONE',  ( 23.05251019904558163, 27.41544800856653197, -33.20617127781074629 ) ) ;
#58134=SURFACE_STYLE_FILL_AREA ( #34440 ) ;
#58146=CARTESIAN_POINT ( 'NONE',  ( 29.68315524076926337, -1.200000000000000030E-05, -42.10535821593530414 ) ) ;
#58147=ORIENTED_EDGE ( 'NONE', *, *, #16049, .T. ) ;
#58150=CARTESIAN_POINT ( 'NONE',  ( -26.18202783569196157, 34.84340182765555483, 9.653642326100298376 ) ) ;
#58153=CARTESIAN_POINT ( 'NONE',  ( 10.61682093389897830, 43.20212652150377863, -15.36618043917111187 ) ) ;
#58163=B_SPLINE_CURVE_WITH_KNOTS ( 'NONE', 3,
 ( #9501, #66697, #8976, #41879, #74768, #33824, #42957, #92561, #75849, #99578, #25755, #91515, #42414, #84482, #59147, #10575, #51026, #50490, #83403, #75307 ),
 .UNSPECIFIED., .F., .F.,
 ( 4, 2, 2, 2, 2, 2, 2, 2, 2, 4 ),
 ( 0.006825806956960024478, 0.007331941334980166675, 0.007838075713000309738, 0.008344210091020451067, 0.008597277280030523466, 0.008850344469040594131, 0.009356478847060733725, 0.009862613225080873319, 0.01036874760310101118, 0.01087488198112114730 ),
 .UNSPECIFIED. ) ;
#58169=CARTESIAN_POINT ( 'NONE',  ( 16.32527301256097374, 45.99414959098179168, 4.187920679398761337 ) ) ;
#58185=( GEOMETRIC_REPRESENTATION_CONTEXT ( 3 ) GLOBAL_UNCERTAINTY_ASSIGNED_CONTEXT ( ( #21191 ) ) GLOBAL_UNIT_ASSIGNED_CONTEXT ( ( #57602, #82433, #74330 ) ) REPRESENTATION_CONTEXT ( 'NONE', 'WORKASPACE' ) );
#58197=CARTESIAN_POINT ( 'NONE',  ( -5.454378341225808668, 52.03812197093989766, -6.039378168782938872 ) ) ;
#58203=CARTESIAN_POINT ( 'NONE',  ( -29.35771261243686325, 8.827287181787188075, 42.06472072717348709 ) ) ;
#58231=CARTESIAN_POINT ( 'NONE',  ( -4.080135247164482060, 53.97828331548330283, 7.632653361217891508 ) ) ;
#58234=CARTESIAN_POINT ( 'NONE',  ( -38.77591069324474660, 25.24252798765403583, -11.84938028368475749 ) ) ;
#58237=FACE_BOUND ( 'NONE', #31675, .T. ) ;
#58266=SURFACE_STYLE_USAGE ( .BOTH. , #100842 ) ;
#58278=ORIENTED_EDGE ( 'NONE', *, *, #71476, .T. ) ;
#58294=( LENGTH_UNIT ( ) NAMED_UNIT ( * ) SI_UNIT ( .MILLI., .METRE. ) );
#58301=B_SPLINE_CURVE_WITH_KNOTS ( 'NONE', 3,
 ( #55439, #105594, #31738, #30688, #46313, #47361, #80249, #64107, #42457, #1450, #49480, #7957, #81831, #65676, #82386, #89949, #48938, #8493, #65142, #57558, #83982, #59194, #67285, #34413 ),
 .UNSPECIFIED., .F., .F.,
 ( 4, 2, 2, 2, 2, 2, 2, 2, 2, 2, 2, 4 ),
 ( 0.007007265619152588075, 0.007512813293216469464, 0.008018360967280349985, 0.008523908641344231374, 0.008776682478376171201, 0.009029456315408111028, 0.009282230152440052590, 0.009535003989471992417, 0.01004055166353587381, 0.01029332550056781537, 0.01054609933759975346, 0.01105164701166362271 ),
 .UNSPECIFIED. ) ;
#58306=CARTESIAN_POINT ( 'NONE',  ( -1.217992623198289381, 53.93920336063153798, 8.677145619086617856 ) ) ;
#58323=VECTOR ( 'NONE', #81596, 1000.000000000000114 ) ;
#58332=CARTESIAN_POINT ( 'NONE',  ( 1.530808498934192310E-16, -1.200000000000000030E-05, -18.75000000000000355 ) ) ;
#58333=EDGE_CURVE ( 'NONE', #77058, #18144, #36575, .T. ) ;
#58335=CARTESIAN_POINT ( 'NONE',  ( -24.46206431567210871, 27.53832621860372143, 31.75666539158942570 ) ) ;
#58351=CARTESIAN_POINT ( 'NONE',  ( 15.99452815637142322, 36.61440916976220450, 24.05462502184699858 ) ) ;
#58380=( NAMED_UNIT ( * ) PLANE_ANGLE_UNIT ( ) SI_UNIT ( $, .RADIAN. ) );
#58383=CARTESIAN_POINT ( 'NONE',  ( -0.2954874734714613149, 18.79241504922601180, -49.28332135316696139 ) ) ;
#58384=CARTESIAN_POINT ( 'NONE',  ( 37.72555958503873796, 27.83005203459011057, -10.95617127781084577 ) ) ;
#58389=( NAMED_UNIT ( * ) SI_UNIT ( $, .STERADIAN. ) SOLID_ANGLE_UNIT ( ) );
#58394=B_SPLINE_CURVE_WITH_KNOTS ( 'NONE', 3,
 ( #49847, #8325, #24553, #74645, #81665, #40693, #25626, #66038, #17508, #42287, #89791, #48773, #73582, #15894, #57399, #106485, #105954, #729, #32642, #32097, #26163, #33166, #33695, #65513 ),
 .UNSPECIFIED., .F., .F.,
 ( 4, 2, 2, 2, 2, 2, 2, 2, 2, 2, 2, 4 ),
 ( 0.003218170336905641204, 0.003470166353295009790, 0.003722162369684378375, 0.004226154402463118583, 0.004730146435241857489, 0.005234138468020597262, 0.005738130500799337036, 0.006242122533578076810, 0.006494118549967440625, 0.006746114566356804440, 0.006998110582746168255, 0.007250106599135532071 ),
 .UNSPECIFIED. ) ;
#58400=CARTESIAN_POINT ( 'NONE',  ( 0.6443172923761060211, 34.22989788132813516, -29.58399804947514866 ) ) ;
#58404=CARTESIAN_POINT ( 'NONE',  ( 7.350040110511026903, 52.09159772936368427, 3.137117077569001378 ) ) ;
#58409=CARTESIAN_POINT ( 'NONE',  ( 0.08528730779465582001, 43.17555810750859280, 18.75000000000001066 ) ) ;
#58429=CARTESIAN_POINT ( 'NONE',  ( -7.980179952708205483E-13, 34.17188553057791722, -29.75000000000694911 ) ) ;
#58436=EDGE_CURVE ( 'NONE', #29217, #46369, #4167, .T. ) ;
#58442=CARTESIAN_POINT ( 'NONE',  ( -16.64348903516517098, 43.47556584774767430, 6.657797401561654560 ) ) ;
#58454=ORIENTED_EDGE ( 'NONE', *, *, #47085, .F. ) ;
#58455=CARTESIAN_POINT ( 'NONE',  ( 8.239573482191097753, 51.66633055143890374, -4.000019732116445681 ) ) ;
#58461=CARTESIAN_POINT ( 'NONE',  ( 15.65045322250983872, 44.05828365038193084, 4.643985932004602191 ) ) ;
#58472=VERTEX_POINT ( 'NONE', #81729 ) ;
#58493=LINE ( 'NONE', #67114, #34369 ) ;
#58514=CARTESIAN_POINT ( 'NONE',  ( 9.807572367705720495, 51.30032996905384834, -2.672138286948423591 ) ) ;
#58522=VERTEX_POINT ( 'NONE', #90924 ) ;
#58526=ADVANCED_FACE ( 'NONE', ( #41826 ), #50436, .F. ) ;
#58530=CARTESIAN_POINT ( 'NONE',  ( -4.237512335919120849E-14, 43.17555810750860701, 18.75000000000000355 ) ) ;
#58539=CARTESIAN_POINT ( 'NONE',  ( -36.39101805957877644, 25.97871564576526993, 12.63848849079480807 ) ) ;
#58561=SURFACE_STYLE_FILL_AREA ( #51512 ) ;
#58587=CYLINDRICAL_SURFACE ( 'NONE', #21439, 1.249999999999999334 ) ;
#58592=CARTESIAN_POINT ( 'NONE',  ( 1.380949872273418351E-15, 0.000000000000000000, -11.27631144943088515 ) ) ;
#58624=CARTESIAN_POINT ( 'NONE',  ( 46.83715889037894442, 13.71037705486508429, 15.21858309684184540 ) ) ;
#58625=( GEOMETRIC_REPRESENTATION_CONTEXT ( 3 ) GLOBAL_UNCERTAINTY_ASSIGNED_CONTEXT ( ( #60750 ) ) GLOBAL_UNIT_ASSIGNED_CONTEXT ( ( #102334, #59234, #51110 ) ) REPRESENTATION_CONTEXT ( 'NONE', 'WORKASPACE' ) );
#58636=CARTESIAN_POINT ( 'NONE',  ( -46.89473120401039097, 12.86731181406129565, -16.16132821689905441 ) ) ;
#58637=FACE_BOUND ( 'NONE', #54675, .T. ) ;
#58644=ORIENTED_EDGE ( 'NONE', *, *, #102503, .F. ) ;
#58649=EDGE_CURVE ( 'NONE', #63888, #49037, #93044, .T. ) ;
#58669=CARTESIAN_POINT ( 'NONE',  ( 17.53682258900642665, 36.29665952923688366, -24.04445569364184720 ) ) ;
#58673=CARTESIAN_POINT ( 'NONE',  ( 15.54266041146151167, 34.77214720869447007, -23.41113234798271847 ) ) ;
#58698=MECHANICAL_DESIGN_GEOMETRIC_PRESENTATION_REPRESENTATION('',(#105192),#100028);
#58725=CYLINDRICAL_SURFACE ( 'NONE', #95552, 1.250000000000001110 ) ;
#58746=CARTESIAN_POINT ( 'NONE',  ( -17.85383517427097999, 34.21385402367462802, -23.65294179858045354 ) ) ;
#58748=CARTESIAN_POINT ( 'NONE',  ( 49.15106604892599051, 13.74065395669558498, 15.05054071407064420 ) ) ;
#58758=ORIENTED_EDGE ( 'NONE', *, *, #99537, .F. ) ;
#58769=CARTESIAN_POINT ( 'NONE',  ( -17.26451694828253736, 43.28515295384694639, -6.504635002224487650 ) ) ;
#58792=STYLED_ITEM ( 'NONE', ( #39826 ), #73803 ) ;
#58793=CARTESIAN_POINT ( 'NONE',  ( 16.48470368732129643, 43.81217145385495826, -4.157797401561333928 ) ) ;
#58803=LINE ( 'NONE', #19447, #98799 ) ;
#58805=DIRECTION ( 'NONE',  ( 0.000000000000000000, 0.000000000000000000, 1.000000000000000000 ) ) ;
#58811=CARTESIAN_POINT ( 'NONE',  ( -37.56673239365863282, 27.60449318992554879, -13.45617127781024891 ) ) ;
#58820=EDGE_CURVE ( 'NONE', #38588, #60788, #76482, .T. ) ;
#58825=CARTESIAN_POINT ( 'NONE',  ( 4.963148786227262299, 54.27416207544131055, 6.071804965689750588 ) ) ;
#58830=CARTESIAN_POINT ( 'NONE',  ( -4.079459744843447311, 51.85061720702498178, 7.630866904860004851 ) ) ;
#58833=CARTESIAN_POINT ( 'NONE',  ( 30.36574723454804925, 11.76891213769397027, -39.80121650896548147 ) ) ;
#58844=ORIENTED_EDGE ( 'NONE', *, *, #7083, .F. ) ;
#58849=ORIENTED_EDGE ( 'NONE', *, *, #88801, .T. ) ;
#58851=( NAMED_UNIT ( * ) SI_UNIT ( $, .STERADIAN. ) SOLID_ANGLE_UNIT ( ) );
#58858=CARTESIAN_POINT ( 'NONE',  ( -1.098502313920018514, 54.05124254343373735, 8.382720770029662205 ) ) ;
#58878=CARTESIAN_POINT ( 'NONE',  ( -0.1699131888054048189, 37.20682675849905507, -27.25876984853695006 ) ) ;
#58879=CARTESIAN_POINT ( 'NONE',  ( 16.96501886467141063, 43.37102725060984199, -6.626625013246036922 ) ) ;
#58901=CARTESIAN_POINT ( 'NONE',  ( 15.93287854420844596, 36.64197083639892583, 24.00465449142940244 ) ) ;
#58920=SURFACE_STYLE_USAGE ( .BOTH. , #19028 ) ;
#58924=SURFACE_STYLE_USAGE ( .BOTH. , #18477 ) ;
#58926=MECHANICAL_DESIGN_GEOMETRIC_PRESENTATION_REPRESENTATION('',(#31380),#84703);
#58928=FACE_OUTER_BOUND ( 'NONE', #57387, .T. ) ;
#58947=CARTESIAN_POINT ( 'NONE',  ( 0.4153015812548951913, 43.19870208648286791, 18.68195870105203937 ) ) ;
#58955=DIRECTION ( 'NONE',  ( 0.000000000000000000, 0.000000000000000000, 1.000000000000000000 ) ) ;
#58962=CARTESIAN_POINT ( 'NONE',  ( -9.686475303456768771, 51.27220077796494735, -3.328476344197629277 ) ) ;
#58966=CARTESIAN_POINT ( 'NONE',  ( 9.038828898411519930, 43.85145043581746904, -14.27146690660104511 ) ) ;
#58973=( NAMED_UNIT ( * ) SI_UNIT ( $, .STERADIAN. ) SOLID_ANGLE_UNIT ( ) );
#59002=FILL_AREA_STYLE_COLOUR ( '', #1273 ) ;
#59006=DIRECTION ( 'NONE',  ( 0.000000000000000000, 0.000000000000000000, 1.000000000000000000 ) ) ;
#59012=EDGE_CURVE ( 'NONE', #10346, #57566, #40374, .T. ) ;
#59026=CARTESIAN_POINT ( 'NONE',  ( -9.522120649308517315, 45.61249502152109159, 15.15976961885335328 ) ) ;
#59030=CARTESIAN_POINT ( 'NONE',  ( 8.559508646656350805, -1.200000000000000030E-05, -4.031152949374623873 ) ) ;
#59035=VERTEX_POINT ( 'NONE', #26107 ) ;
#59049=CARTESIAN_POINT ( 'NONE',  ( 9.307029794195086581, 51.55217658689417703, -1.766585395468054376 ) ) ;
#59058=ADVANCED_FACE ( 'NONE', ( #1208 ), #99383, .F. ) ;
#59064=CARTESIAN_POINT ( 'NONE',  ( -37.40765518169981618, 27.94113209487581528, -10.95617127781004108 ) ) ;
#59086=DIRECTION ( 'NONE',  ( -0.000000000000000000, 1.000000000000000000, -0.000000000000000000 ) ) ;
#59087=EDGE_CURVE ( 'NONE', #89914, #104058, #1770, .T. ) ;
#59107=CARTESIAN_POINT ( 'NONE',  ( 26.02871520198998923, 34.91972164802428580, 9.463174369590962698 ) ) ;
#59110=CARTESIAN_POINT ( 'NONE',  ( -30.42698073564638150, 7.740609016700346956, -41.86289218232771248 ) ) ;
#59140=DIRECTION ( 'NONE',  ( -0.000000000000000000, 1.000000000000000000, 0.000000000000000000 ) ) ;
#59141=ADVANCED_FACE ( 'NONE', ( #41968 ), #99127, .F. ) ;
#59147=CARTESIAN_POINT ( 'NONE',  ( 7.578349687282027958, 54.07909211381803516, 3.571884340861890994 ) ) ;
#59153=CARTESIAN_POINT ( 'NONE',  ( 3.636386562469240082E-15, 36.30024107553216339, 29.75000000000000355 ) ) ;
#59163=EDGE_LOOP ( 'NONE', ( #43389, #14744 ) ) ;
#59166=ORIENTED_EDGE ( 'NONE', *, *, #105476, .F. ) ;
#59171=CARTESIAN_POINT ( 'NONE',  ( -37.17158346111747136, 25.88889118293631952, -11.01749528737839157 ) ) ;
#59184=EDGE_LOOP ( 'NONE', ( #11894, #5055, #44107, #53128 ) ) ;
#59194=CARTESIAN_POINT ( 'NONE',  ( 8.240390551120709617, 54.07589417944840449, -1.561599642362494489 ) ) ;
#59195=UNCERTAINTY_MEASURE_WITH_UNIT (LENGTH_MEASURE( 1.000000000000000082E-05 ), #105425, 'distance_accuracy_value', 'NONE');
#59213=CARTESIAN_POINT ( 'NONE',  ( 22.88839214066227967, 27.45938914059933467, -33.17277703389370203 ) ) ;
#59217=CARTESIAN_POINT ( 'NONE',  ( -29.59231420605931717, 13.59660068169549696, 42.10535821593509098 ) ) ;
#59229=ORIENTED_EDGE ( 'NONE', *, *, #96370, .T. ) ;
#59234=( NAMED_UNIT ( * ) PLANE_ANGLE_UNIT ( ) SI_UNIT ( $, .RADIAN. ) );
#59246=CARTESIAN_POINT ( 'NONE',  ( 10.28624191512063746, 46.12099395432516502, -12.90779740155508826 ) ) ;
#59248=EDGE_LOOP ( 'NONE', ( #94670, #91821, #42312, #76240 ) ) ;
#59249=VECTOR ( 'NONE', #33205, 1000.000000000000000 ) ;
#59255=CARTESIAN_POINT ( 'NONE',  ( 8.559508646656407649, 53.96349637827586321, 1.531152949374444239 ) ) ;
#59259=CARTESIAN_POINT ( 'NONE',  ( 23.21751746555220564, -1.200000000000000030E-05, -31.95617127781077116 ) ) ;
#59263=CARTESIAN_POINT ( 'NONE',  ( -30.93388328643640151, 14.00942575955928682, 40.91282515498028260 ) ) ;
#59268=FILL_AREA_STYLE ('',( #91633 ) ) ;
#59284=CARTESIAN_POINT ( 'NONE',  ( 3.337161262018383995E-15, 37.21016666119768246, 27.25000000000000000 ) ) ;
#59306=CARTESIAN_POINT ( 'NONE',  ( -23.21751746555235840, 25.25267828308461304, -33.20617127781177658 ) ) ;
#59308=VERTEX_POINT ( 'NONE', #37113 ) ;
#59310=CARTESIAN_POINT ( 'NONE',  ( 0.1696663817233923233, 37.20684969797608943, 27.25870950959922467 ) ) ;
#59350=B_SPLINE_CURVE_WITH_KNOTS ( 'NONE', 3,
 ( #72530, #106479, #7255, #81660, #41225, #55273, #32637, #30513, #65509, #56324, #98397, #88726, #90310, #16418, #49298, #73039, #82205, #8321, #63411, #89259 ),
 .UNSPECIFIED., .F., .F.,
 ( 4, 2, 2, 2, 2, 2, 2, 2, 2, 4 ),
 ( 0.003141903260821411921, 0.003645771108259603446, 0.004149638955697794972, 0.004653506803135986497, 0.005157374650574178890, 0.005661242498012371283, 0.006165110345450562808, 0.006668978192888754333, 0.006920912116607849662, 0.007172846040326944991 ),
 .UNSPECIFIED. ) ;
#59363=CARTESIAN_POINT ( 'NONE',  ( 27.85375964729074383, 36.60111159598967134, 7.793250597500285259 ) ) ;
#59375=COLOUR_RGB ( '', 0.09019608, 0.27058824, 0.51372549) ;
#59396=EDGE_CURVE ( 'NONE', #43850, #24510, #53195, .T. ) ;
#59410=CARTESIAN_POINT ( 'NONE',  ( 36.80450393364946393, 25.99766569896315715, -11.20157930558040249 ) ) ;
#59412=CARTESIAN_POINT ( 'NONE',  ( -1.249548360227116905, 36.80417223094376311, -28.33792551024971118 ) ) ;
#59418=FACE_OUTER_BOUND ( 'NONE', #38702, .T. ) ;
#59426=CARTESIAN_POINT ( 'NONE',  ( -1.218812433689057118, 45.85957784483471045, 17.18021691162306652 ) ) ;
#59445=COLOUR_RGB ( '', 0.72549020, 0.75294118, 0.79215686) ;
#59448=CARTESIAN_POINT ( 'NONE',  ( 26.34344435950205465, 37.12862132004229210, -7.801778736123593738 ) ) ;
#59450=SURFACE_STYLE_FILL_AREA ( #2237 ) ;
#59451=FILL_AREA_STYLE ('',( #67005 ) ) ;
#59457=CARTESIAN_POINT ( 'NONE',  ( 30.36547348172748073, 16.93923362554433965, -39.80091097816919188 ) ) ;
#59472=CARTESIAN_POINT ( 'NONE',  ( 16.75187969033515145, -1.200000000000000030E-05, -23.05698433968624528 ) ) ;
#59495=FILL_AREA_STYLE ('',( #44364 ) ) ;
#59510=CARTESIAN_POINT ( 'NONE',  ( -15.65000555345723576, 44.05838121548723052, 4.644554625135834058 ) ) ;
#59532=CARTESIAN_POINT ( 'NONE',  ( -0.4139109374140990671, 28.18113469921472714, -38.31751619540018794 ) ) ;
#59538=CARTESIAN_POINT ( 'NONE',  ( -11.51407961100473010, 43.27659971821058349, 14.44561041839115312 ) ) ;
#59542=DIRECTION ( 'NONE',  ( 0.000000000000000000, 0.000000000000000000, 1.000000000000000000 ) ) ;
#59569=DIRECTION ( 'NONE',  ( 4.738110706560371839E-17, -0.9221233147934838614, 0.3868961001538753219 ) ) ;
#59570=VERTEX_POINT ( 'NONE', #21329 ) ;
#59571=LINE ( 'NONE', #91404, #103897 ) ;
#59581=CARTESIAN_POINT ( 'NONE',  ( -17.53081013949648437, 34.17129575104124939, 24.03823396542000879 ) ) ;
#59602=COLOUR_RGB ( '', 0.72549020, 0.75294118, 0.79215686) ;
#59607=CARTESIAN_POINT ( 'NONE',  ( -36.95256697677980640, 25.70493088644785828, 13.30651231931578415 ) ) ;
#59608=VECTOR ( 'NONE', #101428, 1000.000000000000000 ) ;
#59618=EDGE_CURVE ( 'NONE', #79335, #741, #78994, .T. ) ;
#59619=DIRECTION ( 'NONE',  ( 0.000000000000000000, 1.000000000000000000, 0.000000000000000000 ) ) ;
#59643=CARTESIAN_POINT ( 'NONE',  ( -30.23149608710439651, 7.786108077162772645, -41.98074016422817323 ) ) ;
#59689=CARTESIAN_POINT ( 'NONE',  ( -15.53259594841271962, 37.09623604092400484, -22.76975648258506268 ) ) ;
#59693=CARTESIAN_POINT ( 'NONE',  ( 24.31925498810626607, 25.21059430657137312, -32.55251039702583427 ) ) ;
#59711=ORIENTED_EDGE ( 'NONE', *, *, #55688, .F. ) ;
#59735=CARTESIAN_POINT ( 'NONE',  ( 17.39534200550397713, 36.29816465214055654, -24.14189926133832387 ) ) ;
#59768=DIRECTION ( 'NONE',  ( 0.000000000000000000, 0.000000000000000000, 1.000000000000000000 ) ) ;
#59774=DIRECTION ( 'NONE',  ( 0.000000000000000000, 0.000000000000000000, 1.000000000000000000 ) ) ;
#59804=ORIENTED_EDGE ( 'NONE', *, *, #30652, .F. ) ;
#59814=CARTESIAN_POINT ( 'NONE',  ( 49.27896781154971961, 13.08675713149488473, 15.56311823694137786 ) ) ;
#59819=CARTESIAN_POINT ( 'NONE',  ( -10.28624191511830155, 43.99263840937192782, -12.90779740156156841 ) ) ;
#59828=AXIS2_PLACEMENT_3D ( 'NONE', #105787, #64288, #40526 ) ;
#59840=CARTESIAN_POINT ( 'NONE',  ( -0.1691415264582396272, 46.21383923812596350, -16.25000000000000355 ) ) ;
#59845=CARTESIAN_POINT ( 'NONE',  ( -23.54446046888081412, 25.90716391019113729, -30.73896312393745234 ) ) ;
#59854=VERTEX_POINT ( 'NONE', #11457 ) ;
#59855=CARTESIAN_POINT ( 'NONE',  ( -4.959320189265015166, 53.54750726706794950, 8.497478219416661815 ) ) ;
#59862=CARTESIAN_POINT ( 'NONE',  ( 15.39683056650771675, 44.03739065760672133, -5.597885347425531677 ) ) ;
#59863=VERTEX_POINT ( 'NONE', #86978 ) ;
#59866=B_SPLINE_CURVE_WITH_KNOTS ( 'NONE', 3,
 ( #5797, #38208, #61945, #28524, #53302, #71586, #70012, #30103, #94296, #95888, #71068, #22013, #21488, #87796, #69488, #70550, #29079, #13878 ),
 .UNSPECIFIED., .F., .F.,
 ( 4, 2, 2, 2, 2, 2, 2, 2, 4 ),
 ( 0.007125849503216027947, 0.007630052828287933048, 0.008134256153359838148, 0.008638459478431743249, 0.009142662803503648350, 0.009646866128575553451, 0.01015106945364745855, 0.01065527277871936365, 0.01115947610379126875 ),
 .UNSPECIFIED. ) ;
#59867=CARTESIAN_POINT ( 'NONE',  ( -16.64348903516517098, 45.60392139269950462, 6.657797401561654560 ) ) ;
#59868=ORIENTED_EDGE ( 'NONE', *, *, #31393, .T. ) ;
#59917=DIRECTION ( 'NONE',  ( -0.000000000000000000, 1.000000000000000000, -0.000000000000000000 ) ) ;
#59921=PRESENTATION_STYLE_ASSIGNMENT (( #27036 ) ) ;
#59925=CARTESIAN_POINT ( 'NONE',  ( -29.68315524077004852, -1.200000000000000030E-05, -39.60535821593474282 ) ) ;
#59936=CARTESIAN_POINT ( 'NONE',  ( 0.000000000000000000, 0.000000000000000000, 0.000000000000000000 ) ) ;
#59941=AXIS2_PLACEMENT_3D ( 'NONE', #106468, #25060, #8839 ) ;
#59943=SURFACE_STYLE_FILL_AREA ( #19508 ) ;
#59947=CARTESIAN_POINT ( 'NONE',  ( -6.069413552714997273, 51.26876837080258298, 8.262085557432884642 ) ) ;
#59954=CARTESIAN_POINT ( 'NONE',  ( 1.196618058419959393E-20, 36.30024107553216339, -29.75000000000000355 ) ) ;
#59962=CARTESIAN_POINT ( 'NONE',  ( 16.64348903516523848, 43.47556584774768851, 6.657797401561421857 ) ) ;
#59970=VECTOR ( 'NONE', #85267, 1000.000000000000114 ) ;
#59979=CARTESIAN_POINT ( 'NONE',  ( -7.681258945454893382E-14, -1.200000000000000030E-05, -38.25000000000000000 ) ) ;
#60004=FILL_AREA_STYLE ('',( #50275 ) ) ;
#60011=CARTESIAN_POINT ( 'NONE',  ( 6.692326732991420724E-21, 18.87382441218278828, -49.25000000000000000 ) ) ;
#60015=CARTESIAN_POINT ( 'NONE',  ( 1.231285353216601708, 16.44838349168128033, 50.25257280200809618 ) ) ;
#60022=EDGE_CURVE ( 'NONE', #28485, #22572, #52455, .T. ) ;
#60041=COLOUR_RGB ( '', 0.40784314, 0.44705882, 0.49803922) ;
#60045=CARTESIAN_POINT ( 'NONE',  ( 36.58412289726538802, 25.86933424275333238, 12.99557124040957490 ) ) ;
#60048=CARTESIAN_POINT ( 'NONE',  ( 10.28624191511773844, 43.25714326066793092, -15.40779740156427202 ) ) ;
#60055=CARTESIAN_POINT ( 'NONE',  ( -4.661090069372093581, 53.64050244245383681, -8.373412985213160908 ) ) ;
#60056=ORIENTED_EDGE ( 'NONE', *, *, #15135, .T. ) ;
#60073=EDGE_LOOP ( 'NONE', ( #41527, #78921, #36799, #104886, #42004, #42976, #37580, #82642 ) ) ;
#60091=ADVANCED_FACE ( 'NONE', ( #104191, #79915, #31411, #72876, #31926 ), #97661, .T. ) ;
#60116=CARTESIAN_POINT ( 'NONE',  ( -46.86404804693351878, 18.87323894068644137, -15.14441118170511835 ) ) ;
#60117=ORIENTED_EDGE ( 'NONE', *, *, #97004, .F. ) ;
#60135=CARTESIAN_POINT ( 'NONE',  ( 48.69302399950104387, 8.421789753111580623, -16.66702170536975913 ) ) ;
#60153=CARTESIAN_POINT ( 'NONE',  ( 48.76595811598669883, 13.46359178982426563, -16.61915017902559910 ) ) ;
#60155=CARTESIAN_POINT ( 'NONE',  ( 16.75187969033571989, 36.38380281757302726, 24.30698433968583316 ) ) ;
#60164=CARTESIAN_POINT ( 'NONE',  ( 0.07800279179579312772, 13.70447791526912873, 49.25000000000000711 ) ) ;
#60184=CARTESIAN_POINT ( 'NONE',  ( 4.226620391573794039E-15, 29.56666008184760130, 34.51297463494397988 ) ) ;
#60189=CARTESIAN_POINT ( 'NONE',  ( -7.938137630668183675, 54.17496235756595979, 1.684399108843077864 ) ) ;
#60190=VERTEX_POINT ( 'NONE', #48070 ) ;
#60194=CARTESIAN_POINT ( 'NONE',  ( 4.988960626530190971E-15, 27.29656849860388235, 40.75000000000000000 ) ) ;
#60203=CARTESIAN_POINT ( 'NONE',  ( 0.000000000000000000, 47.29617335651134624, 13.27631144943088515 ) ) ;
#60205=DIRECTION ( 'NONE',  ( 0.000000000000000000, -0.3420201433256725987, -0.9396926207859068736 ) ) ;
#60211=CARTESIAN_POINT ( 'NONE',  ( 4.724649144056972006, 54.30202410408965363, -6.163116443844200987 ) ) ;
#60228=UNCERTAINTY_MEASURE_WITH_UNIT (LENGTH_MEASURE( 1.000000000000000082E-05 ), #106042, 'distance_accuracy_value', 'NONE');
#60230=DIRECTION ( 'NONE',  ( 0.000000000000000000, 0.000000000000000000, 1.000000000000000000 ) ) ;
#60268=CARTESIAN_POINT ( 'NONE',  ( 28.73053610125072410, 13.62316949804204391, -40.04352587319223744 ) ) ;
#60269=CARTESIAN_POINT ( 'NONE',  ( 16.80263806300985863, 45.55013935554967475, -6.657797401561987627 ) ) ;
#60270=LINE ( 'NONE', #85597, #95426 ) ;
#60271=STYLED_ITEM ( 'NONE', ( #32221 ), #48764 ) ;
#60274=ORIENTED_EDGE ( 'NONE', *, *, #47419, .T. ) ;
#60310=CARTESIAN_POINT ( 'NONE',  ( 0.3381605861720692330, 37.19676752111978857, -27.28514138315811266 ) ) ;
#60315=( NAMED_UNIT ( * ) SI_UNIT ( $, .STERADIAN. ) SOLID_ANGLE_UNIT ( ) );
#60334=ORIENTED_EDGE ( 'NONE', *, *, #99094, .F. ) ;
#60343=( NAMED_UNIT ( * ) SI_UNIT ( $, .STERADIAN. ) SOLID_ANGLE_UNIT ( ) );
#60386=CARTESIAN_POINT ( 'NONE',  ( 0.3334405834852849360, 36.31501813831545888, 29.70764397845630000 ) ) ;
#60387=CARTESIAN_POINT ( 'NONE',  ( 16.12471489245790224, 36.55922634087983880, -24.15021214291702378 ) ) ;
#60400=ORIENTED_EDGE ( 'NONE', *, *, #9671, .T. ) ;
#60403=CARTESIAN_POINT ( 'NONE',  ( -15.66258511614958593, 45.99742480776466635, 6.198981311147433004 ) ) ;
#60438=CARTESIAN_POINT ( 'NONE',  ( 27.10511071441197117, 36.60571256639528315, 10.05698433968570704 ) ) ;
#60442=ADVANCED_FACE ( 'NONE', ( #28638 ), #29699, .T. ) ;
#60448=LINE ( 'NONE', #52855, #73825 ) ;
#60469=CARTESIAN_POINT ( 'NONE',  ( 24.00351036083323564, 27.29299690957943980, 32.94270042870552828 ) ) ;
#60481=CARTESIAN_POINT ( 'NONE',  ( -29.87260017595988515, 13.22901743408734276, -42.09629626707205574 ) ) ;
#60484=AXIS2_PLACEMENT_3D ( 'NONE', #4428, #22234, #38931 ) ;
#60488=FACE_BOUND ( 'NONE', #29628, .T. ) ;
#60510=CARTESIAN_POINT ( 'NONE',  ( 1.153719650317168133E-13, -1.200000000000000030E-05, 49.25000000000000000 ) ) ;
#60534=( NAMED_UNIT ( * ) SI_UNIT ( $, .STERADIAN. ) SOLID_ANGLE_UNIT ( ) );
#60535=CARTESIAN_POINT ( 'NONE',  ( 37.88797360199545494, 27.49820559598491343, -13.42505087926272189 ) ) ;
#60538=CARTESIAN_POINT ( 'NONE',  ( 1.251110940609005739, 15.60643737211089110, 50.60543736410414084 ) ) ;
#60559=EDGE_LOOP ( 'NONE', ( #75399, #42364, #34185, #51127, #30959, #76281, #105435 ) ) ;
#60576=SURFACE_STYLE_FILL_AREA ( #43832 ) ;
#60592=VECTOR ( 'NONE', #28074, 1000.000000000000000 ) ;
#60642=LINE ( 'NONE', #59030, #71925 ) ;
#60657=CARTESIAN_POINT ( 'NONE',  ( 48.49490330227207124, 10.48921555948079387, -14.43974515806029579 ) ) ;
#60677=DIRECTION ( 'NONE',  ( 0.000000000000000000, 1.000000000000000000, -0.000000000000000000 ) ) ;
#60714=CARTESIAN_POINT ( 'NONE',  ( 1.125484721681054401, 27.97705396987858961, 38.86472904274390316 ) ) ;
#60715=CARTESIAN_POINT ( 'NONE',  ( -29.68315524077005207, 13.12249633091091816, -39.60535821593474282 ) ) ;
#60719=CARTESIAN_POINT ( 'NONE',  ( 9.781676926622875357, 53.39490368674695731, -3.092698992276897041 ) ) ;
#60720=B_SPLINE_CURVE_WITH_KNOTS ( 'NONE', 3,
 ( #6752, #8341, #89807, #98415, #15906, #216, #97346, #88743, #65528, #81678, #66051, #97884, #48785, #90328, #49320, #7800, #106500, #6208, #24567, #80105, #24039, #98928 ),
 .UNSPECIFIED., .F., .F.,
 ( 4, 2, 2, 2, 2, 2, 2, 2, 2, 2, 4 ),
 ( 0.003271557979369705584, 0.003775597685872196171, 0.004279637392374686759, 0.004783677098877177347, 0.005287716805379667068, 0.005791756511882157656, 0.006043776365133403383, 0.006295796218384648243, 0.006547816071635893104, 0.006799835924887137964, 0.007303875631389625950 ),
 .UNSPECIFIED. ) ;
#60731=CARTESIAN_POINT ( 'NONE',  ( 0.000000000000000000, 27.68727484027578356, 0.000000000000000000 ) ) ;
#60734=DIRECTION ( 'NONE',  ( -0.000000000000000000, 1.000000000000000000, -0.000000000000000000 ) ) ;
#60750=UNCERTAINTY_MEASURE_WITH_UNIT (LENGTH_MEASURE( 1.000000000000000082E-05 ), #102334, 'distance_accuracy_value', 'NONE');
#60752=CYLINDRICAL_SURFACE ( 'NONE', #54314, 1.250000000000001110 ) ;
#60760=CARTESIAN_POINT ( 'NONE',  ( -15.55441737893091947, 37.11602535008573511, -22.68899775139453823 ) ) ;
#60775=CARTESIAN_POINT ( 'NONE',  ( -17.71948856052742016, 43.32302192893173043, -4.750715123135393902 ) ) ;
#60788=VERTEX_POINT ( 'NONE', #17208 ) ;
#60789=CARTESIAN_POINT ( 'NONE',  ( 28.88699125077532059, 13.70431814614561539, -39.88880000601603371 ) ) ;
#60794=( NAMED_UNIT ( * ) PLANE_ANGLE_UNIT ( ) SI_UNIT ( $, .RADIAN. ) );
#60807=CARTESIAN_POINT ( 'NONE',  ( 16.58687548431174363, 34.28952745851042749, -24.30698433968624883 ) ) ;
#60830=CARTESIAN_POINT ( 'NONE',  ( -0.3376690634117764933, 27.30884096673758776, 40.71517686674960856 ) ) ;
#60850=ORIENTED_EDGE ( 'NONE', *, *, #48109, .F. ) ;
#60864=CARTESIAN_POINT ( 'NONE',  ( -8.238951567618261862, 51.66657054343616551, 3.999790829972674544 ) ) ;
#60868=LINE ( 'NONE', #69485, #78012 ) ;
#60870=DIRECTION ( 'NONE',  ( 0.000000000000000000, 1.000000000000000000, 0.000000000000000000 ) ) ;
#60883=CARTESIAN_POINT ( 'NONE',  ( -1.249887675601815129, 36.80302773944718098, 28.34105814077533481 ) ) ;
#60893=ORIENTED_EDGE ( 'NONE', *, *, #87761, .F. ) ;
#60916=CARTESIAN_POINT ( 'NONE',  ( 3.337161262018383995E-15, 37.21016666119768246, 27.25000000000000000 ) ) ;
#60921=ORIENTED_EDGE ( 'NONE', *, *, #91080, .F. ) ;
#60959=CARTESIAN_POINT ( 'NONE',  ( 27.86763638067955640, 36.37524770582945877, 9.811230206501790008 ) ) ;
#60972=SURFACE_STYLE_FILL_AREA ( #100870 ) ;
#60979=CARTESIAN_POINT ( 'NONE',  ( 10.28624191511809371, -1.200000000000000030E-05, -14.15779740156171584 ) ) ;
#60995=CARTESIAN_POINT ( 'NONE',  ( 37.56673239365870387, -1.200000000000000030E-05, 12.20617127780998956 ) ) ;
#61007=CARTESIAN_POINT ( 'NONE',  ( 37.24617447230036049, 25.58981836295230750, -13.42464766883425931 ) ) ;
#61016=CARTESIAN_POINT ( 'NONE',  ( -15.56661972382054948, 46.04807679453923441, -6.063442319127702262 ) ) ;
#61025=CARTESIAN_POINT ( 'NONE',  ( -28.08712643177169355, 36.49724380641310262, 8.016830452732861545 ) ) ;
#61059=CARTESIAN_POINT ( 'NONE',  ( -29.59409995734550236, 13.24979100942360688, -39.60535821593476413 ) ) ;
#61060=CARTESIAN_POINT ( 'NONE',  ( 17.62488890706315914, 43.36868375057044744, 4.616903831776418166 ) ) ;
#61067=CARTESIAN_POINT ( 'NONE',  ( 0.000000000000000000, 23.58303312036771615, 0.000000000000000000 ) ) ;
#61068=DIRECTION ( 'NONE',  ( 0.000000000000000000, 1.000000000000000000, -0.000000000000000000 ) ) ;
#61089=CARTESIAN_POINT ( 'NONE',  ( -16.75187969033532553, 37.11970326878314808, 21.80698433968612093 ) ) ;
#61090=UNCERTAINTY_MEASURE_WITH_UNIT (LENGTH_MEASURE( 1.000000000000000082E-05 ), #24212, 'distance_accuracy_value', 'NONE');
#61096=SURFACE_SIDE_STYLE ('',( #60576 ) ) ;
#61099=CARTESIAN_POINT ( 'NONE',  ( -9.658640570150691218, 45.55801956750498505, -15.25085205539905076 ) ) ;
#61119=CARTESIAN_POINT ( 'NONE',  ( -1.220180779666396820, 27.63012542767911839, -39.81491781757780757 ) ) ;
#61121=CARTESIAN_POINT ( 'NONE',  ( 10.28624191511809371, -1.200000000000000030E-05, -12.90779740156171407 ) ) ;
#61126=CARTESIAN_POINT ( 'NONE',  ( -8.559508646656389885, 53.96349637827586321, -1.531152949374502859 ) ) ;
#61130=SURFACE_SIDE_STYLE ('',( #34755 ) ) ;
#61156=CARTESIAN_POINT ( 'NONE',  ( -10.28624191511829977, 46.12099395432375104, -12.90779740156156841 ) ) ;
#61161=FACE_BOUND ( 'NONE', #4858, .T. ) ;
#61167=( LENGTH_UNIT ( ) NAMED_UNIT ( * ) SI_UNIT ( .MILLI., .METRE. ) );
#61179=FILL_AREA_STYLE ('',( #102151 ) ) ;
#61196=CARTESIAN_POINT ( 'NONE',  ( -36.80389671760433146, 25.99784339350267004, 11.20190813230474802 ) ) ;
#61210=MECHANICAL_DESIGN_GEOMETRIC_PRESENTATION_REPRESENTATION('',(#2587),#28504);
#61212=FACE_OUTER_BOUND ( 'NONE', #39145, .T. ) ;
#61233=ORIENTED_EDGE ( 'NONE', *, *, #24029, .F. ) ;
#61238=CARTESIAN_POINT ( 'NONE',  ( -30.64306277920947963, 7.829637822906565958, -41.65859565436478107 ) ) ;
#61244=CARTESIAN_POINT ( 'NONE',  ( 9.502088046852136927, 53.42926094969260475, -3.606443582442682150 ) ) ;
#61255=CARTESIAN_POINT ( 'NONE',  ( 4.271854802331145784, 54.28677085485544040, -6.536858402226804365 ) ) ;
#61272=UNCERTAINTY_MEASURE_WITH_UNIT (LENGTH_MEASURE( 1.000000000000000082E-05 ), #14401, 'distance_accuracy_value', 'NONE');
#61279=EDGE_LOOP ( 'NONE', ( #41728, #95567 ) ) ;
#61316=VECTOR ( 'NONE', #39634, 1000.000000000000000 ) ;
#61338=FACE_OUTER_BOUND ( 'NONE', #43061, .T. ) ;
#61343=EDGE_CURVE ( 'NONE', #96186, #74990, #38855, .T. ) ;
#61346=CARTESIAN_POINT ( 'NONE',  ( 9.327072865849737937, 44.07210225711265394, 13.35182660753846129 ) ) ;
#61348=DIRECTION ( 'NONE',  ( 0.000000000000000000, 0.000000000000000000, 1.000000000000000000 ) ) ;
#61360=( NAMED_UNIT ( * ) SI_UNIT ( $, .STERADIAN. ) SOLID_ANGLE_UNIT ( ) );
#61362=CARTESIAN_POINT ( 'NONE',  ( -0.3379557265678910793, 28.19330765266871452, 38.28504178355841248 ) ) ;
#61363=CARTESIAN_POINT ( 'NONE',  ( 1.250111974717941443, 36.68751764429408979, -28.65871480211785993 ) ) ;
#61372=CYLINDRICAL_SURFACE ( 'NONE', #36082, 1.250000000000000222 ) ;
#61378=DIRECTION ( 'NONE',  ( -0.000000000000000000, 1.000000000000000000, 0.000000000000000000 ) ) ;
#61421=ORIENTED_EDGE ( 'NONE', *, *, #102133, .T. ) ;
#61437=CARTESIAN_POINT ( 'NONE',  ( -24.47194732006304108, 25.31483624829911960, -32.07842946029033016 ) ) ;
#61447=CARTESIAN_POINT ( 'NONE',  ( -5.290067270632282437, 54.20842449845790867, 6.031152949371105798 ) ) ;
#61454=AXIS2_PLACEMENT_3D ( 'NONE', #3987, #78923, #71355 ) ;
#61481=DIRECTION ( 'NONE',  ( 0.000000000000000000, 0.000000000000000000, 1.000000000000000000 ) ) ;
#61506=VECTOR ( 'NONE', #68645, 1000.000000000000000 ) ;
#61540=CARTESIAN_POINT ( 'NONE',  ( -6.399272939559234707, 51.30530844324656670, 7.881311681917864576 ) ) ;
#61541=ORIENTED_EDGE ( 'NONE', *, *, #30556, .T. ) ;
#61551=CARTESIAN_POINT ( 'NONE',  ( -9.960428250040571641, 43.33465522821285987, -15.36733472782074550 ) ) ;
#61557=CARTESIAN_POINT ( 'NONE',  ( -0.6447495452450531239, 46.14900100259577442, 16.41618316663220511 ) ) ;
#61560=VERTEX_POINT ( 'NONE', #32488 ) ;
#61563=CARTESIAN_POINT ( 'NONE',  ( -48.02835407290533709, 11.61227450977237119, -14.35535821593460248 ) ) ;
#61568=DIRECTION ( 'NONE',  ( 1.150791560227848544E-16, -0.3420201433256727652, 0.9396926207859068736 ) ) ;
#61586=B_SPLINE_CURVE_WITH_KNOTS ( 'NONE', 3,
 ( #97067, #63123, #31315, #88986, #64198, #23213, #22149, #4888, #54458, #13485, #56051, #88465, #15085, #55000, #53946, #87410, #96555, #5925, #38853, #14539, #104631, #30780 ),
 .UNSPECIFIED., .F., .F.,
 ( 4, 2, 2, 2, 2, 2, 2, 2, 2, 2, 4 ),
 ( 0.006473714219450311426, 0.006725523206561636463, 0.006977332193672962368, 0.007480950167895608974, 0.007984568142118255579, 0.008488186116340902185, 0.009495422064786186722, 0.009747231051897509158, 0.009999040039008831593, 0.01025084902612015403, 0.01050265801323147646 ),
 .UNSPECIFIED. ) ;
#61596=CARTESIAN_POINT ( 'NONE',  ( 17.83057459411148926, 34.57788205794057035, 22.40555159655071549 ) ) ;
#61598=CYLINDRICAL_SURFACE ( 'NONE', #57122, 1.250000000000000222 ) ;
#61600=CARTESIAN_POINT ( 'NONE',  ( 1.248765323091368673, 16.16828180304352358, 50.36968963469745830 ) ) ;
#61615=STYLED_ITEM ( 'NONE', ( #1345 ), #58526 ) ;
#61632=CARTESIAN_POINT ( 'NONE',  ( -27.26583764555563150, 34.42251079669566138, 10.05698433968616357 ) ) ;
#61636=CARTESIAN_POINT ( 'NONE',  ( -17.53682258900660074, 36.29665952923689076, 24.04445569364172286 ) ) ;
#61640=CARTESIAN_POINT ( 'NONE',  ( 6.274480239423446903, 53.84149731873487355, -6.494774485913110240 ) ) ;
#61641=CARTESIAN_POINT ( 'NONE',  ( 17.08002596387369110, 34.90866943516432030, -21.84018144932510808 ) ) ;
#61648=CARTESIAN_POINT ( 'NONE',  ( -9.034470188793504164, 46.02977034662631439, -14.11149907944951920 ) ) ;
#61650=PRESENTATION_STYLE_ASSIGNMENT (( #28771 ) ) ;
#61680=CARTESIAN_POINT ( 'NONE',  ( 0.000000000000000000, 38.67090180175566871, 0.000000000000000000 ) ) ;
#61707=SURFACE_STYLE_FILL_AREA ( #93525 ) ;
#61711=EDGE_CURVE ( 'NONE', #16669, #27639, #24804, .T. ) ;
#61714=EDGE_LOOP ( 'NONE', ( #81560, #96443, #85500, #11925, #15020, #37668, #49684 ) ) ;
#61723=CARTESIAN_POINT ( 'NONE',  ( 9.267538580112169910, 46.19448214903180627, -13.41394971794144020 ) ) ;
#61746=CARTESIAN_POINT ( 'NONE',  ( 5.126327086984646897, 52.11936742043627646, 6.031152949374359196 ) ) ;
#61759=CARTESIAN_POINT ( 'NONE',  ( -26.34368984043107531, 37.12851728967876852, -7.801921120626483130 ) ) ;
#61810=CARTESIAN_POINT ( 'NONE',  ( -16.96051095573446332, 45.50173602991597477, -6.619600894237387401 ) ) ;
#61813=CARTESIAN_POINT ( 'NONE',  ( 10.28624191511840458, -1.200000000000000030E-05, 14.15779740156149025 ) ) ;
#61824=CARTESIAN_POINT ( 'NONE',  ( -0.1687275065231993998, 52.17923068443690937, -7.749999999999973355 ) ) ;
#61837=ORIENTED_EDGE ( 'NONE', *, *, #91279, .F. ) ;
#61844=EDGE_CURVE ( 'NONE', #14520, #27731, #48932, .T. ) ;
#61859=LINE ( 'NONE', #5197, #64413 ) ;
#61860=CARTESIAN_POINT ( 'NONE',  ( -9.804047713996713043, 51.27631422876505951, 2.925016539151283013 ) ) ;
#61881=CARTESIAN_POINT ( 'NONE',  ( 16.75187969033515145, 34.99134772383131775, -21.80698433968624528 ) ) ;
#61904=EDGE_CURVE ( 'NONE', #65856, #85904, #9015, .T. ) ;
#61910=EDGE_CURVE ( 'NONE', #59854, #73607, #57917, .T. ) ;
#61925=EDGE_LOOP ( 'NONE', ( #83107, #54595, #52595, #101616 ) ) ;
#61930=SURFACE_STYLE_FILL_AREA ( #55896 ) ;
#61934=FACE_BOUND ( 'NONE', #55767, .T. ) ;
#61945=CARTESIAN_POINT ( 'NONE',  ( 17.08493112194837238, 36.32471929476455585, 24.27338705487281700 ) ) ;
#61956=CARTESIAN_POINT ( 'NONE',  ( -0.6416578798349835688, 36.36110222310433215, 29.57590615574903836 ) ) ;
#61985=CARTESIAN_POINT ( 'NONE',  ( 15.97269242673970702, 37.21081289561244176, -22.07591361862218449 ) ) ;
#61986=CARTESIAN_POINT ( 'NONE',  ( -25.89112870477232065, 37.21026264049879018, 8.497328228240501602 ) ) ;
#62000=CARTESIAN_POINT ( 'NONE',  ( -38.76877242246048638, 27.37289375180844431, 11.85340545765227382 ) ) ;
#62012=CONICAL_SURFACE ( 'NONE', #12002, 34.51297463494397988, 1.221730476396026610 ) ;
#62015=CARTESIAN_POINT ( 'NONE',  ( -16.02654702170687528, 43.95888759761753306, -4.317547509937734951 ) ) ;
#62053=ADVANCED_FACE ( 'NONE', ( #32503 ), #57793, .F. ) ;
#62066=SURFACE_STYLE_USAGE ( .BOTH. , #87386 ) ;
#62076=CARTESIAN_POINT ( 'NONE',  ( -30.25727950662331978, 17.21737621059155643, -39.73669541984511966 ) ) ;
#62087=UNCERTAINTY_MEASURE_WITH_UNIT (LENGTH_MEASURE( 1.000000000000000082E-05 ), #66155, 'distance_accuracy_value', 'NONE');
#62089=VECTOR ( 'NONE', #6456, 1000.000000000000000 ) ;
#62104=CYLINDRICAL_SURFACE ( 'NONE', #55209, 1.250000000000001110 ) ;
#62108=VECTOR ( 'NONE', #4650, 1000.000000000000000 ) ;
#62121=SURFACE_STYLE_USAGE ( .BOTH. , #37855 ) ;
#62134=CARTESIAN_POINT ( 'NONE',  ( -47.36344235967359850, 18.16811379743644395, 14.54383657267810825 ) ) ;
#62158=VERTEX_POINT ( 'NONE', #28143 ) ;
#62172=CARTESIAN_POINT ( 'NONE',  ( 17.76463732149834129, 34.19216742441107471, -23.79440628143193592 ) ) ;
#62218=LINE ( 'NONE', #2474, #101710 ) ;
#62270=CARTESIAN_POINT ( 'NONE',  ( 49.13304414347678772, 12.95525746345893481, -16.19504546972810033 ) ) ;
#62275=CARTESIAN_POINT ( 'NONE',  ( 4.044781357444436232, 51.90680650645019512, 7.474578379459966726 ) ) ;
#62277=CARTESIAN_POINT ( 'NONE',  ( 38.74267013308406860, 27.39035684269769888, 11.77443177698138221 ) ) ;
#62285=CARTESIAN_POINT ( 'NONE',  ( -26.01163681415079765, 37.20415886906720715, -8.178344558965836342 ) ) ;
#62313=ORIENTED_EDGE ( 'NONE', *, *, #72729, .T. ) ;
#62350=B_SPLINE_CURVE_WITH_KNOTS ( 'NONE', 3,
 ( #39915, #994, #49041, #40434, #81938, #99735, #32903, #57661, #91656, #462, #50117, #82492, #33431, #65245, #64717, #89530, #33973, #73313, #99185, #23757, #25348, #48513 ),
 .UNSPECIFIED., .F., .F.,
 ( 4, 2, 2, 2, 2, 2, 2, 2, 2, 2, 4 ),
 ( 0.003600184084728503923, 0.004103037208643595807, 0.004605890332558686823, 0.004857316894516234065, 0.005108743456473779573, 0.005611596580388875793, 0.005863023142346423904, 0.006114449704303972014, 0.006617302828219070836, 0.007120155952134168791, 0.007623009076049266745 ),
 .UNSPECIFIED. ) ;
#62351=EDGE_CURVE ( 'NONE', #55752, #86888, #33489, .T. ) ;
#62353=CARTESIAN_POINT ( 'NONE',  ( 21.97248774489993295, 25.82615788719429872, -32.15153141218966226 ) ) ;
#62400=( GEOMETRIC_REPRESENTATION_CONTEXT ( 3 ) GLOBAL_UNCERTAINTY_ASSIGNED_CONTEXT ( ( #82921 ) ) GLOBAL_UNIT_ASSIGNED_CONTEXT ( ( #8237, #17415, #58389 ) ) REPRESENTATION_CONTEXT ( 'NONE', 'WORKASPACE' ) );
#62405=CARTESIAN_POINT ( 'NONE',  ( 10.28624191511840458, 43.99263840937192782, 12.90779740156148847 ) ) ;
#62422=EDGE_LOOP ( 'NONE', ( #57746, #106246, #2854, #35405 ) ) ;
#62458=CARTESIAN_POINT ( 'NONE',  ( 0.9493808841748633265, 12.66946710488672068, -49.67524744289797667 ) ) ;
#62460=SURFACE_SIDE_STYLE ('',( #30639 ) ) ;
#62473=B_SPLINE_CURVE_WITH_KNOTS ( 'NONE', 3,
 ( #79474, #88111, #79997, #14191, #5584, #38509, #30418, #39032, #71914, #22865, #39570, #82116, #2254, #34682, #110, #83711, #9818, #41147, #9287, #49758 ),
 .UNSPECIFIED., .F., .F.,
 ( 4, 2, 2, 2, 2, 2, 2, 2, 2, 4 ),
 ( 0.007119059105098823372, 0.007623191790411408715, 0.008127324475723994926, 0.008379390818380284128, 0.008631457161036575065, 0.009135589846349155205, 0.009639722531661735344, 0.01014385521697431722, 0.01064798790228689736, 0.01115212058759947750 ),
 .UNSPECIFIED. ) ;
#62480=LINE ( 'NONE', #13364, #85815 ) ;
#62500=COLOUR_RGB ( '', 0.66274510, 0.83137255, 0.94901961) ;
#62516=CARTESIAN_POINT ( 'NONE',  ( -38.81495481606859244, 27.33043566563091176, 12.09930584269103804 ) ) ;
#62517=ORIENTED_EDGE ( 'NONE', *, *, #42692, .F. ) ;
#62528=CARTESIAN_POINT ( 'NONE',  ( 3.616665348617805752E-21, 26.07813853931757464, -38.25000000000000000 ) ) ;
#62531=CARTESIAN_POINT ( 'NONE',  ( -15.43026448159015729, 44.08566165821367377, -5.095151619626889783 ) ) ;
#62539=MECHANICAL_DESIGN_GEOMETRIC_PRESENTATION_REPRESENTATION('',(#45297),#40122);
#62562=ORIENTED_EDGE ( 'NONE', *, *, #34970, .F. ) ;
#62565=CARTESIAN_POINT ( 'NONE',  ( -1.411247199636991373E-12, 7.746009256445978153, -51.75000000000450484 ) ) ;
#62583=ORIENTED_EDGE ( 'NONE', *, *, #40677, .T. ) ;
#62588=CARTESIAN_POINT ( 'NONE',  ( -1.012490096689796948, 51.43211407868803775, 9.751042324627787750 ) ) ;
#62622=CYLINDRICAL_SURFACE ( 'NONE', #78512, 1.250000000000001110 ) ;
#62638=B_SPLINE_CURVE_WITH_KNOTS ( 'NONE', 3,
 ( #120, #26604, #1184, #643, #98834, #66482, #89710, #24479, #24991, #57314, #17953, #57844, #67565, #34155, #25541, #83199, #58400, #48690, #8242, #33090 ),
 .UNSPECIFIED., .F., .F.,
 ( 4, 2, 2, 2, 2, 2, 2, 2, 2, 4 ),
 ( 0.003302071085094845405, 0.003806141473758820667, 0.004058176668090805045, 0.004310211862422788989, 0.005318352639750726502, 0.005822423028414703064, 0.006074458222746694815, 0.006326493417078686565, 0.006830563805742671801, 0.007334634194406657905 ),
 .UNSPECIFIED. ) ;
#62651=SURFACE_SIDE_STYLE ('',( #102571 ) ) ;
#62659=( GEOMETRIC_REPRESENTATION_CONTEXT ( 3 ) GLOBAL_UNCERTAINTY_ASSIGNED_CONTEXT ( ( #1718 ) ) GLOBAL_UNIT_ASSIGNED_CONTEXT ( ( #26069, #58380, #8230 ) ) REPRESENTATION_CONTEXT ( 'NONE', 'WORKASPACE' ) );
#62681=CARTESIAN_POINT ( 'NONE',  ( -17.39534200550415122, 36.29816465214055654, 24.14189926133820308 ) ) ;
#62687=CARTESIAN_POINT ( 'NONE',  ( 18.00625151213652586, 34.31693948171063369, -23.17957379143527419 ) ) ;
#62699=DIRECTION ( 'NONE',  ( 0.000000000000000000, 1.000000000000000000, 0.000000000000000000 ) ) ;
#62729=MECHANICAL_DESIGN_GEOMETRIC_PRESENTATION_REPRESENTATION('',(#52387),#17924);
#62730=ORIENTED_EDGE ( 'NONE', *, *, #79054, .F. ) ;
#62731=CARTESIAN_POINT ( 'NONE',  ( -8.875886419521037851, 53.84819952152465561, -1.561592776398766258 ) ) ;
#62735=ORIENTED_EDGE ( 'NONE', *, *, #100383, .T. ) ;
#62744=CARTESIAN_POINT ( 'NONE',  ( -49.22356967707574427, 12.91018829711988225, -15.97913688296349832 ) ) ;
#62748=B_SPLINE_CURVE_WITH_KNOTS ( 'NONE', 3,
 ( #25477, #34101, #99852, #26026, #1676, #34635, #28666, #21113, #53440, #12953, #37285, #5415, #96023, #44286, #93900, #11357, #22148, #95481, #61551, #45358, #13483, #45873 ),
 .UNSPECIFIED., .F., .F.,
 ( 4, 2, 2, 2, 2, 2, 2, 2, 2, 2, 4 ),
 ( 0.003044036087729489436, 0.003548461684534129183, 0.003800674482936449924, 0.004052887281338770666, 0.004557312878143412148, 0.005061738474948054498, 0.005566164071752695980, 0.006070589668557337462, 0.006575015265361978944, 0.006827228063764296216, 0.007079440862166612621 ),
 .UNSPECIFIED. ) ;
#62756=EDGE_CURVE ( 'NONE', #44079, #106075, #29697, .T. ) ;
#62757=FACE_OUTER_BOUND ( 'NONE', #32051, .T. ) ;
#62759=LINE ( 'NONE', #85989, #88430 ) ;
#62767=ORIENTED_EDGE ( 'NONE', *, *, #58436, .T. ) ;
#62774=CYLINDRICAL_SURFACE ( 'NONE', #97044, 1.250000000000001110 ) ;
#62777=EDGE_CURVE ( 'NONE', #67401, #54018, #30114, .T. ) ;
#62788=CARTESIAN_POINT ( 'NONE',  ( -36.62603724863704713, 26.04072037792466787, 11.37877576920930167 ) ) ;
#62805=VERTEX_POINT ( 'NONE', #22311 ) ;
#62806=DIRECTION ( 'NONE',  ( 0.000000000000000000, 0.000000000000000000, 1.000000000000000000 ) ) ;
#62809=ADVANCED_FACE ( 'NONE', ( #64346, #81025, #79446, #7142, #79968 ), #28439, .T. ) ;
#62849=VERTEX_POINT ( 'NONE', #89675 ) ;
#62852=CARTESIAN_POINT ( 'NONE',  ( -15.67047892703677192, 36.78599904984204017, 23.70382416292481409 ) ) ;
#62860=CARTESIAN_POINT ( 'NONE',  ( 25.90320363122974001, 37.12824114503998629, 9.160210970361452709 ) ) ;
#62862=CARTESIAN_POINT ( 'NONE',  ( 17.89663725870117972, 43.18032939976320250, -5.550406259236770445 ) ) ;
#62867=CARTESIAN_POINT ( 'NONE',  ( 24.46403792248021603, 27.44444016472269610, -32.08006538382090156 ) ) ;
#62873=CARTESIAN_POINT ( 'NONE',  ( 1.637502573363885733E-19, 51.26930509877138320, -10.24999999999999822 ) ) ;
#62895=VERTEX_POINT ( 'NONE', #40054 ) ;
#62909=CARTESIAN_POINT ( 'NONE',  ( -8.559508646656370345, 51.83514083332403999, 1.531152949374564365 ) ) ;
#62928=CARTESIAN_POINT ( 'NONE',  ( 16.41907560254749399, 35.05515302546547218, -21.84033983347977070 ) ) ;
#62939=CARTESIAN_POINT ( 'NONE',  ( 0.000000000000000000, 24.35682532067546902, -46.94949242731048145 ) ) ;
#62949=ORIENTED_EDGE ( 'NONE', *, *, #89452, .T. ) ;
#62950=CARTESIAN_POINT ( 'NONE',  ( 26.16605992612153031, 35.04355381026522309, 7.977766528426338155 ) ) ;
#62955=CARTESIAN_POINT ( 'NONE',  ( -1.248908226501082908, 53.88132084694859003, -8.833326452425996678 ) ) ;
#62957=( LENGTH_UNIT ( ) NAMED_UNIT ( * ) SI_UNIT ( .MILLI., .METRE. ) );
#62966=ORIENTED_EDGE ( 'NONE', *, *, #92748, .T. ) ;
#62971=MECHANICAL_DESIGN_GEOMETRIC_PRESENTATION_REPRESENTATION('',(#87083),#100829);
#62992=CARTESIAN_POINT ( 'NONE',  ( -5.290067270632269114, -1.200000000000000030E-05, -7.281152949374520844 ) ) ;
#63003=DIRECTION ( 'NONE',  ( 0.000000000000000000, 1.000000000000000000, -0.000000000000000000 ) ) ;
#63022=FACE_OUTER_BOUND ( 'NONE', #30876, .T. ) ;
#63028=CARTESIAN_POINT ( 'NONE',  ( -26.35516898678989151, 36.89168544900753943, 9.819666744838436045 ) ) ;
#63029=ORIENTED_EDGE ( 'NONE', *, *, #35342, .T. ) ;
#63039=CARTESIAN_POINT ( 'NONE',  ( -48.98802391561670078, 7.953645742798949314, 16.40821160912093291 ) ) ;
#63047=ADVANCED_FACE ( 'NONE', ( #41118 ), #57275, .F. ) ;
#63053=CARTESIAN_POINT ( 'NONE',  ( -7.665950860465550857E-14, -1.200000000000000030E-05, -40.75000000000000000 ) ) ;
#63075=CARTESIAN_POINT ( 'NONE',  ( 0.000000000000000000, 47.77514352166374323, 0.000000000000000000 ) ) ;
#63123=CARTESIAN_POINT ( 'NONE',  ( -0.08420089935654326285, 35.08181111624585213, 27.25000000000000355 ) ) ;
#63141=CARTESIAN_POINT ( 'NONE',  ( 10.83537542021312383, 43.83140336798144432, 13.03201732437568161 ) ) ;
#63143=DIRECTION ( 'NONE',  ( -0.000000000000000000, 1.000000000000000000, -0.000000000000000000 ) ) ;
#63162=( NAMED_UNIT ( * ) SI_UNIT ( $, .STERADIAN. ) SOLID_ANGLE_UNIT ( ) );
#63173=CARTESIAN_POINT ( 'NONE',  ( 36.47172676003749103, 28.20078810612359987, 11.58029744488031554 ) ) ;
#63196=ORIENTED_EDGE ( 'NONE', *, *, #3930, .F. ) ;
#63205=STYLED_ITEM ( 'NONE', ( #27566 ), #25527 ) ;
#63206=VECTOR ( 'NONE', #46625, 1000.000000000000000 ) ;
#63218=CARTESIAN_POINT ( 'NONE',  ( 16.91683273982978619, 34.22137765266874965, -24.30698433968624883 ) ) ;
#63226=FILL_AREA_STYLE_COLOUR ( '', #105923 ) ;
#63234=EDGE_CURVE ( 'NONE', #21252, #33697, #65689, .T. ) ;
#63243=CARTESIAN_POINT ( 'NONE',  ( 29.68315524077034340, 13.12249633091093415, 39.60535821593451544 ) ) ;
#63244=ORIENTED_EDGE ( 'NONE', *, *, #20294, .T. ) ;
#63246=CARTESIAN_POINT ( 'NONE',  ( -11.30587238908023195, 45.32085087904604848, 14.90049756856780228 ) ) ;
#63273=CARTESIAN_POINT ( 'NONE',  ( 16.66870162890474205, 37.13814613750710691, 21.80698433968582961 ) ) ;
#63274=CARTESIAN_POINT ( 'NONE',  ( 1.124716868846474149, 43.84887597193111475, -16.86397666530443473 ) ) ;
#63277=COLOUR_RGB ( '', 0.66274510, 0.83137255, 0.94901961) ;
#63298=ADVANCED_FACE ( 'NONE', ( #47471 ), #62622, .F. ) ;
#63322=SURFACE_STYLE_USAGE ( .BOTH. , #30970 ) ;
#63327=CARTESIAN_POINT ( 'NONE',  ( -1.152188841818234133E-13, -1.200000000000000030E-05, -50.50000000000000000 ) ) ;
#63336=CARTESIAN_POINT ( 'NONE',  ( 10.61508837294732999, 43.20235039013163458, 15.36662796280145038 ) ) ;
#63361=LINE ( 'NONE', #97286, #45672 ) ;
#63391=CARTESIAN_POINT ( 'NONE',  ( -16.75187969033459012, 36.38380281757147827, 24.30698433969199357 ) ) ;
#63398=CARTESIAN_POINT ( 'NONE',  ( 0.1683342203993841713, 34.17188553058033307, 29.75000000000001066 ) ) ;
#63399=CARTESIAN_POINT ( 'NONE',  ( 26.01020368950299400, 37.20437420822879204, 8.180924129841026016 ) ) ;
#63400=CARTESIAN_POINT ( 'NONE',  ( -48.02835407290534420, 14.94086294439724227, -16.85535821593460426 ) ) ;
#63401=CARTESIAN_POINT ( 'NONE',  ( -24.32789867356884628, 27.33682607920834684, -32.55354264101782036 ) ) ;
#63406=CARTESIAN_POINT ( 'NONE',  ( -24.46934747735757298, 25.33804889760450862, 32.00006138626095975 ) ) ;
#63411=CARTESIAN_POINT ( 'NONE',  ( 0.08445723013546542479, 52.17923068443687384, 7.750000000000003553 ) ) ;
#63414=CARTESIAN_POINT ( 'NONE',  ( -0.7862562837408798577, 51.35452495058204647, -9.985734753308584288 ) ) ;
#63416=CARTESIAN_POINT ( 'NONE',  ( 0.3590100610935850756, 18.74889334034432764, -49.30114299272825917 ) ) ;
#63425=VERTEX_POINT ( 'NONE', #52792 ) ;
#63430=PRESENTATION_STYLE_ASSIGNMENT (( #40181 ) ) ;
#63445=ORIENTED_EDGE ( 'NONE', *, *, #43111, .F. ) ;
#63452=CARTESIAN_POINT ( 'NONE',  ( 47.90217879170857884, 15.22462055664289338, 16.85535821593427031 ) ) ;
#63472=CARTESIAN_POINT ( 'NONE',  ( -0.9558972795473693607, 25.32440591748497738, -40.30957252762832610 ) ) ;
#63515=DIRECTION ( 'NONE',  ( -0.000000000000000000, 1.000000000000000000, -0.000000000000000000 ) ) ;
#63524=EDGE_LOOP ( 'NONE', ( #25612, #77761 ) ) ;
#63525=CARTESIAN_POINT ( 'NONE',  ( 0.9522645442514227065, 8.765251389120953363, -51.31355066132082499 ) ) ;
#63527=SURFACE_STYLE_USAGE ( .BOTH. , #62460 ) ;
#63539=CARTESIAN_POINT ( 'NONE',  ( -0.9549771330164267269, 36.45450309182552928, 29.31067408448910427 ) ) ;
#63543=ORIENTED_EDGE ( 'NONE', *, *, #74556, .T. ) ;
#63566=ADVANCED_FACE ( 'NONE', ( #63022 ), #6346, .F. ) ;
#63570=CARTESIAN_POINT ( 'NONE',  ( -25.86049976764029523, 37.20180571946941228, 8.663517206654082869 ) ) ;
#63581=ORIENTED_EDGE ( 'NONE', *, *, #77742, .F. ) ;
#63583=CARTESIAN_POINT ( 'NONE',  ( -38.81963395482446089, 27.30149883538651778, 12.34989123519421206 ) ) ;
#63590=CARTESIAN_POINT ( 'NONE',  ( -30.87917441950785857, 8.312254468506221627, 41.23121050640273921 ) ) ;
#63591=CARTESIAN_POINT ( 'NONE',  ( 28.53023071193278426, 11.34323491540342488, 41.35403323942976783 ) ) ;
#63602=CARTESIAN_POINT ( 'NONE',  ( -27.72596789763197478, 36.41250443191194819, -9.903931038345092475 ) ) ;
#63608=EDGE_CURVE ( 'NONE', #58522, #90581, #6444, .T. ) ;
#63619=ORIENTED_EDGE ( 'NONE', *, *, #88138, .T. ) ;
#63626=CARTESIAN_POINT ( 'NONE',  ( -7.940862310547813330, 54.17408618097004336, -1.683098319245891039 ) ) ;
#63628=FACE_OUTER_BOUND ( 'NONE', #54530, .T. ) ;
#63665=CARTESIAN_POINT ( 'NONE',  ( 4.038456955263700188, 51.98520879605556644, -7.231977661697025717 ) ) ;
#63672=CARTESIAN_POINT ( 'NONE',  ( -0.07745360819684599107, 7.746009256456465764, 51.75000000000001421 ) ) ;
#63690=CARTESIAN_POINT ( 'NONE',  ( -15.53255836610350116, 34.96781356575814215, 22.77000419570328305 ) ) ;
#63703=PRESENTATION_STYLE_ASSIGNMENT (( #62121 ) ) ;
#63707=DIRECTION ( 'NONE',  ( -0.000000000000000000, 1.000000000000000000, 0.000000000000000000 ) ) ;
#63709=EDGE_LOOP ( 'NONE', ( #92639, #8597, #78097, #75826, #70201, #33410, #19897, #59804 ) ) ;
#63721=ORIENTED_EDGE ( 'NONE', *, *, #38775, .T. ) ;
#63725=CARTESIAN_POINT ( 'NONE',  ( 1.250782632067709566, 25.50131467620691694, 39.81516996845464007 ) ) ;
#63749=CARTESIAN_POINT ( 'NONE',  ( 6.488675057781621902, 53.47862480557490983, -7.645533103099348082 ) ) ;
#63759=DIRECTION ( 'NONE',  ( -0.000000000000000000, 1.000000000000000000, -0.000000000000000000 ) ) ;
#63769=ORIENTED_EDGE ( 'NONE', *, *, #7455, .T. ) ;
#63778=CARTESIAN_POINT ( 'NONE',  ( -10.61273427954654736, 46.03711080233982500, 12.94042145964155210 ) ) ;
#63815=DIRECTION ( 'NONE',  ( 0.000000000000000000, 0.000000000000000000, -1.000000000000000000 ) ) ;
#63819=EDGE_LOOP ( 'NONE', ( #26700, #103489, #64893, #30941 ) ) ;
#63837=CARTESIAN_POINT ( 'NONE',  ( -1.115893604525096228, 14.48218051350517754, -51.08048210849830184 ) ) ;
#63846=CARTESIAN_POINT ( 'NONE',  ( -23.21751746555247919, 25.98869614573810694, 30.70617127781050471 ) ) ;
#63850=CARTESIAN_POINT ( 'NONE',  ( 48.48308721883813632, 13.98293033111261785, -16.77185627386677425 ) ) ;
#63857=FACE_OUTER_BOUND ( 'NONE', #5025, .T. ) ;
#63865=EDGE_CURVE ( 'NONE', #13191, #34768, #23301, .T. ) ;
#63877=VECTOR ( 'NONE', #63707, 1000.000000000000000 ) ;
#63880=CARTESIAN_POINT ( 'NONE',  ( -6.400037421424863204, 53.43404507722560481, 7.879308159338338946 ) ) ;
#63888=VERTEX_POINT ( 'NONE', #22468 ) ;
#63914=CARTESIAN_POINT ( 'NONE',  ( -22.88430703375227893, 26.05182353366611281, 30.73977527160241507 ) ) ;
#63921=CARTESIAN_POINT ( 'NONE',  ( 1.218458762081870761, 34.73422897157483646, 28.17869402526995160 ) ) ;
#63922=CARTESIAN_POINT ( 'NONE',  ( 26.48484422076975164, 37.08860641375430589, 7.709683435484037339 ) ) ;
#63923=SURFACE_STYLE_USAGE ( .BOTH. , #104905 ) ;
#63930=CARTESIAN_POINT ( 'NONE',  ( 24.00241574749180273, 27.29294457708169830, -32.94367910540196931 ) ) ;
#63935=CARTESIAN_POINT ( 'NONE',  ( -1.013018381689523073, 43.34736372649656033, -18.25026088174005423 ) ) ;
#63949=CARTESIAN_POINT ( 'NONE',  ( 47.90408546931266898, 11.89605000366072396, -14.35535821593550487 ) ) ;
#63961=DIRECTION ( 'NONE',  ( -0.000000000000000000, 1.000000000000000000, -0.000000000000000000 ) ) ;
#63996=EDGE_CURVE ( 'NONE', #29217, #63888, #16777, .T. ) ;
#64029=CARTESIAN_POINT ( 'NONE',  ( 5.290067270632161645, -1.200000000000000030E-05, -8.531152949374595451 ) ) ;
#64032=CARTESIAN_POINT ( 'NONE',  ( -0.1699152989463506569, 54.30758622938874680, -7.750000000000000888 ) ) ;
#64033=EDGE_LOOP ( 'NONE', ( #87515, #14908, #84899, #22915, #74015, #51665, #5298, #34542 ) ) ;
#64046=( LENGTH_UNIT ( ) NAMED_UNIT ( * ) SI_UNIT ( .MILLI., .METRE. ) );
#64059=CARTESIAN_POINT ( 'NONE',  ( -0.1698782441665641074, 34.17493339656093809, -29.74125536344337917 ) ) ;
#64062=CYLINDRICAL_SURFACE ( 'NONE', #30679, 1.250000000000001110 ) ;
#64064=CARTESIAN_POINT ( 'NONE',  ( 2.470381878726035567E-14, 18.87382441218300144, 49.24999999999992184 ) ) ;
#64067=DIRECTION ( 'NONE',  ( -0.000000000000000000, 1.000000000000000000, -0.000000000000000000 ) ) ;
#64070=ORIENTED_EDGE ( 'NONE', *, *, #101410, .T. ) ;
#64107=CARTESIAN_POINT ( 'NONE',  ( 7.382723172920433008, 54.19823143065442395, -3.210640374493870297 ) ) ;
#64108=ADVANCED_FACE ( 'NONE', ( #55976 ), #39837, .F. ) ;
#64116=CYLINDRICAL_SURFACE ( 'NONE', #26103, 1.250000000000001110 ) ;
#64131=CARTESIAN_POINT ( 'NONE',  ( 29.68315524077033629, 13.47185074185905584, 42.10535821593451544 ) ) ;
#64138=CARTESIAN_POINT ( 'NONE',  ( -28.19205650684127562, 36.30852143868257542, -9.429946862361873627 ) ) ;
#64154=CARTESIAN_POINT ( 'NONE',  ( -7.306728573036795460, 54.30193072519075059, -2.634352804278476512 ) ) ;
#64164=ADVANCED_FACE ( 'NONE', ( #51081 ), #101260, .F. ) ;
#64166=( NAMED_UNIT ( * ) PLANE_ANGLE_UNIT ( ) SI_UNIT ( $, .RADIAN. ) );
#64175=CARTESIAN_POINT ( 'NONE',  ( 0.9542819463626004417, 27.45207584973554304, -40.31149540464158321 ) ) ;
#64180=ORIENTED_EDGE ( 'NONE', *, *, #78245, .F. ) ;
#64184=CARTESIAN_POINT ( 'NONE',  ( -0.3382046435677298901, 52.16426612011243691, 7.785187884561949545 ) ) ;
#64197=CARTESIAN_POINT ( 'NONE',  ( 5.123541259261425118, 51.37833675238564268, -8.531152949374599004 ) ) ;
#64198=CARTESIAN_POINT ( 'NONE',  ( -0.4143444918978542724, 35.05607634723067889, 27.31767140698388729 ) ) ;
#64216=SURFACE_SIDE_STYLE ('',( #9526 ) ) ;
#64240=DIRECTION ( 'NONE',  ( 0.000000000000000000, 1.000000000000000000, 0.000000000000000000 ) ) ;
#64246=CARTESIAN_POINT ( 'NONE',  ( -29.49969761086808617, 8.554442461696824651, -42.10535821593507677 ) ) ;
#64254=CARTESIAN_POINT ( 'NONE',  ( -5.580966921651770022E-13, 25.16821295365027211, 40.75000000000505906 ) ) ;
#64259=( NAMED_UNIT ( * ) PLANE_ANGLE_UNIT ( ) SI_UNIT ( $, .RADIAN. ) );
#64261=CARTESIAN_POINT ( 'NONE',  ( 24.43710448268778990, 25.27504818406982778, 32.24217181898259099 ) ) ;
#64271=ORIENTED_EDGE ( 'NONE', *, *, #30652, .T. ) ;
#64288=DIRECTION ( 'NONE',  ( -0.000000000000000000, -1.000000000000000000, -0.000000000000000000 ) ) ;
#64308=CARTESIAN_POINT ( 'NONE',  ( 11.39656771499216070, 45.34267223356316379, -14.75529722941197619 ) ) ;
#64333=VERTEX_POINT ( 'NONE', #13814 ) ;
#64346=FACE_OUTER_BOUND ( 'NONE', #61714, .T. ) ;
#64366=CARTESIAN_POINT ( 'NONE',  ( -38.78836065780162556, 27.29347728569982223, -12.51982235623151851 ) ) ;
#64384=CARTESIAN_POINT ( 'NONE',  ( 1.248516582103246009, 51.80897656934063633, -8.678012929920056351 ) ) ;
#64388=CARTESIAN_POINT ( 'NONE',  ( 38.78798808878313054, 27.29340589088336344, 12.52162365134328503 ) ) ;
#64399=CARTESIAN_POINT ( 'NONE',  ( -26.02875901964593908, 37.04802764152638872, -9.463460753397949787 ) ) ;
#64404=CARTESIAN_POINT ( 'NONE',  ( -6.541984439259562301, 53.55430410265342545, 7.323266717688901473 ) ) ;
#64413=VECTOR ( 'NONE', #70465, 1000.000000000000000 ) ;
#64427=CARTESIAN_POINT ( 'NONE',  ( -22.45459161911049506, 27.61281158839761574, 32.95901622140758036 ) ) ;
#64434=CARTESIAN_POINT ( 'NONE',  ( 27.26479357511244572, 34.70231048953318265, 7.556984339685708818 ) ) ;
#64440=CARTESIAN_POINT ( 'NONE',  ( 16.48330046594864484, 43.81266695705367908, 4.157797401561414752 ) ) ;
#64444=PRESENTATION_STYLE_ASSIGNMENT (( #48227 ) ) ;
#64448=PRESENTATION_STYLE_ASSIGNMENT (( #97853 ) ) ;
#64453=CARTESIAN_POINT ( 'NONE',  ( 24.41558313457649376, 27.38491394452229954, -32.32218024782121546 ) ) ;
#64459=FACE_OUTER_BOUND ( 'NONE', #100746, .T. ) ;
#64468=CARTESIAN_POINT ( 'NONE',  ( 22.37334360784583964, 26.07629531780827037, -31.03047284417121432 ) ) ;
#64479=FILL_AREA_STYLE_COLOUR ( '', #53993 ) ;
#64486=CARTESIAN_POINT ( 'NONE',  ( -10.28624191511820207, 43.25714326066858462, 15.40779740156164124 ) ) ;
#64503=CARTESIAN_POINT ( 'NONE',  ( 47.24255575150607456, 16.92138162734670459, 16.58509488952848443 ) ) ;
#64570=CARTESIAN_POINT ( 'NONE',  ( 0.7778616825338859897, 25.97774080628767734, -38.51804523354821441 ) ) ;
#64575=CARTESIAN_POINT ( 'NONE',  ( 0.8415227374406197836, 53.50197623860572804, -9.927990696562751793 ) ) ;
#64601=FILL_AREA_STYLE ('',( #82366 ) ) ;
#64604=ORIENTED_EDGE ( 'NONE', *, *, #102462, .F. ) ;
#64621=ORIENTED_EDGE ( 'NONE', *, *, #81656, .T. ) ;
#64680=FACE_OUTER_BOUND ( 'NONE', #86645, .T. ) ;
#64700=CARTESIAN_POINT ( 'NONE',  ( -18.00634752349238710, 34.31709907050714037, -23.17894427062218554 ) ) ;
#64702=CARTESIAN_POINT ( 'NONE',  ( 49.13563689125552258, 12.95301730162418252, 16.19018188726472474 ) ) ;
#64706=( GEOMETRIC_REPRESENTATION_CONTEXT ( 3 ) GLOBAL_UNCERTAINTY_ASSIGNED_CONTEXT ( ( #43749 ) ) GLOBAL_UNIT_ASSIGNED_CONTEXT ( ( #50172, #35628, #100313 ) ) REPRESENTATION_CONTEXT ( 'NONE', 'WORKASPACE' ) );
#64713=ORIENTED_EDGE ( 'NONE', *, *, #63608, .F. ) ;
#64717=CARTESIAN_POINT ( 'NONE',  ( 9.735511751164029448, 51.35490659063075469, 2.349585191579547150 ) ) ;
#64747=FACE_BOUND ( 'NONE', #91805, .T. ) ;
#64750=CONICAL_SURFACE ( 'NONE', #83676, 22.55262289886175964, 1.221730476396026388 ) ;
#64763=CARTESIAN_POINT ( 'NONE',  ( -28.79633237789201772, 10.21664471455435397, -41.74470786255343313 ) ) ;
#64764=ORIENTED_EDGE ( 'NONE', *, *, #49313, .F. ) ;
#64773=EDGE_CURVE ( 'NONE', #87776, #4091, #35900, .T. ) ;
#64791=CARTESIAN_POINT ( 'NONE',  ( 16.75187969033571989, 34.99134772383131065, 21.80698433968582961 ) ) ;
#64807=DIRECTION ( 'NONE',  ( 0.000000000000000000, 1.000000000000000000, 0.000000000000000000 ) ) ;
#64847=CARTESIAN_POINT ( 'NONE',  ( 4.142849616820252293E-15, 0.000000000000000000, -33.82893434829263413 ) ) ;
#64851=CARTESIAN_POINT ( 'NONE',  ( 0.3379670387979981649, 44.07169264148151910, -16.28508512065656788 ) ) ;
#64856=CARTESIAN_POINT ( 'NONE',  ( -29.68315524076989576, 13.12249633091057177, 39.60535821593503414 ) ) ;
#64857=DIRECTION ( 'NONE',  ( 0.000000000000000000, 0.000000000000000000, -1.000000000000000000 ) ) ;
#64861=ORIENTED_EDGE ( 'NONE', *, *, #52200, .T. ) ;
#64871=EDGE_CURVE ( 'NONE', #1846, #9249, #85480, .T. ) ;
#64877=CARTESIAN_POINT ( 'NONE',  ( -37.56673239365863282, 27.60449318992554879, -13.45617127781024891 ) ) ;
#64888=CYLINDRICAL_SURFACE ( 'NONE', #70041, 1.250000000000001110 ) ;
#64890=CARTESIAN_POINT ( 'NONE',  ( 0.000000000000000000, 38.19193163660327173, 0.000000000000000000 ) ) ;
#64892=( LENGTH_UNIT ( ) NAMED_UNIT ( * ) SI_UNIT ( .MILLI., .METRE. ) );
#64893=ORIENTED_EDGE ( 'NONE', *, *, #91059, .T. ) ;
#64900=AXIS2_PLACEMENT_3D ( 'NONE', #94955, #5900, #86338 ) ;
#64901=CARTESIAN_POINT ( 'NONE',  ( 1.013110838965806781, 51.43236336151769450, -9.750292636990165462 ) ) ;
#64906=CARTESIAN_POINT ( 'NONE',  ( 49.28004588020311161, 7.871673175840917303, 15.62336800674797033 ) ) ;
#64912=CARTESIAN_POINT ( 'NONE',  ( -16.75187969033459012, 36.38380281757147827, 24.30698433969199357 ) ) ;
#64921=CARTESIAN_POINT ( 'NONE',  ( -8.879818925004332897, 51.45542084839959074, -4.000492447368358739 ) ) ;
#64922=CARTESIAN_POINT ( 'NONE',  ( -6.076451815340398355, 53.39448025720301416, 8.267155348349421118 ) ) ;
#64950=FACE_BOUND ( 'NONE', #72751, .T. ) ;
#64951=ORIENTED_EDGE ( 'NONE', *, *, #82873, .T. ) ;
#64962=ORIENTED_EDGE ( 'NONE', *, *, #12047, .F. ) ;
#64974=DIRECTION ( 'NONE',  ( 0.000000000000000000, 0.000000000000000000, 1.000000000000000000 ) ) ;
#64979=DIRECTION ( 'NONE',  ( 0.000000000000000000, 1.000000000000000000, 0.000000000000000000 ) ) ;
#64984=CARTESIAN_POINT ( 'NONE',  ( 37.56673239365841255, -1.200000000000000030E-05, -13.45617127781092215 ) ) ;
#64987=ORIENTED_EDGE ( 'NONE', *, *, #99945, .F. ) ;
#65000=CARTESIAN_POINT ( 'NONE',  ( 30.92868852183930883, 8.704894651777095760, 40.98784967800731494 ) ) ;
#65001=B_SPLINE_CURVE_WITH_KNOTS ( 'NONE', 3,
 ( #84257, #58384, #43268, #76151, #34143, #92869, #51874, #43791, #76686, #35745, #98824, #57832, #16875, #49755, #82661, #41668, #74557, #60535, #85323, #21679 ),
 .UNSPECIFIED., .F., .F.,
 ( 4, 2, 2, 2, 2, 2, 2, 2, 2, 4 ),
 ( 0.003104382421020200622, 0.003608261970678582845, 0.004112141520336965068, 0.004616021069995346858, 0.005119900619653729515, 0.005371840394482917808, 0.005623780169312107835, 0.006127659718970490492, 0.006631539268628873149, 0.007135418818287256673 ),
 .UNSPECIFIED. ) ;
#65015=ORIENTED_EDGE ( 'NONE', *, *, #48124, .T. ) ;
#65026=VERTEX_POINT ( 'NONE', #50302 ) ;
#65031=EDGE_CURVE ( 'NONE', #17567, #1846, #21779, .T. ) ;
#65046=CARTESIAN_POINT ( 'NONE',  ( 1.012109584170803878, 45.47521634855998229, -18.25170135021002338 ) ) ;
#65065=( GEOMETRIC_REPRESENTATION_CONTEXT ( 3 ) GLOBAL_UNCERTAINTY_ASSIGNED_CONTEXT ( ( #89433 ) ) GLOBAL_UNIT_ASSIGNED_CONTEXT ( ( #709, #82193, #26149 ) ) REPRESENTATION_CONTEXT ( 'NONE', 'WORKASPACE' ) );
#65142=CARTESIAN_POINT ( 'NONE',  ( 7.804526534074642363, 54.21474955791582317, -1.781545048635569506 ) ) ;
#65157=EDGE_CURVE ( 'NONE', #59854, #95973, #51896, .T. ) ;
#65159=CARTESIAN_POINT ( 'NONE',  ( 28.98628617572774502, 14.82338180310330600, 41.90038909576666981 ) ) ;
#65166=DIRECTION ( 'NONE',  ( -0.000000000000000000, 1.000000000000000000, 0.000000000000000000 ) ) ;
#65167=CARTESIAN_POINT ( 'NONE',  ( -28.88608732843799842, 18.87339843927421157, 39.88959139356617811 ) ) ;
#65173=CIRCLE ( 'NONE', #8356, 45.10524579772351217 ) ;
#65184=COLOUR_RGB ( '', 0.40784314, 0.44705882, 0.49803922) ;
#65189=CARTESIAN_POINT ( 'NONE',  ( 11.42599714053744009, 43.22993183554735452, -14.67767878811811499 ) ) ;
#65197=CARTESIAN_POINT ( 'NONE',  ( -17.71915776462827452, 45.45154592806376570, 4.750161495150144297 ) ) ;
#65203=PRESENTATION_STYLE_ASSIGNMENT (( #49000 ) ) ;
#65212=CARTESIAN_POINT ( 'NONE',  ( 23.21751746555303342, -1.200000000000000030E-05, 30.70617127781016720 ) ) ;
#65214=CARTESIAN_POINT ( 'NONE',  ( -0.08424723020174174071, 25.16821295365208044, 40.74999999999992895 ) ) ;
#65229=CARTESIAN_POINT ( 'NONE',  ( -17.62469156230236678, 43.36877173574055888, 4.616701353127022678 ) ) ;
#65238=CARTESIAN_POINT ( 'NONE',  ( -29.28872172473212032, 8.962789800749089153, 42.04350091203786377 ) ) ;
#65245=CARTESIAN_POINT ( 'NONE',  ( 9.761892272724042030, 51.33867874450312740, 2.429489512219626057 ) ) ;
#65253=CARTESIAN_POINT ( 'NONE',  ( -37.25037493859557003, 25.86378812652969472, -10.99421910838864491 ) ) ;
#65284=CARTESIAN_POINT ( 'NONE',  ( 25.85375728719300170, 35.06604825452144070, -8.747230897557770390 ) ) ;
#65286=( LENGTH_UNIT ( ) NAMED_UNIT ( * ) SI_UNIT ( .MILLI., .METRE. ) );
#65309=CARTESIAN_POINT ( 'NONE',  ( 24.46941191925081327, 25.33812252964237999, 31.99975807270328332 ) ) ;
#65322=CARTESIAN_POINT ( 'NONE',  ( 28.77727207546485744, 18.82954237789024532, -39.99083609194124023 ) ) ;
#65350=EDGE_LOOP ( 'NONE', ( #101192, #35179, #64764, #92833, #66141, #64180, #88190, #79702 ) ) ;
#65354=CARTESIAN_POINT ( 'NONE',  ( -5.934079579182491848, 51.88593101752500303, 6.163529546931266978 ) ) ;
#65358=DIRECTION ( 'NONE',  ( 0.000000000000000000, 0.000000000000000000, 1.000000000000000000 ) ) ;
#65365=CARTESIAN_POINT ( 'NONE',  ( -6.310069744396033187, 53.41366035806711920, -8.023364406089665835 ) ) ;
#65374=( GEOMETRIC_REPRESENTATION_CONTEXT ( 3 ) GLOBAL_UNCERTAINTY_ASSIGNED_CONTEXT ( ( #70686 ) ) GLOBAL_UNIT_ASSIGNED_CONTEXT ( ( #101775, #69426, #28459 ) ) REPRESENTATION_CONTEXT ( 'NONE', 'WORKASPACE' ) );
#65381=EDGE_LOOP ( 'NONE', ( #73875, #93200 ) ) ;
#65387=CARTESIAN_POINT ( 'NONE',  ( 0.9546611534775700791, 43.32630963623820008, -18.31104130856166989 ) ) ;
#65390=CARTESIAN_POINT ( 'NONE',  ( 17.73803972846102894, 45.30907581182018617, 6.035033385463663080 ) ) ;
#65395=ORIENTED_EDGE ( 'NONE', *, *, #93760, .F. ) ;
#65414=DIRECTION ( 'NONE',  ( -0.000000000000000000, 1.000000000000000000, 0.000000000000000000 ) ) ;
#65422=FILL_AREA_STYLE ('',( #111 ) ) ;
#65426=( GEOMETRIC_REPRESENTATION_CONTEXT ( 3 ) GLOBAL_UNCERTAINTY_ASSIGNED_CONTEXT ( ( #79818 ) ) GLOBAL_UNIT_ASSIGNED_CONTEXT ( ( #31621, #23536, #92480 ) ) REPRESENTATION_CONTEXT ( 'NONE', 'WORKASPACE' ) );
#65434=CARTESIAN_POINT ( 'NONE',  ( 9.757377548409222196E-14, 52.17923068443732149, -7.749999999998994582 ) ) ;
#65437=CARTESIAN_POINT ( 'NONE',  ( 49.19734730806133882, 7.744866885593247652, 16.05423930868156646 ) ) ;
#65455=CARTESIAN_POINT ( 'NONE',  ( -5.912056797256391327, 54.01423965850416664, 6.185180643280336454 ) ) ;
#65498=CARTESIAN_POINT ( 'NONE',  ( -17.83392795039137724, 45.30293236282058444, -5.798433727367500623 ) ) ;
#65504=CIRCLE ( 'NONE', #32807, 24.55262289886175964 ) ;
#65505=CARTESIAN_POINT ( 'NONE',  ( -4.524349771038530754, 51.56521623581706137, -8.281859981072610566 ) ) ;
#65509=CARTESIAN_POINT ( 'NONE',  ( 1.250952833799880093, 51.63827851261836344, 9.151171491867097885 ) ) ;
#65510=FILL_AREA_STYLE_COLOUR ( '', #66355 ) ;
#65513=CARTESIAN_POINT ( 'NONE',  ( 1.990040563172386960E-15, 46.21383923812596350, 16.25000000000000000 ) ) ;
#65518=CARTESIAN_POINT ( 'NONE',  ( -10.28624191511830155, 45.38549880562041494, -15.40779740156157196 ) ) ;
#65525=CARTESIAN_POINT ( 'NONE',  ( -37.24777618596957751, 27.71756692439280556, 13.42512197595613799 ) ) ;
#65528=CARTESIAN_POINT ( 'NONE',  ( 1.251035906659782038, 53.76664673156008689, 9.151124987501372487 ) ) ;
#65530=CARTESIAN_POINT ( 'NONE',  ( -36.35273129748642873, 28.20658870731680778, 11.89657741949426217 ) ) ;
#65534=DIRECTION ( 'NONE',  ( -0.000000000000000000, 1.000000000000000000, -0.000000000000000000 ) ) ;
#65537=CARTESIAN_POINT ( 'NONE',  ( -9.294025530568919891, 43.59757399217205887, 14.93482143293892683 ) ) ;
#65539=CARTESIAN_POINT ( 'NONE',  ( 8.719384894354538673, 51.50373999171648620, -4.031152949374879668 ) ) ;
#65541=FACE_BOUND ( 'NONE', #8769, .T. ) ;
#65569=COLOUR_RGB ( '', 0.66274510, 0.83137255, 0.94901961) ;
#65572=CARTESIAN_POINT ( 'NONE',  ( -9.323499571257183760, 53.46640638443131621, 3.784400446240228533 ) ) ;
#65580=CARTESIAN_POINT ( 'NONE',  ( 1.219168918416350333, 45.85934970230554342, -17.18082165270119788 ) ) ;
#65584=LINE ( 'NONE', #41832, #103872 ) ;
#65600=ORIENTED_EDGE ( 'NONE', *, *, #104134, .T. ) ;
#65603=FILL_AREA_STYLE_COLOUR ( '', #9301 ) ;
#65614=MECHANICAL_DESIGN_GEOMETRIC_PRESENTATION_REPRESENTATION('',(#36327),#53527);
#65617=CARTESIAN_POINT ( 'NONE',  ( 9.088913997560187141, 46.11732115646233865, 13.78939345329811061 ) ) ;
#65632=CARTESIAN_POINT ( 'NONE',  ( -0.08414610906330061146, 35.08181111624585213, -27.24999999999999289 ) ) ;
#65646=DIRECTION ( 'NONE',  ( 0.000000000000000000, 0.000000000000000000, 1.000000000000000000 ) ) ;
#65647=DIRECTION ( 'NONE',  ( 0.000000000000000000, 1.000000000000000000, 0.000000000000000000 ) ) ;
#65662=ORIENTED_EDGE ( 'NONE', *, *, #11141, .F. ) ;
#65668=CARTESIAN_POINT ( 'NONE',  ( -28.23200706912922797, 34.17505432317837943, -9.354431903020278938 ) ) ;
#65676=CARTESIAN_POINT ( 'NONE',  ( 7.345812283465320114, 54.30771946477985779, -2.470391858893527193 ) ) ;
#65689=B_SPLINE_CURVE_WITH_KNOTS ( 'NONE', 3,
 ( #15108, #95509, #7012, #55025, #21136, #12976, #96578, #47996, #45903, #63690, #78779, #105710, #53967, #29749, #4913, #80902, #39411, #37843, #96048, #38874, #46943, #71744 ),
 .UNSPECIFIED., .F., .F.,
 ( 4, 2, 2, 2, 2, 2, 2, 2, 2, 2, 4 ),
 ( 0.002852421517196360775, 0.003356447398460141000, 0.003860473279723920792, 0.004868525042251481243, 0.005120537982883364633, 0.005372550923515247157, 0.005624563864147129680, 0.005876576804779012203, 0.006380602686042778984, 0.006632615626674665844, 0.006884628567306552704 ),
 .UNSPECIFIED. ) ;
#65694=CARTESIAN_POINT ( 'NONE',  ( 28.46836751014411249, 13.00004364346769847, 40.55018863591786982 ) ) ;
#65697=EDGE_CURVE ( 'NONE', #50266, #8098, #93765, .T. ) ;
#65699=CARTESIAN_POINT ( 'NONE',  ( 29.59387530091309060, 18.41945862786180044, 39.60535821593452255 ) ) ;
#65708=CARTESIAN_POINT ( 'NONE',  ( -28.98629307556481294, 14.82330134267485455, 41.90042541400651999 ) ) ;
#65710=CARTESIAN_POINT ( 'NONE',  ( -21.99019548641716426, 25.96786802809918271, 31.66672321705982895 ) ) ;
#65713=ORIENTED_EDGE ( 'NONE', *, *, #96878, .F. ) ;
#65722=VECTOR ( 'NONE', #67479, 1000.000000000000227 ) ;
#65734=PRESENTATION_STYLE_ASSIGNMENT (( #106164 ) ) ;
#65735=CARTESIAN_POINT ( 'NONE',  ( -17.73948671138772326, 45.30893932440049099, 6.031879864029515481 ) ) ;
#65741=CARTESIAN_POINT ( 'NONE',  ( 15.66121600890972587, 45.99808261488239225, 6.197534896529969473 ) ) ;
#65750=CARTESIAN_POINT ( 'NONE',  ( -0.7828899409542838805, 25.26077281027161447, 40.48829533037867634 ) ) ;
#65751=CARTESIAN_POINT ( 'NONE',  ( -6.287528586677907235E-14, 28.20649408426966431, -38.24999999999931077 ) ) ;
#65771=CARTESIAN_POINT ( 'NONE',  ( -28.58246259357190056, 11.06567680426943667, 41.45945986390892557 ) ) ;
#65788=CYLINDRICAL_SURFACE ( 'NONE', #71446, 1.250000000000001110 ) ;
#65818=CARTESIAN_POINT ( 'NONE',  ( -28.46836751014381051, 13.00004364346765762, -40.55018863591808298 ) ) ;
#65827=CARTESIAN_POINT ( 'NONE',  ( -28.43253669899745617, 17.35855320307313221, -40.99008157358994708 ) ) ;
#65828=FILL_AREA_STYLE_COLOUR ( '', #65569 ) ;
#65841=CARTESIAN_POINT ( 'NONE',  ( -5.207109540145846260, 52.09997922571544393, 6.031152949374557259 ) ) ;
#65854=CARTESIAN_POINT ( 'NONE',  ( 5.290067270632321517, 52.08006895350504095, 6.031152949374479100 ) ) ;
#65856=VERTEX_POINT ( 'NONE', #63846 ) ;
#65857=PRESENTATION_STYLE_ASSIGNMENT (( #7601 ) ) ;
#65894=CARTESIAN_POINT ( 'NONE',  ( -23.38404382908472456, 27.34872606290121055, 33.19783523858075824 ) ) ;
#65895=B_SPLINE_CURVE_WITH_KNOTS ( 'NONE', 3,
 ( #6889, #39810, #97480, #48404, #81294, #69272, #3460, #21271, #102145, #20761, #28298, #37989, #61723, #44996, #36404, #101626, #29363, #76800, #87049, #5053 ),
 .UNSPECIFIED., .F., .F.,
 ( 4, 2, 2, 2, 2, 2, 2, 2, 2, 4 ),
 ( 0.0009508909574247000930, 0.001455760884198634402, 0.001960630810972568278, 0.002465500737746502587, 0.002970370664520436896, 0.003475240591294370771, 0.003980110518068305514, 0.004232545481455271368, 0.004484980444842237221, 0.004989850371616175867 ),
 .UNSPECIFIED. ) ;
#65896=ADVANCED_FACE ( 'NONE', ( #78947 ), #64888, .F. ) ;
#65902=VERTEX_POINT ( 'NONE', #5590 ) ;
#65911=CARTESIAN_POINT ( 'NONE',  ( -48.76867190053926748, 8.289666503167254064, -16.61714170248003342 ) ) ;
#65915=VECTOR ( 'NONE', #20040, 1000.000000000000000 ) ;
#65959=CARTESIAN_POINT ( 'NONE',  ( 7.483202312393204991, 52.00295125296706544, 3.437726841112358045 ) ) ;
#65962=CARTESIAN_POINT ( 'NONE',  ( 48.49185632690715408, 10.49696353563009410, 14.43858684427206640 ) ) ;
#65964=CARTESIAN_POINT ( 'NONE',  ( 0.6460500001699683859, 43.23245175272156615, 18.58310964118233954 ) ) ;
#66025=FILL_AREA_STYLE ('',( #97857 ) ) ;
#66038=CARTESIAN_POINT ( 'NONE',  ( 1.012362131619463090, 45.47537026410230254, 18.25126109922685558 ) ) ;
#66051=CARTESIAN_POINT ( 'NONE',  ( 1.217386590295936655, 53.94013396134795357, 8.674651084135625467 ) ) ;
#66059=ORIENTED_EDGE ( 'NONE', *, *, #55109, .F. ) ;
#66060=CARTESIAN_POINT ( 'NONE',  ( 30.80805190526341519, 8.074044156869311095, 41.40902236837642647 ) ) ;
#66067=VERTEX_POINT ( 'NONE', #353 ) ;
#66071=AXIS2_PLACEMENT_3D ( 'NONE', #19484, #35119, #67987 ) ;
#66076=CARTESIAN_POINT ( 'NONE',  ( 23.21751746555303342, -1.200000000000000030E-05, 33.20617127781017075 ) ) ;
#66084=CARTESIAN_POINT ( 'NONE',  ( 48.02835407290414338, 14.94086294439859408, -16.85535821593631667 ) ) ;
#66098=CARTESIAN_POINT ( 'NONE',  ( 37.56673239365899519, 25.75719283951025318, -10.95617127780834998 ) ) ;
#66101=CARTESIAN_POINT ( 'NONE',  ( -9.182222763132468657, 53.50083500536204184, 3.877122753022949730 ) ) ;
#66135=ORIENTED_EDGE ( 'NONE', *, *, #79519, .T. ) ;
#66141=ORIENTED_EDGE ( 'NONE', *, *, #78781, .T. ) ;
#66145=FACE_OUTER_BOUND ( 'NONE', #77782, .T. ) ;
#66155=( LENGTH_UNIT ( ) NAMED_UNIT ( * ) SI_UNIT ( .MILLI., .METRE. ) );
#66180=CARTESIAN_POINT ( 'NONE',  ( 22.88516029091543302, 26.05169045632067437, 30.73959371576558297 ) ) ;
#66193=B_SPLINE_CURVE_WITH_KNOTS ( 'NONE', 3,
 ( #63391, #56303, #15340, #89242, #70926, #96803, #62852, #22411, #14800, #71443, #79544, #78481, #6174, #55772, #87127, #71986, #103305, #96286, #13204, #46644 ),
 .UNSPECIFIED., .F., .F.,
 ( 4, 2, 2, 2, 2, 2, 2, 2, 2, 4 ),
 ( 0.0009441224788332293989, 0.001448919914566972403, 0.001953717350300715732, 0.002458514786034458628, 0.002963312221768201957, 0.003468109657501945286, 0.003972907093235689482, 0.004225305811102561364, 0.004477704528969433245, 0.004982501964703170937 ),
 .UNSPECIFIED. ) ;
#66215=CARTESIAN_POINT ( 'NONE',  ( 0.000000000000000000, 56.87938524157181774, -0.6840402866513453084 ) ) ;
#66217=EDGE_CURVE ( 'NONE', #28485, #25485, #78533, .T. ) ;
#66218=B_SPLINE_CURVE_WITH_KNOTS ( 'NONE', 3,
 ( #96835, #22965, #14829, #9379, #50376, #34247, #19674, #42833, #41768, #91400, #17515, #74652, #8863, #60116, #76788, #2363, #100531, #26694, #52514, #84894, #10982, #101613, #10455, #68173, #738, #93529, #101070, #18590, #33703, #75730 ),
 .UNSPECIFIED., .F., .F.,
 ( 4, 2, 2, 2, 2, 2, 2, 2, 2, 2, 2, 2, 2, 2, 4 ),
 ( 0.004426540215027332387, 0.005358602402239606710, 0.005824633495845744739, 0.006290664589451882768, 0.006523680136254953951, 0.006756695683058026869, 0.006989711229861098052, 0.007222726776664170970, 0.007455742323467242152, 0.007688757870270314203, 0.008154788963876466110, 0.009086851151088764719, 0.01001891333830106506, 0.01095097552551336367, 0.01188303771272565881 ),
 .UNSPECIFIED. ) ;
#66225=CARTESIAN_POINT ( 'NONE',  ( -28.43952395724186388, 17.90362770311683605, 40.70652153699781906 ) ) ;
#66226=CARTESIAN_POINT ( 'NONE',  ( -15.56704895981947168, 43.91947438609057741, -6.064211335331039621 ) ) ;
#66249=CARTESIAN_POINT ( 'NONE',  ( 11.36542776952655487, 43.57490045297072356, -13.50743829070831659 ) ) ;
#66250=EDGE_CURVE ( 'NONE', #15279, #84521, #94202, .T. ) ;
#66261=EDGE_LOOP ( 'NONE', ( #79554, #99433 ) ) ;
#66264=CARTESIAN_POINT ( 'NONE',  ( 9.180492345103683505, 53.50238668477037862, 3.869105311585077978 ) ) ;
#66265=EDGE_LOOP ( 'NONE', ( #83750, #6184, #23737, #60056 ) ) ;
#66272=CARTESIAN_POINT ( 'NONE',  ( -30.29489621385934228, 12.93001532776399642, 41.94819669044308341 ) ) ;
#66300=ORIENTED_EDGE ( 'NONE', *, *, #31133, .T. ) ;
#66305=CARTESIAN_POINT ( 'NONE',  ( 36.57348720720209201, 28.18042387246633851, -11.44262404694478974 ) ) ;
#66313=SURFACE_STYLE_FILL_AREA ( #41504 ) ;
#66323=ADVANCED_FACE ( 'NONE', ( #81691, #97898, #90885, #32673, #65541 ), #83883, .F. ) ;
#66328=CARTESIAN_POINT ( 'NONE',  ( -4.659670875555729452, 53.64098639941263258, 8.372684524479227619 ) ) ;
#66355=COLOUR_RGB ( '', 0.31764706, 0.68627451, 0.89019608) ;
#66370=EDGE_CURVE ( 'NONE', #7616, #3716, #67962, .T. ) ;
#66375=CARTESIAN_POINT ( 'NONE',  ( 28.79508601474799789, 15.38969543640854987, -41.74367987815723779 ) ) ;
#66410=VERTEX_POINT ( 'NONE', #85449 ) ;
#66421=CARTESIAN_POINT ( 'NONE',  ( -24.42584379203423950, 27.59191556861859596, 31.59852321640927642 ) ) ;
#66430=( NAMED_UNIT ( * ) SI_UNIT ( $, .STERADIAN. ) SOLID_ANGLE_UNIT ( ) );
#66447=CARTESIAN_POINT ( 'NONE',  ( 17.85237544995468895, 45.37579490857303455, 5.050174946722796321 ) ) ;
#66452=FILL_AREA_STYLE_COLOUR ( '', #59445 ) ;
#66457=CARTESIAN_POINT ( 'NONE',  ( 25.85844197703628211, 37.16340362582887025, -8.997040705657223469 ) ) ;
#66471=CARTESIAN_POINT ( 'NONE',  ( -46.81357782755159747, 18.41089473351688000, 15.91307620878805018 ) ) ;
#66482=CARTESIAN_POINT ( 'NONE',  ( 0.7777704900234801988, 34.98030770577876325, -27.51796982157703297 ) ) ;
#66489=CARTESIAN_POINT ( 'NONE',  ( 48.02835407290544367, 11.61227450977237829, 14.35535821593427386 ) ) ;
#66508=AXIS2_PLACEMENT_3D ( 'NONE', #4653, #68868, #86652 ) ;
#66509=CARTESIAN_POINT ( 'NONE',  ( 36.34557008114963139, 26.08151611875061349, 11.89035452524019476 ) ) ;
#66519=AXIS2_PLACEMENT_3D ( 'NONE', #61067, #93962, #20112 ) ;
#66541=CARTESIAN_POINT ( 'NONE',  ( 7.465554980039875943, 52.17267064398219389, -2.153157956675398665 ) ) ;
#66551=LINE ( 'NONE', #18017, #21026 ) ;
#66562=CARTESIAN_POINT ( 'NONE',  ( -0.7710323107892651517, 18.23550529380447927, 49.51187434724097614 ) ) ;
#66566=CARTESIAN_POINT ( 'NONE',  ( 16.64348903516523848, 45.88445698070336221, 4.157797401561420081 ) ) ;
#66574=CARTESIAN_POINT ( 'NONE',  ( -11.53045486031949807, 45.53936973856495030, -13.95636496209362143 ) ) ;
#66584=ORIENTED_EDGE ( 'NONE', *, *, #39960, .F. ) ;
#66587=CARTESIAN_POINT ( 'NONE',  ( -15.52500069721948250, 34.97057647050228013, -22.76630647231286275 ) ) ;
#66594=CARTESIAN_POINT ( 'NONE',  ( -9.040072111321892478, 43.92509090302731067, 14.03063673340002993 ) ) ;
#66596=CARTESIAN_POINT ( 'NONE',  ( 9.797545558212032546, 51.31160919791983588, -2.589760350952462709 ) ) ;
#66600=CARTESIAN_POINT ( 'NONE',  ( 6.133952071448687704, 51.27085470495629949, 8.207115774551422049 ) ) ;
#66637=CARTESIAN_POINT ( 'NONE',  ( -1.100143057407436675, 43.84113189085540085, 16.88562200540562941 ) ) ;
#66642=CARTESIAN_POINT ( 'NONE',  ( 0.7784210542099400110, 45.39571455979881165, -18.48152473499649773 ) ) ;
#66655=CARTESIAN_POINT ( 'NONE',  ( 26.78690032903771012, 34.58979447066111845, 10.02622625454039529 ) ) ;
#66691=CARTESIAN_POINT ( 'NONE',  ( -2.637755229554568666E-21, 53.39766064372320642, -10.24999999999999822 ) ) ;
#66697=CARTESIAN_POINT ( 'NONE',  ( 8.398900012642918966, 54.02103971888446665, 1.531152949374444239 ) ) ;
#66735=CARTESIAN_POINT ( 'NONE',  ( -28.09914318796796096, 34.19596624573215138, -9.569481124490501145 ) ) ;
#66751=MECHANICAL_DESIGN_GEOMETRIC_PRESENTATION_REPRESENTATION('',(#15071),#1272);
#66753=MECHANICAL_DESIGN_GEOMETRIC_PRESENTATION_REPRESENTATION('',(#25432),#39200);
#66761=AXIS2_PLACEMENT_3D ( 'NONE', #76495, #60870, #92687 ) ;
#66770=CARTESIAN_POINT ( 'NONE',  ( -28.94969860575643139, 18.87958371857672546, 39.84024749387425857 ) ) ;
#66790=CARTESIAN_POINT ( 'NONE',  ( -26.16445804740967063, 35.04392636896330515, 7.979516327253138641 ) ) ;
#66808=CARTESIAN_POINT ( 'NONE',  ( 16.02196273765584067, 46.08952128005080340, -4.311160109051586531 ) ) ;
#66839=CARTESIAN_POINT ( 'NONE',  ( -3.840629472727446691E-14, -1.200000000000000030E-05, -27.25000000000000000 ) ) ;
#66854=CARTESIAN_POINT ( 'NONE',  ( -16.80224347588841383, 43.42191715542256958, -6.657797401562048023 ) ) ;
#66869=CARTESIAN_POINT ( 'NONE',  ( -4.036353419639556961, 54.13891293591672849, 7.153575984207336091 ) ) ;
#66872=CARTESIAN_POINT ( 'NONE',  ( -38.64289892958222339, 25.32045246094368807, -11.54945401700677188 ) ) ;
#66877=CARTESIAN_POINT ( 'NONE',  ( 15.89150943383949333, 43.76196850971604846, -6.419014916071676957 ) ) ;
#66879=VERTEX_POINT ( 'NONE', #104806 ) ;
#66917=CARTESIAN_POINT ( 'NONE',  ( -4.524258892669210219, 51.56515624534051057, 8.282099392949428207 ) ) ;
#66922=CARTESIAN_POINT ( 'NONE',  ( 30.25640691047251707, 12.05011699928722102, -39.73625916528182245 ) ) ;
#66937=ADVANCED_FACE ( 'NONE', ( #622 ), #34672, .F. ) ;
#66947=CARTESIAN_POINT ( 'NONE',  ( -16.91657744243853045, 36.34978592707986422, -24.30698433968596461 ) ) ;
#66966=CARTESIAN_POINT ( 'NONE',  ( 36.57304083009643136, 26.05215988785383630, -11.44320818231313730 ) ) ;
#66968=CARTESIAN_POINT ( 'NONE',  ( 0.000000000000000000, 23.58303312036771615, 0.000000000000000000 ) ) ;
#66974=CARTESIAN_POINT ( 'NONE',  ( -24.32770621568460001, 27.33676458719045144, 32.55389746325912625 ) ) ;
#66988=CARTESIAN_POINT ( 'NONE',  ( -48.28061695858873748, 9.217865022612228287, -16.83796839065926676 ) ) ;
#66994=CARTESIAN_POINT ( 'NONE',  ( 16.80328583523077768, 45.82802980027266671, 4.157797401561413864 ) ) ;
#67005=FILL_AREA_STYLE_COLOUR ( '', #26577 ) ;
#67012=COLOUR_RGB ( '', 0.40784314, 0.44705882, 0.49803922) ;
#67016=VECTOR ( 'NONE', #50767, 1000.000000000000000 ) ;
#67024=SURFACE_STYLE_USAGE ( .BOTH. , #49220 ) ;
#67026=( GEOMETRIC_REPRESENTATION_CONTEXT ( 3 ) GLOBAL_UNCERTAINTY_ASSIGNED_CONTEXT ( ( #11090 ) ) GLOBAL_UNIT_ASSIGNED_CONTEXT ( ( #10002, #11049, #1356 ) ) REPRESENTATION_CONTEXT ( 'NONE', 'WORKASPACE' ) );
#67033=DIRECTION ( 'NONE',  ( -0.000000000000000000, 1.000000000000000000, -0.000000000000000000 ) ) ;
#67036=PRESENTATION_STYLE_ASSIGNMENT (( #19591 ) ) ;
#67040=CARTESIAN_POINT ( 'NONE',  ( 0.1699708769753489057, 44.08204242029594866, 16.25877257701097989 ) ) ;
#67053=CARTESIAN_POINT ( 'NONE',  ( -8.720250784003027889, 51.50345487123529864, -4.031152949374509298 ) ) ;
#67057=AXIS2_PLACEMENT_3D ( 'NONE', #48046, #13563, #47525 ) ;
#67062=CARTESIAN_POINT ( 'NONE',  ( -4.524249911684786518, 53.69361481913332312, -8.281779686802252627 ) ) ;
#67069=CARTESIAN_POINT ( 'NONE',  ( -15.51658955605313217, 44.08192631113433890, 4.860327001126657720 ) ) ;
#67071=CARTESIAN_POINT ( 'NONE',  ( 28.20029758590857227, 36.30545350850469077, -9.433058495126838139 ) ) ;
#67082=CARTESIAN_POINT ( 'NONE',  ( 7.576405003894376655, 51.95174893343489231, -3.569492037579363952 ) ) ;
#67090=CARTESIAN_POINT ( 'NONE',  ( -49.07662235626727920, 14.00107037724450798, 14.92012541985352669 ) ) ;
#67102=CARTESIAN_POINT ( 'NONE',  ( -0.2947874284240592502, 18.79274386076835768, 49.28318674568507873 ) ) ;
#67111=CARTESIAN_POINT ( 'NONE',  ( 0.9887502050300159828, 17.70131422926374398, -49.73213769803840023 ) ) ;
#67112=ORIENTED_EDGE ( 'NONE', *, *, #100888, .T. ) ;
#67114=CARTESIAN_POINT ( 'NONE',  ( 3.855937557716788584E-14, -1.200000000000000030E-05, 27.25000000000000000 ) ) ;
#67115=FACE_OUTER_BOUND ( 'NONE', #42091, .T. ) ;
#67118=ADVANCED_FACE ( 'NONE', ( #38376 ), #86400, .F. ) ;
#67135=CARTESIAN_POINT ( 'NONE',  ( 8.876331957793322402, 51.71967626501947279, -1.561720172594562195 ) ) ;
#67140=CARTESIAN_POINT ( 'NONE',  ( 6.509970471953121951, 51.36724606752097344, 7.565900303448065856 ) ) ;
#67184=CARTESIAN_POINT ( 'NONE',  ( -1.101319585913861587, 43.39549463643071192, 18.11240750576352809 ) ) ;
#67203=CARTESIAN_POINT ( 'NONE',  ( -30.63590201688455750, 10.93049107008196330, -40.03749794393677774 ) ) ;
#67204=AXIS2_PLACEMENT_3D ( 'NONE', #29388, #78956, #44482 ) ;
#67218=LINE ( 'NONE', #82315, #90641 ) ;
#67239=CARTESIAN_POINT ( 'NONE',  ( -8.719137237811853680, 53.63217708511133708, -4.031152949374852135 ) ) ;
#67248=EDGE_LOOP ( 'NONE', ( #52215, #79643 ) ) ;
#67250=CARTESIAN_POINT ( 'NONE',  ( 47.07447497471061126, 13.47837589781632950, 14.79567547011555995 ) ) ;
#67252=CARTESIAN_POINT ( 'NONE',  ( 24.17890427073063009, 25.18054377835295909, -32.75958092602339633 ) ) ;
#67262=CARTESIAN_POINT ( 'NONE',  ( -46.79842100651292469, 13.68672532571791400, -15.36912611011954510 ) ) ;
#67263=FACE_BOUND ( 'NONE', #101298, .T. ) ;
#67264=CARTESIAN_POINT ( 'NONE',  ( -36.31400481676831760, 26.07308277780756711, -12.05999164150846070 ) ) ;
#67280=CARTESIAN_POINT ( 'NONE',  ( 17.86532138382082024, 45.30096510830348677, -5.720552158557850930 ) ) ;
#67285=CARTESIAN_POINT ( 'NONE',  ( 8.399605801963765828, 54.02078684658069108, -1.531152949374517291 ) ) ;
#67295=CARTESIAN_POINT ( 'NONE',  ( 17.74039601254145637, 36.76373445370536075, -22.27539783717256228 ) ) ;
#67300=CARTESIAN_POINT ( 'NONE',  ( 15.73368388934906470, 35.06301254113061105, -22.31274010331293312 ) ) ;
#67310=SURFACE_STYLE_USAGE ( .BOTH. , #40895 ) ;
#67330=CARTESIAN_POINT ( 'NONE',  ( -25.88320034774018907, 35.08514486786264541, 8.494208376200145238 ) ) ;
#67346=CARTESIAN_POINT ( 'NONE',  ( 9.170976460981439260, 53.73491031865484047, 1.679364399482070391 ) ) ;
#67353=CARTESIAN_POINT ( 'NONE',  ( -29.77344787310991947, 13.34785391060250959, 42.10535821593509098 ) ) ;
#67357=CYLINDRICAL_SURFACE ( 'NONE', #1682, 1.250000000000001110 ) ;
#67401=VERTEX_POINT ( 'NONE', #5722 ) ;
#67414=( GEOMETRIC_REPRESENTATION_CONTEXT ( 3 ) GLOBAL_UNCERTAINTY_ASSIGNED_CONTEXT ( ( #26789 ) ) GLOBAL_UNIT_ASSIGNED_CONTEXT ( ( #72703, #47884, #5842 ) ) REPRESENTATION_CONTEXT ( 'NONE', 'WORKASPACE' ) );
#67455=CARTESIAN_POINT ( 'NONE',  ( 30.87917441950755659, 8.312254468506253602, -41.23121050640295238 ) ) ;
#67456=( LENGTH_UNIT ( ) NAMED_UNIT ( * ) SI_UNIT ( .MILLI., .METRE. ) );
#67463=SURFACE_STYLE_FILL_AREA ( #11860 ) ;
#67479=DIRECTION ( 'NONE',  ( 1.150791560227848051E-16, -0.3420201433256733758, 0.9396926207859066515 ) ) ;
#67496=CARTESIAN_POINT ( 'NONE',  ( 36.62728554792472124, 26.04043489851655480, -11.37739872878407255 ) ) ;
#67503=SURFACE_STYLE_USAGE ( .BOTH. , #34636 ) ;
#67505=UNCERTAINTY_MEASURE_WITH_UNIT (LENGTH_MEASURE( 1.000000000000000082E-05 ), #27572, 'distance_accuracy_value', 'NONE');
#67535=CARTESIAN_POINT ( 'NONE',  ( 26.35426118683261620, 36.89205985873699944, -9.819161256584076014 ) ) ;
#67565=CARTESIAN_POINT ( 'NONE',  ( 1.093552547293052069, 34.39704201091980451, -29.11089208678710705 ) ) ;
#67569=CARTESIAN_POINT ( 'NONE',  ( 7.578119713073430574, 51.95084648887009848, 3.571665354261504888 ) ) ;
#67576=EDGE_CURVE ( 'NONE', #91282, #91423, #81865, .T. ) ;
#67580=DIRECTION ( 'NONE',  ( 0.000000000000000000, 1.000000000000000000, -0.000000000000000000 ) ) ;
#67581=CYLINDRICAL_SURFACE ( 'NONE', #72023, 1.250000000000000222 ) ;
#67585=B_SPLINE_CURVE_WITH_KNOTS ( 'NONE', 3,
 ( #92582, #106217, #32381, #65253, #59171, #92052, #18736, #18185, #98143, #26833, #10593, #57144, #67264, #100142, #51044, #42981, #10069, #28973, #37583, #77999, #79059, #5179 ),
 .UNSPECIFIED., .F., .F.,
 ( 4, 2, 2, 2, 2, 2, 2, 2, 2, 2, 4 ),
 ( 0.003005601947361117611, 0.003258126653066766108, 0.003510651358772414604, 0.003763176064478062667, 0.004015700770183711597, 0.004520750181594991243, 0.005025799593006271757, 0.005530849004417552270, 0.006035898415828832783, 0.006540947827240112429, 0.007045997238651392942 ),
 .UNSPECIFIED. ) ;
#67594=( LENGTH_UNIT ( ) NAMED_UNIT ( * ) SI_UNIT ( .MILLI., .METRE. ) );
#67616=CARTESIAN_POINT ( 'NONE',  ( 7.306651344440208362, 52.17319877359566505, -2.637493225739738101 ) ) ;
#67619=CARTESIAN_POINT ( 'NONE',  ( -0.6458819410170080211, 27.35549314424027756, -40.58326240071404811 ) ) ;
#67623=CARTESIAN_POINT ( 'NONE',  ( 47.44867487729116817, 16.35164899989712239, -16.71951642917279202 ) ) ;
#67626=CARTESIAN_POINT ( 'NONE',  ( -49.26579422795270347, 13.23794831108498649, 15.39367580924676560 ) ) ;
#67629=CYLINDRICAL_SURFACE ( 'NONE', #35766, 1.249999999999999334 ) ;
#67638=CARTESIAN_POINT ( 'NONE',  ( -4.036265570123655166, 52.01079393774872983, -7.152884558231209056 ) ) ;
#67639=VERTEX_POINT ( 'NONE', #93015 ) ;
#67640=CARTESIAN_POINT ( 'NONE',  ( -3.312116827214752676E-14, 12.91535575336970965, 51.75000000000017764 ) ) ;
#67650=FACE_OUTER_BOUND ( 'NONE', #46148, .T. ) ;
#67651=( NAMED_UNIT ( * ) PLANE_ANGLE_UNIT ( ) SI_UNIT ( $, .RADIAN. ) );
#67658=EDGE_LOOP ( 'NONE', ( #89593, #22162 ) ) ;
#67664=FILL_AREA_STYLE_COLOUR ( '', #74304 ) ;
#67666=ORIENTED_EDGE ( 'NONE', *, *, #95044, .F. ) ;
#67669=CARTESIAN_POINT ( 'NONE',  ( 8.559508646656349029, 51.83514083332403999, -1.531152949374623873 ) ) ;
#67670=CARTESIAN_POINT ( 'NONE',  ( -8.559508646656370345, -1.200000000000000030E-05, 2.781152949374564365 ) ) ;
#67679=EDGE_CURVE ( 'NONE', #96995, #68089, #67769, .T. ) ;
#67680=VERTEX_POINT ( 'NONE', #19707 ) ;
#67684=CARTESIAN_POINT ( 'NONE',  ( -36.31544203073882215, 28.19121493635761766, -12.14374965612692669 ) ) ;
#67689=CARTESIAN_POINT ( 'NONE',  ( -36.64357978206631117, 25.84195196822051344, 13.05277382008214282 ) ) ;
#67693=CARTESIAN_POINT ( 'NONE',  ( -10.28624191511829977, 46.12099395432375104, -12.90779740156156841 ) ) ;
#67705=CARTESIAN_POINT ( 'NONE',  ( 38.33084065836750653, 25.24363705771616750, -13.20929050494120993 ) ) ;
#67711=( NAMED_UNIT ( * ) PLANE_ANGLE_UNIT ( ) SI_UNIT ( $, .RADIAN. ) );
#67713=SURFACE_SIDE_STYLE ('',( #68242 ) ) ;
#67724=CARTESIAN_POINT ( 'NONE',  ( 1.249391989912810752, 27.86128073807352834, 39.17855071985294302 ) ) ;
#67730=DIRECTION ( 'NONE',  ( 0.000000000000000000, 1.000000000000000000, 0.000000000000000000 ) ) ;
#67742=UNCERTAINTY_MEASURE_WITH_UNIT (LENGTH_MEASURE( 1.000000000000000082E-05 ), #44110, 'distance_accuracy_value', 'NONE');
#67764=LINE ( 'NONE', #93102, #50937 ) ;
#67769=B_SPLINE_CURVE_WITH_KNOTS ( 'NONE', 3,
 ( #9965, #59064, #100037, #11016, #69292, #9413, #100567, #26204, #91950, #75766, #67684, #27801, #102165, #50409, #35887, #83321, #93559, #1860, #52544, #68765 ),
 .UNSPECIFIED., .F., .F.,
 ( 4, 2, 2, 2, 2, 2, 2, 2, 2, 4 ),
 ( 0.003063312233486976607, 0.003568397869495329531, 0.004073483505503682454, 0.004578569141512035812, 0.004831111959516212057, 0.005083654777520388302, 0.005588740413528742526, 0.006093826049537097618, 0.006598911685545452710, 0.007103997321553806935 ),
 .UNSPECIFIED. ) ;
#67774=CARTESIAN_POINT ( 'NONE',  ( 23.21751746555220564, 25.98869614573808917, -30.70617127781077116 ) ) ;
#67798=CARTESIAN_POINT ( 'NONE',  ( 17.89653557359968872, 45.30873500717390101, -5.550246105160208110 ) ) ;
#67819=ORIENTED_EDGE ( 'NONE', *, *, #78805, .F. ) ;
#67820=DIRECTION ( 'NONE',  ( -0.000000000000000000, 1.000000000000000000, -0.000000000000000000 ) ) ;
#67826=CARTESIAN_POINT ( 'NONE',  ( 22.57731121199973856, 28.20557510165626880, -30.87924556879413984 ) ) ;
#67848=( NAMED_UNIT ( * ) PLANE_ANGLE_UNIT ( ) SI_UNIT ( $, .RADIAN. ) );
#67853=EDGE_LOOP ( 'NONE', ( #52576, #69393, #89161, #50980, #90456, #54071, #99067, #42022 ) ) ;
#67866=CARTESIAN_POINT ( 'NONE',  ( 8.559508646656407649, 53.68473964988125857, 4.031152949374444461 ) ) ;
#67869=( NAMED_UNIT ( * ) SI_UNIT ( $, .STERADIAN. ) SOLID_ANGLE_UNIT ( ) );
#67877=SURFACE_STYLE_FILL_AREA ( #59268 ) ;
#67879=VERTEX_POINT ( 'NONE', #69163 ) ;
#67895=CARTESIAN_POINT ( 'NONE',  ( -11.51402452371067042, 43.27676821513870209, -14.44504951838048967 ) ) ;
#67915=CARTESIAN_POINT ( 'NONE',  ( -24.46186824438995799, 25.41025174371402784, -31.75584039582438933 ) ) ;
#67933=CARTESIAN_POINT ( 'NONE',  ( 15.88274348574180195, 44.00148148787235414, -4.401868159917717627 ) ) ;
#67938=CARTESIAN_POINT ( 'NONE',  ( -15.42941528477439306, 46.21391461311945648, 5.098611828030516158 ) ) ;
#67962=B_SPLINE_CURVE_WITH_KNOTS ( 'NONE', 3,
 ( #2916, #43395, #99479, #50396, #76278, #19696, #66600, #50926, #17536, #83309, #67140, #18068, #52000, #52530, #93548, #35332, #754, #43919, #33721, #35872, #2386, #1845 ),
 .UNSPECIFIED., .F., .F.,
 ( 4, 2, 2, 2, 2, 2, 2, 2, 2, 2, 4 ),
 ( 0.002311503593064429506, 0.002814959816865062261, 0.003066687928765378639, 0.003318416040665695017, 0.003821872264466328641, 0.004073600376366644585, 0.004325328488266960529, 0.005332240935868233847, 0.005835697159668867470, 0.006087425271569182547, 0.006339153383469499359 ),
 .UNSPECIFIED. ) ;
#67970=CARTESIAN_POINT ( 'NONE',  ( 28.10294377376055053, 36.32212184348568229, 9.577882736625975113 ) ) ;
#67974=EDGE_CURVE ( 'NONE', #57566, #10346, #103663, .T. ) ;
#67975=CARTESIAN_POINT ( 'NONE',  ( 30.75967547141102187, 7.962001144779974560, -41.50359925574515785 ) ) ;
#67980=AXIS2_PLACEMENT_3D ( 'NONE', #76233, #36365, #99430 ) ;
#67987=DIRECTION ( 'NONE',  ( 0.000000000000000000, 0.000000000000000000, 1.000000000000000000 ) ) ;
#67988=EDGE_CURVE ( 'NONE', #54873, #6732, #15671, .T. ) ;
#68007=SURFACE_STYLE_USAGE ( .BOTH. , #84724 ) ;
#68028=CARTESIAN_POINT ( 'NONE',  ( -0.1693524243964244225, 45.30391365246044444, 18.74999999999999645 ) ) ;
#68035=CARTESIAN_POINT ( 'NONE',  ( -49.10020235979911973, 7.817788915495857083, -16.25178062802477186 ) ) ;
#68037=CARTESIAN_POINT ( 'NONE',  ( 7.696567030444234644E-14, -1.200000000000000030E-05, 38.25000000000000000 ) ) ;
#68049=VERTEX_POINT ( 'NONE', #31372 ) ;
#68059=AXIS2_PLACEMENT_3D ( 'NONE', #24896, #49127, #98223 ) ;
#68071=CARTESIAN_POINT ( 'NONE',  ( -46.97732051764550931, 17.75298140206600905, 16.28617214199123353 ) ) ;
#68076=CARTESIAN_POINT ( 'NONE',  ( 0.8433544674962375476, 13.67115454006535558, 51.42600440392107686 ) ) ;
#68085=LINE ( 'NONE', #27138, #14723 ) ;
#68089=VERTEX_POINT ( 'NONE', #58811 ) ;
#68097=CARTESIAN_POINT ( 'NONE',  ( -8.717757428195424652, 51.77844298770122577, -1.531152949373723482 ) ) ;
#68099=CARTESIAN_POINT ( 'NONE',  ( 36.48965585550728719, 25.91808176478719616, 12.86142835070472223 ) ) ;
#68107=CARTESIAN_POINT ( 'NONE',  ( -4.652092900574788636, 54.30645573760831724, -6.202889689747271618 ) ) ;
#68110=CARTESIAN_POINT ( 'NONE',  ( -9.045746190732444347, 45.90313006749668290, -14.51680462862712062 ) ) ;
#68115=B_SPLINE_CURVE_WITH_KNOTS ( 'NONE', 3,
 ( #72653, #39250, #64059, #55907, #98516, #24145, #73707, #80735, #96422, #23069, #32215, #97443, #97992, #48370, #88844, #105552, #106609, #56455, #14938, #82340, #65632, #106066 ),
 .UNSPECIFIED., .F., .F.,
 ( 4, 2, 2, 2, 2, 2, 2, 2, 2, 2, 4 ),
 ( 0.007334634194406657905, 0.007586619625986230908, 0.007838605057565803044, 0.008342575920724945582, 0.008846546783884086385, 0.009350517647043227187, 0.01035845937336151053, 0.01061044480494107919, 0.01086243023652064786, 0.01111441566810021826, 0.01136640109967978693 ),
 .UNSPECIFIED. ) ;
#68119=COLOUR_RGB ( '', 0.40784314, 0.44705882, 0.49803922) ;
#68135=CARTESIAN_POINT ( 'NONE',  ( 7.337993220704071007, 52.18301828126001141, -2.466490591092684870 ) ) ;
#68139=PRODUCT_DEFINITION_SHAPE ( 'NONE', 'NONE',  #30479 ) ;
#68141=ORIENTED_EDGE ( 'NONE', *, *, #42627, .F. ) ;
#68146=CARTESIAN_POINT ( 'NONE',  ( -48.76595811598829755, 13.46359178982173255, 16.61915017902422420 ) ) ;
#68152=CARTESIAN_POINT ( 'NONE',  ( 7.715274834628325378E-15, 2.000000000000000000, -63.00000000000000000 ) ) ;
#68159=CARTESIAN_POINT ( 'NONE',  ( -22.89219133817175589, 25.33230817006059965, -33.16583220086505435 ) ) ;
#68162=CARTESIAN_POINT ( 'NONE',  ( -26.35037284168458527, 34.99717245364579554, -7.807171992874543776 ) ) ;
#68169=VERTEX_POINT ( 'NONE', #2128 ) ;
#68173=CARTESIAN_POINT ( 'NONE',  ( -47.14583847125333449, 17.20522387600227532, -16.50112645798017041 ) ) ;
#68178=MECHANICAL_DESIGN_GEOMETRIC_PRESENTATION_REPRESENTATION('',(#81374),#83740);
#68182=CARTESIAN_POINT ( 'NONE',  ( -16.58598004038824314, 34.29213908405171196, -24.29859534253508713 ) ) ;
#68191=CARTESIAN_POINT ( 'NONE',  ( 48.02835407290503866, 11.61227450977245468, -14.35535821593549954 ) ) ;
#68192=SURFACE_STYLE_USAGE ( .BOTH. , #35330 ) ;
#68211=CARTESIAN_POINT ( 'NONE',  ( 48.26904874857434180, 16.21976735686757110, -14.37315625587818069 ) ) ;
#68220=CARTESIAN_POINT ( 'NONE',  ( 23.21751746555220564, -1.200000000000000030E-05, -31.95617127781077116 ) ) ;
#68242=SURFACE_STYLE_FILL_AREA ( #93047 ) ;
#68253=CARTESIAN_POINT ( 'NONE',  ( -8.398775527966902743, 54.02108431962560786, 1.531152949374565475 ) ) ;
#68259=CARTESIAN_POINT ( 'NONE',  ( -30.93386089602973499, 8.839832930400778110, -40.91297150549259953 ) ) ;
#68278=( LENGTH_UNIT ( ) NAMED_UNIT ( * ) SI_UNIT ( .MILLI., .METRE. ) );
#68297=UNCERTAINTY_MEASURE_WITH_UNIT (LENGTH_MEASURE( 1.000000000000000082E-05 ), #102024, 'distance_accuracy_value', 'NONE');
#68338=CARTESIAN_POINT ( 'NONE',  ( 17.84510959215113601, 45.37789619860912183, -5.053583809357707679 ) ) ;
#68345=CARTESIAN_POINT ( 'NONE',  ( 16.75187969033515145, -1.200000000000000030E-05, -21.80698433968624528 ) ) ;
#68358=ORIENTED_EDGE ( 'NONE', *, *, #73524, .T. ) ;
#68362=DIRECTION ( 'NONE',  ( -0.000000000000000000, 1.000000000000000000, 0.000000000000000000 ) ) ;
#68364=SURFACE_STYLE_USAGE ( .BOTH. , #93162 ) ;
#68379=CONICAL_SURFACE ( 'NONE', #75278, 0.6840402866513453084, 1.221730476396026610 ) ;
#68387=CARTESIAN_POINT ( 'NONE',  ( 0.000000000000000000, 50.89575828009192549, 0.000000000000000000 ) ) ;
#68388=CARTESIAN_POINT ( 'NONE',  ( -1.219336931563358206, 27.86033604905912142, 39.18213164352511058 ) ) ;
#68389=CARTESIAN_POINT ( 'NONE',  ( 1.099490667017193335, 36.97155732390793048, -27.88395719433528086 ) ) ;
#68390=EDGE_CURVE ( 'NONE', #27731, #14520, #41957, .T. ) ;
#68427=AXIS2_PLACEMENT_3D ( 'NONE', #47908, #39324, #31763 ) ;
#68428=DIRECTION ( 'NONE',  ( 0.000000000000000000, 1.000000000000000000, 0.000000000000000000 ) ) ;
#68434=CARTESIAN_POINT ( 'NONE',  ( 49.24259736700050638, 13.36037099747072077, 15.29523612018071965 ) ) ;
#68439=CARTESIAN_POINT ( 'NONE',  ( 0.6443221131828161807, 46.14907239561987495, -16.41599980877370868 ) ) ;
#68442=EDGE_LOOP ( 'NONE', ( #32368, #63619, #105948, #61233 ) ) ;
#68455=CARTESIAN_POINT ( 'NONE',  ( -0.7826757305971107082, 46.11193258928162209, -16.51179486519325579 ) ) ;
#68457=( GEOMETRIC_REPRESENTATION_CONTEXT ( 3 ) GLOBAL_UNCERTAINTY_ASSIGNED_CONTEXT ( ( #47182 ) ) GLOBAL_UNIT_ASSIGNED_CONTEXT ( ( #105026, #36884, #27197 ) ) REPRESENTATION_CONTEXT ( 'NONE', 'WORKASPACE' ) );
#68463=ORIENTED_EDGE ( 'NONE', *, *, #101515, .F. ) ;
#68469=ORIENTED_EDGE ( 'NONE', *, *, #96960, .F. ) ;
#68478=CARTESIAN_POINT ( 'NONE',  ( 16.48332215917152155, 43.52969185147832576, -6.657797401561809991 ) ) ;
#68503=ORIENTED_EDGE ( 'NONE', *, *, #64871, .F. ) ;
#68531=B_SPLINE_CURVE_WITH_KNOTS ( 'NONE', 3,
 ( #90527, #15033, #16639, #6942, #33376, #15569, #66249, #48984, #32849, #31264, #56001, #65189, #88938, #99130, #48460, #80830, #25295, #81350, #58153, #39862, #40378, #49528 ),
 .UNSPECIFIED., .F., .F.,
 ( 4, 2, 2, 2, 2, 2, 2, 2, 2, 2, 4 ),
 ( 0.003086826075679745870, 0.003590365117157389135, 0.004093904158635032833, 0.004597443200112676098, 0.005100982241590319363, 0.005604521283067962628, 0.005856290803806785995, 0.006108060324545609363, 0.006611599366023262168, 0.006863368886762087270, 0.007115138407500913240 ),
 .UNSPECIFIED. ) ;
#68548=CARTESIAN_POINT ( 'NONE',  ( 23.21751746555303342, 28.11705169068991594, 30.70617127781016720 ) ) ;
#68561=CARTESIAN_POINT ( 'NONE',  ( -6.133363361299304373, 51.27081518319509712, 8.207696194639346743 ) ) ;
#68569=DIRECTION ( 'NONE',  ( 0.000000000000000000, 0.000000000000000000, -1.000000000000000000 ) ) ;
#68580=UNCERTAINTY_MEASURE_WITH_UNIT (LENGTH_MEASURE( 1.000000000000000082E-05 ), #104340, 'distance_accuracy_value', 'NONE');
#68606=CARTESIAN_POINT ( 'NONE',  ( 8.559508646656350805, -1.200000000000000030E-05, -2.781152949374623873 ) ) ;
#68631=CARTESIAN_POINT ( 'NONE',  ( 17.72964667321921084, 43.18374047180136444, 6.032092183256372309 ) ) ;
#68640=CIRCLE ( 'NONE', #1456, 55.00000000000000000 ) ;
#68645=DIRECTION ( 'NONE',  ( 0.000000000000000000, 1.000000000000000000, 0.000000000000000000 ) ) ;
#68652=CARTESIAN_POINT ( 'NONE',  ( -8.400245266945324474, 51.89220219220736396, -1.531152949373711269 ) ) ;
#68658=CARTESIAN_POINT ( 'NONE',  ( -8.875831270970040876, 51.71986688677656474, -1.561544505752369139 ) ) ;
#68660=CARTESIAN_POINT ( 'NONE',  ( -16.75187969033459012, 36.38380281757147827, 24.30698433969199357 ) ) ;
#68663=CARTESIAN_POINT ( 'NONE',  ( 9.067167209133366157, 43.96885688137683701, -13.86970262315736413 ) ) ;
#68668=ORIENTED_EDGE ( 'NONE', *, *, #88801, .F. ) ;
#68673=CARTESIAN_POINT ( 'NONE',  ( -15.55686096457869461, 44.07612650370892737, 4.784268412334826692 ) ) ;
#68676=CARTESIAN_POINT ( 'NONE',  ( 28.31925951855187051, 36.30018004457540570, -9.115863556877831897 ) ) ;
#68687=COLOUR_RGB ( '', 0.08235294, 0.09019608, 0.10196078) ;
#68691=EDGE_CURVE ( 'NONE', #43850, #46319, #16352, .T. ) ;
#68692=CARTESIAN_POINT ( 'NONE',  ( -1.250365908232453638, 27.68769234945010638, -39.65568885478079153 ) ) ;
#68701=CARTESIAN_POINT ( 'NONE',  ( -49.09761780907699347, 12.98984206366086980, 16.25597134831825130 ) ) ;
#68714=CARTESIAN_POINT ( 'NONE',  ( -22.19943786829402299, 26.05963078907934971, -31.21165477453312320 ) ) ;
#68751=EDGE_LOOP ( 'NONE', ( #50321, #105902, #98902, #43833 ) ) ;
#68765=CARTESIAN_POINT ( 'NONE',  ( -37.56673239365863282, 27.60449318992554879, -13.45617127781024891 ) ) ;
#68781=DIRECTION ( 'NONE',  ( 0.000000000000000000, 1.000000000000000000, 0.000000000000000000 ) ) ;
#68805=CARTESIAN_POINT ( 'NONE',  ( 0.3334354129020682400, 27.31151862705754141, 40.70764297020699019 ) ) ;
#68821=UNCERTAINTY_MEASURE_WITH_UNIT (LENGTH_MEASURE( 1.000000000000000082E-05 ), #16828, 'distance_accuracy_value', 'NONE');
#68822=CARTESIAN_POINT ( 'NONE',  ( 4.079861200793539311, 53.97863311128789121, -7.631710309917290935 ) ) ;
#68832=VERTEX_POINT ( 'NONE', #102046 ) ;
#68839=UNCERTAINTY_MEASURE_WITH_UNIT (LENGTH_MEASURE( 1.000000000000000082E-05 ), #61167, 'distance_accuracy_value', 'NONE');
#68849=CARTESIAN_POINT ( 'NONE',  ( -16.34245632501147583, 37.19060558336133937, -21.87293403489680088 ) ) ;
#68862=CARTESIAN_POINT ( 'NONE',  ( -46.92822048327052897, 13.65838325462196323, -15.00718171297879344 ) ) ;
#68867=CARTESIAN_POINT ( 'NONE',  ( -17.73049404743309410, 43.18361977675543528, -6.030632858976519906 ) ) ;
#68868=DIRECTION ( 'NONE',  ( 0.000000000000000000, 1.000000000000000000, 0.000000000000000000 ) ) ;
#68923=FILL_AREA_STYLE ('',( #86178 ) ) ;
#68924=CARTESIAN_POINT ( 'NONE',  ( -3.311033882356798252E-14, 37.21016666119783167, -27.24999999999961986 ) ) ;
#68928=B_SPLINE_CURVE_WITH_KNOTS ( 'NONE', 3,
 ( #59284, #92161, #77048, #52233, #43095, #85142, #11235, #3164, #60883, #36109, #101854, #53829, #96435, #78110, #63539, #31192, #53313, #61956, #37162, #54880, #71079, #94848 ),
 .UNSPECIFIED., .F., .F.,
 ( 4, 2, 2, 2, 2, 2, 2, 2, 2, 2, 4 ),
 ( 0.007230059716208242504, 0.007733998775341412342, 0.008237937834474582180, 0.008741876893607751151, 0.009245815952740921856, 0.009749755011874090826, 0.01000172454144068052, 0.01025369407100727021, 0.01050566360057385989, 0.01075763313014044958, 0.01126157218927362549 ),
 .UNSPECIFIED. ) ;
#68961=FACE_OUTER_BOUND ( 'NONE', #9587, .T. ) ;
#68978=CARTESIAN_POINT ( 'NONE',  ( -11.29926588360462603, 43.19537255330742198, -14.89485451155379359 ) ) ;
#68980=B_SPLINE_CURVE_WITH_KNOTS ( 'NONE', 3,
 ( #99754, #2641, #9135, #60386, #43118, #18882, #27510, #28037, #36134, #44184, #76004, #35587, #101877, #1569, #100282, #26443, #93797, #93263, #51725, #59310, #83043, #35054 ),
 .UNSPECIFIED., .F., .F.,
 ( 4, 2, 2, 2, 2, 2, 2, 2, 2, 2, 4 ),
 ( 0.003198323314689233317, 0.003450306839784169494, 0.003702290364879106104, 0.004206257415068978892, 0.004710224465258851245, 0.005214191515448723599, 0.006222125615828478715, 0.006474109140923419228, 0.006726092666018360609, 0.006978076191113301990, 0.007230059716208242504 ),
 .UNSPECIFIED. ) ;
#68982=VERTEX_POINT ( 'NONE', #20669 ) ;
#69000=ORIENTED_EDGE ( 'NONE', *, *, #91279, .T. ) ;
#69019=CARTESIAN_POINT ( 'NONE',  ( -15.39894322001510574, 46.20524723896237163, 5.264004132386240542 ) ) ;
#69027=AXIS2_PLACEMENT_3D ( 'NONE', #15104, #80899, #7008 ) ;
#69057=( NAMED_UNIT ( * ) PLANE_ANGLE_UNIT ( ) SI_UNIT ( $, .RADIAN. ) );
#69068=ORIENTED_EDGE ( 'NONE', *, *, #7083, .T. ) ;
#69074=DIRECTION ( 'NONE',  ( 0.000000000000000000, 1.000000000000000000, 0.000000000000000000 ) ) ;
#69106=CARTESIAN_POINT ( 'NONE',  ( -15.66121600890969390, 45.99808261488237804, -6.197534896530083159 ) ) ;
#69112=COLOUR_RGB ( '', 0.09019608, 0.27058824, 0.51372549) ;
#69122=FACE_OUTER_BOUND ( 'NONE', #100138, .T. ) ;
#69156=CARTESIAN_POINT ( 'NONE',  ( 0.6249480602962063092, 13.29596660449504952, 51.58658030989757037 ) ) ;
#69163=CARTESIAN_POINT ( 'NONE',  ( 1.196618058419959393E-20, 36.30024107553216339, -29.75000000000000355 ) ) ;
#69170=FACE_BOUND ( 'NONE', #25023, .T. ) ;
#69180=AXIS2_PLACEMENT_3D ( 'NONE', #2562, #75931, #59768 ) ;
#69186=( NAMED_UNIT ( * ) PLANE_ANGLE_UNIT ( ) SI_UNIT ( $, .RADIAN. ) );
#69196=ORIENTED_EDGE ( 'NONE', *, *, #68390, .F. ) ;
#69226=CARTESIAN_POINT ( 'NONE',  ( 48.02835407290504577, 16.78162100668611956, -14.35535821593549954 ) ) ;
#69228=FACE_BOUND ( 'NONE', #83547, .T. ) ;
#69233=B_SPLINE_CURVE_WITH_KNOTS ( 'NONE', 3,
 ( #82062, #30498, #12684, #95226, #7632, #54198, #98256, #96295, #24409, #29974, #57248, #62862, #90167, #73970, #8182, #81511, #95747, #22419, #54730, #58879, #579, #2740 ),
 .UNSPECIFIED., .F., .F.,
 ( 4, 2, 2, 2, 2, 2, 2, 2, 2, 2, 4 ),
 ( 0.003159815893393695240, 0.003663154312159962872, 0.004166492730926230938, 0.004669831149692498136, 0.004921500359075634337, 0.005173169568458770538, 0.005676507987225038604, 0.005928177196608170468, 0.006179846405991303200, 0.006683184824757560857, 0.007186523243523819382 ),
 .UNSPECIFIED. ) ;
#69243=CARTESIAN_POINT ( 'NONE',  ( -26.28481937415909542, 35.01454853161727954, -7.860150299234582860 ) ) ;
#69256=PRESENTATION_STYLE_ASSIGNMENT (( #28283 ) ) ;
#69265=( LENGTH_UNIT ( ) NAMED_UNIT ( * ) SI_UNIT ( .MILLI., .METRE. ) );
#69271=CARTESIAN_POINT ( 'NONE',  ( -17.94988149306818315, 34.25920654870290605, 23.42332176153287193 ) ) ;
#69272=CARTESIAN_POINT ( 'NONE',  ( 9.295423129715947752, 45.72519545954834541, -14.93632663516908821 ) ) ;
#69292=CARTESIAN_POINT ( 'NONE',  ( -36.80513907854941635, 28.12583545932849916, -11.20123465776408445 ) ) ;
#69325=AXIS2_PLACEMENT_3D ( 'NONE', #59472, #94496, #85327 ) ;
#69332=CARTESIAN_POINT ( 'NONE',  ( -29.77184624873650520, 12.99572234387823322, -39.60535821593474992 ) ) ;
#69371=CARTESIAN_POINT ( 'NONE',  ( -0.7817778800081601753, 52.07046414514121579, -8.011393227464683520 ) ) ;
#69377=ORIENTED_EDGE ( 'NONE', *, *, #51839, .F. ) ;
#69393=ORIENTED_EDGE ( 'NONE', *, *, #45715, .T. ) ;
#69404=STYLED_ITEM ( 'NONE', ( #41808 ), #83685 ) ;
#69405=VERTEX_POINT ( 'NONE', #79721 ) ;
#69426=( NAMED_UNIT ( * ) PLANE_ANGLE_UNIT ( ) SI_UNIT ( $, .RADIAN. ) );
#69450=CARTESIAN_POINT ( 'NONE',  ( -1.100699873904698034, 27.52274837490087478, 40.11352787695132349 ) ) ;
#69485=CARTESIAN_POINT ( 'NONE',  ( -23.21751746555244722, -1.200000000000000030E-05, 33.20617127781060418 ) ) ;
#69487=CARTESIAN_POINT ( 'NONE',  ( 0.1545845557741672149, 7.763550624989376203, -51.74245695911944409 ) ) ;
#69488=CARTESIAN_POINT ( 'NONE',  ( 17.37733725250692629, 36.93507598878604625, 21.96268678933276775 ) ) ;
#69544=AXIS2_PLACEMENT_3D ( 'NONE', #38297, #31270, #15038 ) ;
#69548=CARTESIAN_POINT ( 'NONE',  ( -30.04470542674692268, 7.904892719711607896, 42.05337092467510729 ) ) ;
#69550=STYLED_ITEM ( 'NONE', ( #59921 ), #52620 ) ;
#69567=ADVANCED_FACE ( 'NONE', ( #37115 ), #77000, .F. ) ;
#69568=ORIENTED_EDGE ( 'NONE', *, *, #49598, .F. ) ;
#69576=MECHANICAL_DESIGN_GEOMETRIC_PRESENTATION_REPRESENTATION('',(#86830),#85118);
#69591=SURFACE_SIDE_STYLE ('',( #60972 ) ) ;
#69601=CARTESIAN_POINT ( 'NONE',  ( 0.000000000000000000, 0.000000000000000000, 0.000000000000000000 ) ) ;
#69630=CARTESIAN_POINT ( 'NONE',  ( -16.48350313421780555, 45.65798623861609684, -6.657797401561613704 ) ) ;
#69636=CARTESIAN_POINT ( 'NONE',  ( -0.1682199022586588766, 46.21383923812595640, 16.24999999999999645 ) ) ;
#69643=CARTESIAN_POINT ( 'NONE',  ( 23.13430097919854944, 28.13531915807118367, 30.70617127781017786 ) ) ;
#69644=SURFACE_STYLE_USAGE ( .BOTH. , #45898 ) ;
#69670=CARTESIAN_POINT ( 'NONE',  ( -46.77788840983944141, 18.69141115048825696, 15.65052543522504891 ) ) ;
#69672=FILL_AREA_STYLE_COLOUR ( '', #29620 ) ;
#69673=CARTESIAN_POINT ( 'NONE',  ( 0.5330506804320168657, 13.17793295771842210, 51.63720770525478088 ) ) ;
#69676=VERTEX_POINT ( 'NONE', #88810 ) ;
#69705=CARTESIAN_POINT ( 'NONE',  ( -27.86245019093637154, 34.24933485205252026, 9.804843171747192443 ) ) ;
#69706=CARTESIAN_POINT ( 'NONE',  ( -0.1583024797166763253, 13.70447791526913939, -49.24999999999997158 ) ) ;
#69708=CARTESIAN_POINT ( 'NONE',  ( -18.00376551885552345, 36.46870192104549346, 23.09987717863819157 ) ) ;
#69712=CARTESIAN_POINT ( 'NONE',  ( 5.623709101673032507, 53.42003182002678585, -8.497490178355675994 ) ) ;
#69721=FILL_AREA_STYLE ('',( #63226 ) ) ;
#69732=EDGE_LOOP ( 'NONE', ( #76597, #103997, #97456, #102344 ) ) ;
#69743=DIRECTION ( 'NONE',  ( -0.000000000000000000, 1.000000000000000000, -0.000000000000000000 ) ) ;
#69762=CARTESIAN_POINT ( 'NONE',  ( -23.13495288362992852, 25.26989808490225542, -33.20617127781031996 ) ) ;
#69775=CARTESIAN_POINT ( 'NONE',  ( -10.61203977153288136, 46.03732009579939444, -12.94024766200783993 ) ) ;
#69783=ORIENTED_EDGE ( 'NONE', *, *, #43186, .T. ) ;
#69788=CARTESIAN_POINT ( 'NONE',  ( -17.85455871053495969, 34.57759917020306517, 22.38743647938886383 ) ) ;
#69793=CARTESIAN_POINT ( 'NONE',  ( 48.28084718957915555, 9.217476947337159388, -16.83779905917619502 ) ) ;
#69821=CARTESIAN_POINT ( 'NONE',  ( 0.8476627094018533981, 12.94087125257734350, 49.56336647345505497 ) ) ;
#69826=ORIENTED_EDGE ( 'NONE', *, *, #27995, .T. ) ;
#69827=CARTESIAN_POINT ( 'NONE',  ( -27.10511071441333542, 36.88665068479732412, -7.556984339679825524 ) ) ;
#69833=VECTOR ( 'NONE', #73812, 1000.000000000000000 ) ;
#69849=EDGE_CURVE ( 'NONE', #15839, #100346, #35304, .T. ) ;
#69881=SURFACE_STYLE_FILL_AREA ( #4085 ) ;
#69882=ORIENTED_EDGE ( 'NONE', *, *, #63996, .F. ) ;
#69888=EDGE_CURVE ( 'NONE', #101431, #41831, #27679, .T. ) ;
#69898=ORIENTED_EDGE ( 'NONE', *, *, #42692, .T. ) ;
#69913=( NAMED_UNIT ( * ) PLANE_ANGLE_UNIT ( ) SI_UNIT ( $, .RADIAN. ) );
#69917=CARTESIAN_POINT ( 'NONE',  ( 30.29801405241549261, 7.759806510565452342, 41.94638970127574851 ) ) ;
#69918=ORIENTED_EDGE ( 'NONE', *, *, #32974, .T. ) ;
#69922=MECHANICAL_DESIGN_GEOMETRIC_PRESENTATION_REPRESENTATION('',(#19985),#30278);
#69930=CARTESIAN_POINT ( 'NONE',  ( 28.49081357557730243, 13.12961590422140468, -40.46799408310457125 ) ) ;
#69933=CARTESIAN_POINT ( 'NONE',  ( -9.540582173716337877, 51.45292987738289270, 1.989850725143638810 ) ) ;
#69965=CARTESIAN_POINT ( 'NONE',  ( 29.68315524076926337, 8.302504244945327017, -42.10535821593530414 ) ) ;
#69967=PRESENTATION_STYLE_ASSIGNMENT (( #99668 ) ) ;
#69970=CARTESIAN_POINT ( 'NONE',  ( 1.010790367957777658, 37.02275760693545692, -27.74671416529730905 ) ) ;
#69971=STYLED_ITEM ( 'NONE', ( #24726 ), #64108 ) ;
#69996=CYLINDRICAL_SURFACE ( 'NONE', #41099, 1.250000000000000000 ) ;
#69999=FACE_BOUND ( 'NONE', #51937, .T. ) ;
#70012=CARTESIAN_POINT ( 'NONE',  ( 17.86230688873627415, 36.34004572609662631, 23.65428218925767112 ) ) ;
#70026=ORIENTED_EDGE ( 'NONE', *, *, #33895, .T. ) ;
#70041=AXIS2_PLACEMENT_3D ( 'NONE', #103759, #29896, #13673 ) ;
#70047=CARTESIAN_POINT ( 'NONE',  ( 15.67047892703660139, 36.78599904984204017, -23.70382416292494199 ) ) ;
#70064=CARTESIAN_POINT ( 'NONE',  ( -48.02835407290516656, 11.61227450977240494, 14.35535821593516559 ) ) ;
#70065=CARTESIAN_POINT ( 'NONE',  ( -15.56772955930216185, 46.04746595587302238, 6.065209611211459517 ) ) ;
#70094=ORIENTED_EDGE ( 'NONE', *, *, #19305, .F. ) ;
#70097=ORIENTED_EDGE ( 'NONE', *, *, #119, .F. ) ;
#70104=FACE_BOUND ( 'NONE', #39630, .T. ) ;
#70120=ORIENTED_EDGE ( 'NONE', *, *, #67679, .T. ) ;
#70126=CARTESIAN_POINT ( 'NONE',  ( 23.84332598391564062, 27.93368204320126225, 30.86206213703118451 ) ) ;
#70136=VECTOR ( 'NONE', #29029, 1000.000000000000000 ) ;
#70141=CARTESIAN_POINT ( 'NONE',  ( -30.48515219902031603, 12.91670175270527210, -41.81704193310824991 ) ) ;
#70160=CARTESIAN_POINT ( 'NONE',  ( -0.07795483430646524270, 13.70447791526909853, 49.25000000000002132 ) ) ;
#70166=CARTESIAN_POINT ( 'NONE',  ( -49.15082508851313037, 8.572194610415261096, -15.05005620232426722 ) ) ;
#70194=ORIENTED_EDGE ( 'NONE', *, *, #9265, .F. ) ;
#70198=SURFACE_STYLE_USAGE ( .BOTH. , #62651 ) ;
#70199=CARTESIAN_POINT ( 'NONE',  ( 16.64348903516523848, 43.47556584774768851, 6.657797401561421857 ) ) ;
#70201=ORIENTED_EDGE ( 'NONE', *, *, #62777, .T. ) ;
#70215=COLOUR_RGB ( '', 0.08235294, 0.09019608, 0.10196078) ;
#70228=CARTESIAN_POINT ( 'NONE',  ( -7.939867041329224939, 52.04605724232908415, -1.683498186040722544 ) ) ;
#70266=( GEOMETRIC_REPRESENTATION_CONTEXT ( 3 ) GLOBAL_UNCERTAINTY_ASSIGNED_CONTEXT ( ( #37350 ) ) GLOBAL_UNIT_ASSIGNED_CONTEXT ( ( #105788, #22783, #16246 ) ) REPRESENTATION_CONTEXT ( 'NONE', 'WORKASPACE' ) );
#70284=FACE_OUTER_BOUND ( 'NONE', #3500, .T. ) ;
#70315=SURFACE_STYLE_USAGE ( .BOTH. , #95131 ) ;
#70324=ORIENTED_EDGE ( 'NONE', *, *, #66217, .F. ) ;
#70350=CARTESIAN_POINT ( 'NONE',  ( 37.56673239365870387, 27.60449318992555945, 13.45617127780999134 ) ) ;
#70368=DIRECTION ( 'NONE',  ( -0.000000000000000000, 1.000000000000000000, -0.000000000000000000 ) ) ;
#70380=CARTESIAN_POINT ( 'NONE',  ( -8.559508646656370345, 53.96349637827587031, 1.531152949374564365 ) ) ;
#70391=CARTESIAN_POINT ( 'NONE',  ( 9.812601528912281879, 53.40226535921740236, -2.922597654565728398 ) ) ;
#70415=CARTESIAN_POINT ( 'NONE',  ( -29.68315524077005207, 13.12249633091091816, -39.60535821593474282 ) ) ;
#70432=ORIENTED_EDGE ( 'NONE', *, *, #8277, .T. ) ;
#70465=DIRECTION ( 'NONE',  ( -0.000000000000000000, 1.000000000000000000, -0.000000000000000000 ) ) ;
#70466=CARTESIAN_POINT ( 'NONE',  ( -9.807756029461570435, 51.30004223800749941, 2.674464121017646967 ) ) ;
#70492=CARTESIAN_POINT ( 'NONE',  ( 9.032162165387472186, 43.92599673635245949, 14.03290463794137999 ) ) ;
#70517=SURFACE_SIDE_STYLE ('',( #29047 ) ) ;
#70550=CARTESIAN_POINT ( 'NONE',  ( 17.07807050392529291, 37.03766137757074972, 21.83949354139796029 ) ) ;
#70600=CARTESIAN_POINT ( 'NONE',  ( -48.87659302348963308, 8.116727071898555579, 16.52478270335610944 ) ) ;
#70605=CARTESIAN_POINT ( 'NONE',  ( -30.63612296757520070, 10.92940684821784991, 40.03790167141636402 ) ) ;
#70617=CARTESIAN_POINT ( 'NONE',  ( -15.45459933393545704, 44.08658193089431165, -5.012668390913509242 ) ) ;
#70623=ORIENTED_EDGE ( 'NONE', *, *, #88646, .T. ) ;
#70633=FACE_BOUND ( 'NONE', #34139, .T. ) ;
#70659=CARTESIAN_POINT ( 'NONE',  ( 24.42523734047254891, 27.59258781593598542, 31.59665717925384243 ) ) ;
#70668=ORIENTED_EDGE ( 'NONE', *, *, #46495, .F. ) ;
#70671=CARTESIAN_POINT ( 'NONE',  ( -1.009927083827795835, 51.97655585224438113, 8.245822313973391715 ) ) ;
#70686=UNCERTAINTY_MEASURE_WITH_UNIT (LENGTH_MEASURE( 1.000000000000000082E-05 ), #101775, 'distance_accuracy_value', 'NONE');
#70689=ORIENTED_EDGE ( 'NONE', *, *, #102592, .F. ) ;
#70692=CARTESIAN_POINT ( 'NONE',  ( -0.3597357069889666747, 7.865396870477057156, 51.69868941200407164 ) ) ;
#70722=ORIENTED_EDGE ( 'NONE', *, *, #75458, .F. ) ;
#70725=CARTESIAN_POINT ( 'NONE',  ( 36.58643307874533690, 27.99658350115647565, 12.99814384291319769 ) ) ;
#70760=CARTESIAN_POINT ( 'NONE',  ( -17.51195277503164149, 36.87917477456677062, 22.05183216906712929 ) ) ;
#70769=DIRECTION ( 'NONE',  ( 0.000000000000000000, 0.000000000000000000, 1.000000000000000000 ) ) ;
#70770=( GEOMETRIC_REPRESENTATION_CONTEXT ( 3 ) GLOBAL_UNCERTAINTY_ASSIGNED_CONTEXT ( ( #36237 ) ) GLOBAL_UNIT_ASSIGNED_CONTEXT ( ( #84288, #69186, #93978 ) ) REPRESENTATION_CONTEXT ( 'NONE', 'WORKASPACE' ) );
#70801=CYLINDRICAL_SURFACE ( 'NONE', #81185, 24.55262289886175964 ) ;
#70841=CARTESIAN_POINT ( 'NONE',  ( 1.464720647026959308E-15, 47.77514352166374323, 11.96035173608223090 ) ) ;
#70842=( NAMED_UNIT ( * ) PLANE_ANGLE_UNIT ( ) SI_UNIT ( $, .RADIAN. ) );
#70884=ORIENTED_EDGE ( 'NONE', *, *, #79895, .T. ) ;
#70887=VECTOR ( 'NONE', #82478, 1000.000000000000000 ) ;
#70925=VECTOR ( 'NONE', #101506, 1000.000000000000000 ) ;
#70926=CARTESIAN_POINT ( 'NONE',  ( -15.98857071195793367, 36.61411899915854207, 24.05954505250353392 ) ) ;
#70937=ORIENTED_EDGE ( 'NONE', *, *, #82271, .F. ) ;
#70942=CARTESIAN_POINT ( 'NONE',  ( 23.97799606807651429, 27.87796489320410132, -30.95132209396242473 ) ) ;
#70943=ADVANCED_FACE ( 'NONE', ( #7359 ), #40271, .F. ) ;
#70972=CARTESIAN_POINT ( 'NONE',  ( 29.68315524077034340, 8.302504244945382084, 42.10535821593451544 ) ) ;
#70995=B_SPLINE_CURVE_WITH_KNOTS ( 'NONE', 3,
 ( #3246, #100863, #50696, #66922, #58833, #76582, #52313, #44241, #2155, #77129, #1621, #91728, #17846, #35108, #67455, #100332, #67975, #26497, #78703, #20557, #3781, #12904, #45831, #79246, #54956, #71153, #30185, #53392 ),
 .UNSPECIFIED., .F., .F.,
 ( 4, 2, 2, 2, 2, 2, 2, 2, 2, 2, 2, 2, 2, 4 ),
 ( 0.007813944516173556773, 0.008738276158831416451, 0.009662607801489277864, 0.01058693944414713928, 0.01151127108680499896, 0.01243560272946285863, 0.01289776855079178761, 0.01335993437212071658, 0.01382210019344964208, 0.01405318310411410830, 0.01428426601477857452, 0.01451534892544303901, 0.01474643183610750523, 0.01520859765743644634 ),
 .UNSPECIFIED. ) ;
#71009=CARTESIAN_POINT ( 'NONE',  ( 9.274304459112276078, 44.06289711030127165, 13.41925210190729345 ) ) ;
#71015=FACE_OUTER_BOUND ( 'NONE', #74948, .T. ) ;
#71066=CARTESIAN_POINT ( 'NONE',  ( 0.1555215442364585587, 13.68570359899996447, -49.25768108662912681 ) ) ;
#71067=STYLED_ITEM ( 'NONE', ( #27058 ), #53370 ) ;
#71068=CARTESIAN_POINT ( 'NONE',  ( 17.95946947111420045, 36.59397683629514830, 22.69701383365348590 ) ) ;
#71079=CARTESIAN_POINT ( 'NONE',  ( -0.1697044463282662841, 36.30024107553216339, 29.74999999999999645 ) ) ;
#71084=DIRECTION ( 'NONE',  ( -0.000000000000000000, 1.000000000000000000, -0.000000000000000000 ) ) ;
#71089=B_SPLINE_CURVE_WITH_KNOTS ( 'NONE', 3,
 ( #106738, #56588, #445, #80868, #8577, #65229, #6979, #57117, #50101, #81389, #98642, #40417, #24792, #73296, #41479, #90031, #57645, #39896, #16137, #90566, #16676, #91119, #33414, #9101 ),
 .UNSPECIFIED., .F., .F.,
 ( 4, 2, 2, 2, 2, 2, 2, 2, 2, 2, 2, 4 ),
 ( 0.007008940962998030239, 0.007512207565765160328, 0.008015474168532290417, 0.008518740771299420506, 0.008770374072682987285, 0.009022007374066552329, 0.009273640675450119109, 0.009525273976833684153, 0.01002854057960081424, 0.01028017388098438623, 0.01053180718236795821, 0.01103507378513509524 ),
 .UNSPECIFIED. ) ;
#71120=CARTESIAN_POINT ( 'NONE',  ( -49.15776748649652461, 8.563726824893079126, 15.04013919214055939 ) ) ;
#71125=CARTESIAN_POINT ( 'NONE',  ( -30.75967547141130609, 7.962001144779934592, 41.50359925574495179 ) ) ;
#71152=EDGE_LOOP ( 'NONE', ( #68503, #93775, #62735, #99625 ) ) ;
#71153=CARTESIAN_POINT ( 'NONE',  ( 29.87373162892120249, 8.058069557479617728, -42.09632259471328553 ) ) ;
#71173=CARTESIAN_POINT ( 'NONE',  ( 15.66258511614954507, 45.99742480776468057, -6.198981311147548467 ) ) ;
#71179=CYLINDRICAL_SURFACE ( 'NONE', #64900, 1.250000000000001110 ) ;
#71185=ORIENTED_EDGE ( 'NONE', *, *, #102503, .T. ) ;
#71189=CARTESIAN_POINT ( 'NONE',  ( -29.68315524077005207, 18.29184282782459547, -39.60535821593474282 ) ) ;
#71204=ORIENTED_EDGE ( 'NONE', *, *, #92479, .T. ) ;
#71207=CARTESIAN_POINT ( 'NONE',  ( -0.9601284218943312299, 8.766929892175371108, 51.31273321731734427 ) ) ;
#71218=CARTESIAN_POINT ( 'NONE',  ( 23.05203244996646106, 28.15092755562140425, 30.71439907890176357 ) ) ;
#71222=AXIS2_PLACEMENT_3D ( 'NONE', #29168, #11312, #101933 ) ;
#71238=CARTESIAN_POINT ( 'NONE',  ( 29.87369781377603317, 13.22774345441024302, -42.09617408282285567 ) ) ;
#71239=PRESENTATION_STYLE_ASSIGNMENT (( #36798 ) ) ;
#71247=CARTESIAN_POINT ( 'NONE',  ( 17.99627583047975676, 34.41216799978017349, 22.85523091777987759 ) ) ;
#71248=CARTESIAN_POINT ( 'NONE',  ( 26.10623851654674610, 35.05815521469033769, -8.037091760151625408 ) ) ;
#71255=AXIS2_PLACEMENT_3D ( 'NONE', #25525, #51340, #84253 ) ;
#71259=EDGE_CURVE ( 'NONE', #101681, #14947, #9447, .T. ) ;
#71287=CARTESIAN_POINT ( 'NONE',  ( 17.53752536966238651, 34.16832498362924753, -24.04387053720026657 ) ) ;
#71300=SURFACE_STYLE_USAGE ( .BOTH. , #24383 ) ;
#71319=CARTESIAN_POINT ( 'NONE',  ( 47.90320435033614643, 17.06740859345636352, -14.35535821593550665 ) ) ;
#71323=LINE ( 'NONE', #36881, #20659 ) ;
#71343=CARTESIAN_POINT ( 'NONE',  ( -48.28161701412196294, 14.38519811849624119, -16.83766359355620779 ) ) ;
#71350=FACE_BOUND ( 'NONE', #37317, .T. ) ;
#71355=DIRECTION ( 'NONE',  ( 0.000000000000000000, 0.000000000000000000, 1.000000000000000000 ) ) ;
#71361=SURFACE_STYLE_USAGE ( .BOTH. , #15254 ) ;
#71384=CARTESIAN_POINT ( 'NONE',  ( -36.94420904047371579, 25.95859750996718063, 11.10997783219646351 ) ) ;
#71403=DIRECTION ( 'NONE',  ( -0.000000000000000000, 1.000000000000000000, -0.000000000000000000 ) ) ;
#71405=CARTESIAN_POINT ( 'NONE',  ( 16.64348903516512834, 45.60392139269950462, -6.657797401561770911 ) ) ;
#71414=ORIENTED_EDGE ( 'NONE', *, *, #6733, .T. ) ;
#71440=VECTOR ( 'NONE', #11875, 1000.000000000000000 ) ;
#71441=SURFACE_STYLE_FILL_AREA ( #38068 ) ;
#71443=CARTESIAN_POINT ( 'NONE',  ( -15.49776003473001929, 37.05489105806098138, 22.93080861416538241 ) ) ;
#71446=AXIS2_PLACEMENT_3D ( 'NONE', #72031, #87166, #6213 ) ;
#71451=CARTESIAN_POINT ( 'NONE',  ( 25.85691572190012621, 37.17365521382656368, 8.914359746511365756 ) ) ;
#71453=B_SPLINE_CURVE_WITH_KNOTS ( 'NONE', 3,
 ( #47231, #7296, #38643, #81184, #56367, #31616, #72573, #105989, #13801, #14862, #6235, #6778, #39698, #7826, #96347, #104958, #80129, #55833, #96865, #40737, #88768, #47754, #24586, #48286, #64503, #22995, #88244, #48812, #63452, #73622 ),
 .UNSPECIFIED., .F., .F.,
 ( 4, 2, 2, 2, 2, 2, 2, 2, 2, 2, 2, 2, 2, 2, 4 ),
 ( 0.004426540215022530672, 0.005358602402234739076, 0.005824633495840844145, 0.006290664589446949215, 0.006523680136250001316, 0.006756695683053053417, 0.006989711229856105518, 0.007222726776659157619, 0.007455742323462209720, 0.007688757870265261821, 0.008154788963871379900, 0.009086851151083614325, 0.01001891333829584702, 0.01095097552550807971, 0.01188303771272031933 ),
 .UNSPECIFIED. ) ;
#71459=CARTESIAN_POINT ( 'NONE',  ( -24.41540814755808242, 25.25641607359507290, 32.32280296090762306 ) ) ;
#71463=FACE_OUTER_BOUND ( 'NONE', #82051, .T. ) ;
#71476=EDGE_CURVE ( 'NONE', #69405, #36646, #71323, .T. ) ;
#71484=DIRECTION ( 'NONE',  ( 1.150791560227848297E-16, -0.3420201433256725987, 0.9396926207859068736 ) ) ;
#71485=DIRECTION ( 'NONE',  ( -0.000000000000000000, 1.000000000000000000, -0.000000000000000000 ) ) ;
#71504=COLOUR_RGB ( '', 0.09019608, 0.27058824, 0.51372549) ;
#71529=CARTESIAN_POINT ( 'NONE',  ( -0.7860077071742745947, 25.26175349633248857, -40.48553591025817866 ) ) ;
#71546=CARTESIAN_POINT ( 'NONE',  ( 26.48397582124719207, 34.96050029299994577, 7.710214323866814823 ) ) ;
#71554=SURFACE_STYLE_USAGE ( .BOTH. , #70517 ) ;
#71560=ORIENTED_EDGE ( 'NONE', *, *, #6867, .T. ) ;
#71562=ORIENTED_EDGE ( 'NONE', *, *, #58649, .T. ) ;
#71583=CARTESIAN_POINT ( 'NONE',  ( 0.5289635065121225388, 13.43332938984680780, -49.36106157705717123 ) ) ;
#71586=CARTESIAN_POINT ( 'NONE',  ( 17.77153375527972301, 36.31766862386357531, 23.79949801963309142 ) ) ;
#71603=EDGE_LOOP ( 'NONE', ( #17712, #57240, #36461, #14283 ) ) ;
#71604=ORIENTED_EDGE ( 'NONE', *, *, #60022, .T. ) ;
#71630=DIRECTION ( 'NONE',  ( -0.000000000000000000, 1.000000000000000000, 0.000000000000000000 ) ) ;
#71636=CARTESIAN_POINT ( 'NONE',  ( -48.80588606933632434, 9.656672550839656921, 14.61916856843029144 ) ) ;
#71643=CARTESIAN_POINT ( 'NONE',  ( 28.45466774515011821, 11.90937068246397779, 41.11752270887368610 ) ) ;
#71655=CARTESIAN_POINT ( 'NONE',  ( -16.24848081785642506, 43.88994330808112920, -4.219092678288193454 ) ) ;
#71663=DIRECTION ( 'NONE',  ( 0.000000000000000000, 1.000000000000000000, -0.000000000000000000 ) ) ;
#71689=FILL_AREA_STYLE_COLOUR ( '', #34642 ) ;
#71695=FACE_OUTER_BOUND ( 'NONE', #10048, .T. ) ;
#71696=CARTESIAN_POINT ( 'NONE',  ( 0.1688296452888967958, 28.20649408426941562, -38.25000000000001421 ) ) ;
#71704=CARTESIAN_POINT ( 'NONE',  ( -30.10055902053746379, 13.03130292445769634, -42.03558690210238780 ) ) ;
#71714=CARTESIAN_POINT ( 'NONE',  ( 4.658343928564455894, 51.51306124665670438, -8.372077115008158543 ) ) ;
#71724=CARTESIAN_POINT ( 'NONE',  ( -0.9432067108799188082, 12.66774627894649363, 49.67605769803894589 ) ) ;
#71744=CARTESIAN_POINT ( 'NONE',  ( -16.75187969033532553, 34.99134772383131065, 21.80698433968612093 ) ) ;
#71765=ORIENTED_EDGE ( 'NONE', *, *, #642, .T. ) ;
#71773=ADVANCED_FACE ( 'NONE', ( #17360, #26019, #60488, #35694, #1670 ), #18937, .F. ) ;
#71776=CARTESIAN_POINT ( 'NONE',  ( 38.65303601453097571, 25.17668755055779428, 12.83022762705334330 ) ) ;
#71779=EDGE_CURVE ( 'NONE', #67879, #106068, #45400, .T. ) ;
#71783=CARTESIAN_POINT ( 'NONE',  ( -28.52992520858366632, 16.51490304376828178, -41.35306031657921011 ) ) ;
#71784=FACE_OUTER_BOUND ( 'NONE', #68442, .T. ) ;
#71798=EDGE_LOOP ( 'NONE', ( #70722, #61837, #63029, #10066 ) ) ;
#71803=SURFACE_STYLE_USAGE ( .BOTH. , #55603 ) ;
#71843=CARTESIAN_POINT ( 'NONE',  ( 11.30587238908012360, 45.32085087904604848, -14.90049756856787866 ) ) ;
#71846=FACE_OUTER_BOUND ( 'NONE', #47056, .T. ) ;
#71850=CARTESIAN_POINT ( 'NONE',  ( -5.615632394126207849, 54.12034592349190376, -6.063825715703227814 ) ) ;
#71876=CARTESIAN_POINT ( 'NONE',  ( -48.76802610285282924, 13.46002349908751050, -16.61772763643321582 ) ) ;
#71881=ADVANCED_FACE ( 'NONE', ( #53436 ), #103570, .F. ) ;
#71908=PRESENTATION_STYLE_ASSIGNMENT (( #6101 ) ) ;
#71914=CARTESIAN_POINT ( 'NONE',  ( 11.42604336269065612, 45.35830052782391419, 14.67759751612675423 ) ) ;
#71925=VECTOR ( 'NONE', #35852, 1000.000000000000000 ) ;
#71932=CARTESIAN_POINT ( 'NONE',  ( 4.650141638649412990, 52.18144075392523717, 6.194407870437166785 ) ) ;
#71986=CARTESIAN_POINT ( 'NONE',  ( -16.11174065067163852, 37.20923313995303516, 21.98001889856140068 ) ) ;
#71991=CARTESIAN_POINT ( 'NONE',  ( 0.8412457115897011839, 34.28465343340348426, 29.42821019032353291 ) ) ;
#71993=DIRECTION ( 'NONE',  ( 0.000000000000000000, 0.000000000000000000, 1.000000000000000000 ) ) ;
#72000=CARTESIAN_POINT ( 'NONE',  ( 23.86089617542257457, 27.29447341560884510, -33.04113357524870054 ) ) ;
#72023=AXIS2_PLACEMENT_3D ( 'NONE', #57330, #25010, #58955 ) ;
#72028=CARTESIAN_POINT ( 'NONE',  ( -37.24606932108090973, 27.99441749650426559, 10.98714381882859215 ) ) ;
#72031=CARTESIAN_POINT ( 'NONE',  ( 37.56673239365841255, -1.200000000000000030E-05, -12.20617127781092215 ) ) ;
#72058=PRESENTATION_STYLE_ASSIGNMENT (( #39177 ) ) ;
#72073=DIRECTION ( 'NONE',  ( 0.000000000000000000, 0.000000000000000000, 1.000000000000000000 ) ) ;
#72087=CARTESIAN_POINT ( 'NONE',  ( 25.97942814979532145, 35.07822400896434090, 8.256891463089578664 ) ) ;
#72094=CARTESIAN_POINT ( 'NONE',  ( -7.199040112754230057E-19, 54.30758622938872549, -7.749999999999999112 ) ) ;
#72116=LINE ( 'NONE', #42266, #6366 ) ;
#72126=( NAMED_UNIT ( * ) SI_UNIT ( $, .STERADIAN. ) SOLID_ANGLE_UNIT ( ) );
#72129=CARTESIAN_POINT ( 'NONE',  ( -1.235494359605229464, 15.32027490366484201, 50.72593522979114766 ) ) ;
#72151=VECTOR ( 'NONE', #25497, 1000.000000000000000 ) ;
#72185=ORIENTED_EDGE ( 'NONE', *, *, #19748, .T. ) ;
#72194=CARTESIAN_POINT ( 'NONE',  ( 28.94895647869510569, 13.71030094619077033, 39.84075445247401603 ) ) ;
#72196=CARTESIAN_POINT ( 'NONE',  ( 29.50183317260396265, 13.72085623994622061, 42.10535821593450123 ) ) ;
#72202=CARTESIAN_POINT ( 'NONE',  ( -15.55016539897052397, 44.07927076389781718, -4.778920582525040928 ) ) ;
#72203=CARTESIAN_POINT ( 'NONE',  ( -28.34313791092428758, 36.34626504971495109, -8.615479580127324510 ) ) ;
#72206=AXIS2_PLACEMENT_3D ( 'NONE', #25558, #67580, #26099 ) ;
#72226=DIRECTION ( 'NONE',  ( 0.000000000000000000, 0.000000000000000000, 1.000000000000000000 ) ) ;
#72227=CARTESIAN_POINT ( 'NONE',  ( -7.338578092433039046, 54.31146207452502495, -2.464013259436235614 ) ) ;
#72237=( LENGTH_UNIT ( ) NAMED_UNIT ( * ) SI_UNIT ( .MILLI., .METRE. ) );
#72244=CARTESIAN_POINT ( 'NONE',  ( -5.580966921651770022E-13, 25.16821295365027211, 40.75000000000505906 ) ) ;
#72245=CARTESIAN_POINT ( 'NONE',  ( 0.7835956671373057736, 28.10810970921148311, -38.51249778524339717 ) ) ;
#72257=CARTESIAN_POINT ( 'NONE',  ( -16.83450711267213151, 34.23838129605825742, -24.30698433968598238 ) ) ;
#72323=CARTESIAN_POINT ( 'NONE',  ( 38.81340407398939618, 25.21178748735488284, 12.01518403244543087 ) ) ;
#72329=CARTESIAN_POINT ( 'NONE',  ( -28.58272191126927098, 16.23375075743840412, -41.45992959583551851 ) ) ;
#72363=FACE_OUTER_BOUND ( 'NONE', #40307, .T. ) ;
#72408=DIRECTION ( 'NONE',  ( -0.000000000000000000, -1.000000000000000000, -0.000000000000000000 ) ) ;
#72412=CARTESIAN_POINT ( 'NONE',  ( -49.10072971674536291, 12.98664841672704107, -16.25083509557213191 ) ) ;
#72426=CARTESIAN_POINT ( 'NONE',  ( 2.761899744546835519E-15, 36.79151656018385097, 22.55262289886175964 ) ) ;
#72432=ORIENTED_EDGE ( 'NONE', *, *, #96963, .F. ) ;
#72438=CARTESIAN_POINT ( 'NONE',  ( -37.72546545933433748, 27.83008492337310358, -10.95617127781036437 ) ) ;
#72441=CARTESIAN_POINT ( 'NONE',  ( -1.231024308828225999, 16.45180670219713903, -50.25114264119800822 ) ) ;
#72459=CARTESIAN_POINT ( 'NONE',  ( 38.81959903812767720, 27.30122739460367853, 12.35248524812892512 ) ) ;
#72485=ORIENTED_EDGE ( 'NONE', *, *, #17490, .T. ) ;
#72496=CARTESIAN_POINT ( 'NONE',  ( -22.59067934059571314, 27.55769764751302020, 33.04957285560292490 ) ) ;
#72519=EDGE_CURVE ( 'NONE', #65856, #104203, #38476, .T. ) ;
#72525=CARTESIAN_POINT ( 'NONE',  ( -23.21751746555244722, 25.25267828308493634, 33.20617127781060418 ) ) ;
#72530=CARTESIAN_POINT ( 'NONE',  ( 1.255263095696489281E-15, 51.26930509877138320, 10.24999999999999822 ) ) ;
#72542=CARTESIAN_POINT ( 'NONE',  ( 48.02835407290504577, 9.771516447483525880, -16.85535821593549954 ) ) ;
#72573=CARTESIAN_POINT ( 'NONE',  ( 47.29386731606080474, 18.29473622528960064, 14.58939859131256256 ) ) ;
#72584=ORIENTED_EDGE ( 'NONE', *, *, #29950, .T. ) ;
#72622=CARTESIAN_POINT ( 'NONE',  ( -1.103649760378013100, 53.60830983912105552, -9.608372721927825211 ) ) ;
#72649=CARTESIAN_POINT ( 'NONE',  ( 0.7827249903936659425, 54.19856013892794522, -8.012020349616371107 ) ) ;
#72653=CARTESIAN_POINT ( 'NONE',  ( -7.980179952708205483E-13, 34.17188553057791722, -29.75000000000694911 ) ) ;
#72655=SURFACE_STYLE_USAGE ( .BOTH. , #24147 ) ;
#72661=CARTESIAN_POINT ( 'NONE',  ( -16.75187969033554936, 37.11970326878314097, -21.80698433968595751 ) ) ;
#72673=CARTESIAN_POINT ( 'NONE',  ( 22.89018779209756005, 25.33046591275928705, 33.17343505111048074 ) ) ;
#72675=ORIENTED_EDGE ( 'NONE', *, *, #75429, .T. ) ;
#72684=CARTESIAN_POINT ( 'NONE',  ( 1.625879232102889239E-15, 52.29617335651133914, 13.27631144943088692 ) ) ;
#72698=CARTESIAN_POINT ( 'NONE',  ( -29.68315524077004852, -1.200000000000000030E-05, -42.10535821593474282 ) ) ;
#72703=( LENGTH_UNIT ( ) NAMED_UNIT ( * ) SI_UNIT ( .MILLI., .METRE. ) );
#72711=CARTESIAN_POINT ( 'NONE',  ( 28.61324058441463336, 13.48935699407724265, 40.19649855359969592 ) ) ;
#72713=CARTESIAN_POINT ( 'NONE',  ( 29.32938745888697696, 18.70033273455120693, 39.65510828929031817 ) ) ;
#72727=EDGE_CURVE ( 'NONE', #52295, #80390, #14208, .T. ) ;
#72729=EDGE_CURVE ( 'NONE', #34601, #36282, #33375, .T. ) ;
#72742=CARTESIAN_POINT ( 'NONE',  ( -16.64348903516517098, 45.88445698070336221, 4.157797401561652784 ) ) ;
#72745=ORIENTED_EDGE ( 'NONE', *, *, #85967, .F. ) ;
#72751=EDGE_LOOP ( 'NONE', ( #58758, #14631 ) ) ;
#72771=CARTESIAN_POINT ( 'NONE',  ( -17.08050361159542874, 34.19939120091158458, -24.26590151447872401 ) ) ;
#72773=CARTESIAN_POINT ( 'NONE',  ( 48.99295625602575655, 13.11026251878881688, 16.41069188772014087 ) ) ;
#72792=CARTESIAN_POINT ( 'NONE',  ( 27.72754708733857854, 34.28370776901574857, -9.903118175739001217 ) ) ;
#72798=CARTESIAN_POINT ( 'NONE',  ( 22.10829536976860510, 28.16405687208418485, 31.35662012625468265 ) ) ;
#72824=CARTESIAN_POINT ( 'NONE',  ( 37.24697956223116080, 27.99412332198319220, 10.98691340867259036 ) ) ;
#72834=CIRCLE ( 'NONE', #100329, 13.27631144943088515 ) ;
#72836=CARTESIAN_POINT ( 'NONE',  ( 0.1683002306914084256, 26.07813853931758530, 38.24999999999999289 ) ) ;
#72843=CARTESIAN_POINT ( 'NONE',  ( 23.38262301493118756, 25.94998521817065651, 30.71445628890077373 ) ) ;
#72859=UNCERTAINTY_MEASURE_WITH_UNIT (LENGTH_MEASURE( 1.000000000000000082E-05 ), #77263, 'distance_accuracy_value', 'NONE');
#72862=CARTESIAN_POINT ( 'NONE',  ( 29.49662366984231454, 18.54149253525968533, -39.61409757040036084 ) ) ;
#72870=CYLINDRICAL_SURFACE ( 'NONE', #29845, 1.250000000000001110 ) ;
#72876=FACE_BOUND ( 'NONE', #67658, .T. ) ;
#72878=CYLINDRICAL_SURFACE ( 'NONE', #21822, 22.55262289886175964 ) ;
#72879=DIRECTION ( 'NONE',  ( 0.000000000000000000, -0.3420201433256725987, -0.9396926207859068736 ) ) ;
#72884=ORIENTED_EDGE ( 'NONE', *, *, #78990, .F. ) ;
#72894=CARTESIAN_POINT ( 'NONE',  ( 10.61653353389823984, 45.33051817006433026, -15.36625836153913127 ) ) ;
#72944=( NAMED_UNIT ( * ) SI_UNIT ( $, .STERADIAN. ) SOLID_ANGLE_UNIT ( ) );
#72952=CARTESIAN_POINT ( 'NONE',  ( -38.74274399182664297, 27.39031700910832967, -11.77456647869184359 ) ) ;
#72956=CARTESIAN_POINT ( 'NONE',  ( -0.5328921654508612660, 13.17767128240470065, -51.63731992219727118 ) ) ;
#72958=DIRECTION ( 'NONE',  ( 0.000000000000000000, 0.000000000000000000, 1.000000000000000000 ) ) ;
#72976=CARTESIAN_POINT ( 'NONE',  ( 48.98943663899292744, 7.951733423214422558, 16.40652009737647887 ) ) ;
#72982=EDGE_CURVE ( 'NONE', #93975, #79044, #10389, .T. ) ;
#72988=CARTESIAN_POINT ( 'NONE',  ( -9.797648506390736145, 51.31151531669312504, -2.590383122573969299 ) ) ;
#73035=CARTESIAN_POINT ( 'NONE',  ( 23.84378987346994805, 27.93349636785022483, -30.86234801138825645 ) ) ;
#73036=ORIENTED_EDGE ( 'NONE', *, *, #93374, .F. ) ;
#73039=CARTESIAN_POINT ( 'NONE',  ( 0.4137165646001804142, 52.15082680420621841, 7.817459332776711456 ) ) ;
#73047=CARTESIAN_POINT ( 'NONE',  ( 23.21751746555220564, 25.25267828308493634, -33.20617127781077471 ) ) ;
#73051=CARTESIAN_POINT ( 'NONE',  ( 46.92658635379572729, 13.66002169525850007, -15.01004073971110486 ) ) ;
#73054=B_SPLINE_CURVE_WITH_KNOTS ( 'NONE', 3,
 ( #39243, #5788, #105546, #31684, #80198, #64570, #6845, #14391, #39769, #55901, #73157, #96415, #97437, #47303, #89379, #88837, #23062, #6303, #31167, #32209 ),
 .UNSPECIFIED., .F., .F.,
 ( 4, 2, 2, 2, 2, 2, 2, 2, 2, 4 ),
 ( 0.003321483407199190673, 0.003825559474142698705, 0.004077597507614457058, 0.004329635541086214977, 0.004833711608029716070, 0.005337787674973218030, 0.005841863741916719990, 0.006345939808860221951, 0.006850015875803723911, 0.007354091942747225871 ),
 .UNSPECIFIED. ) ;
#73064=CARTESIAN_POINT ( 'NONE',  ( -2.637755229554568666E-21, 53.39766064372320642, -10.24999999999999822 ) ) ;
#73066=CARTESIAN_POINT ( 'NONE',  ( 30.88008372391074730, 8.315965929874641560, 41.22858563418517264 ) ) ;
#73067=ORIENTED_EDGE ( 'NONE', *, *, #44818, .F. ) ;
#73099=CARTESIAN_POINT ( 'NONE',  ( -9.306508628549350348, 53.68076281443192954, 1.765973350150533916 ) ) ;
#73106=CARTESIAN_POINT ( 'NONE',  ( 29.68315524077034695, -1.200000000000000030E-05, 39.60535821593451544 ) ) ;
#73110=STYLED_ITEM ( 'NONE', ( #99431 ), #42019 ) ;
#73112=CARTESIAN_POINT ( 'NONE',  ( 6.400188988269344570, 53.43406968874433716, 7.879101709558080202 ) ) ;
#73145=FILL_AREA_STYLE_COLOUR ( '', #17303 ) ;
#73150=PRODUCT_DEFINITION_FORMATION_WITH_SPECIFIED_SOURCE ( 'ANY', '', #79411, .NOT_KNOWN. ) ;
#73157=CARTESIAN_POINT ( 'NONE',  ( 1.250014052124106323, 25.67358186333530767, -39.34165713028683342 ) ) ;
#73160=DIRECTION ( 'NONE',  ( 0.000000000000000000, 0.000000000000000000, 1.000000000000000000 ) ) ;
#73161=CARTESIAN_POINT ( 'NONE',  ( 1.008786712439213362, 54.10551997402946256, -8.244280760490370952 ) ) ;
#73171=CARTESIAN_POINT ( 'NONE',  ( -16.66870162890457863, 37.13814613750710691, -21.80698433968596106 ) ) ;
#73172=ORIENTED_EDGE ( 'NONE', *, *, #103942, .T. ) ;
#73182=ORIENTED_EDGE ( 'NONE', *, *, #40207, .F. ) ;
#73187=( LENGTH_UNIT ( ) NAMED_UNIT ( * ) SI_UNIT ( .MILLI., .METRE. ) );
#73188=EDGE_CURVE ( 'NONE', #93736, #68089, #49614, .T. ) ;
#73198=( GEOMETRIC_REPRESENTATION_CONTEXT ( 3 ) GLOBAL_UNCERTAINTY_ASSIGNED_CONTEXT ( ( #23482 ) ) GLOBAL_UNIT_ASSIGNED_CONTEXT ( ( #79981, #7154, #72944 ) ) REPRESENTATION_CONTEXT ( 'NONE', 'WORKASPACE' ) );
#73239=CARTESIAN_POINT ( 'NONE',  ( -27.10511071441333542, 36.88665068479732412, -7.556984339679825524 ) ) ;
#73241=CARTESIAN_POINT ( 'NONE',  ( 0.000000000000000000, 0.000000000000000000, -55.00000000000000000 ) ) ;
#73266=FILL_AREA_STYLE ('',( #40385 ) ) ;
#73268=EDGE_CURVE ( 'NONE', #78054, #93975, #55565, .T. ) ;
#73277=CARTESIAN_POINT ( 'NONE',  ( -29.68315524077004852, -1.200000000000000030E-05, -40.85535821593474282 ) ) ;
#73294=CARTESIAN_POINT ( 'NONE',  ( -0.1688158579390501568, 51.27205306785339900, 10.24139233105815272 ) ) ;
#73296=CARTESIAN_POINT ( 'NONE',  ( -17.85751735367976067, 43.17548293752579980, 5.717193597672930672 ) ) ;
#73313=CARTESIAN_POINT ( 'NONE',  ( 9.307407628962446111, 51.55202669552782169, 1.766814834372365306 ) ) ;
#73318=CARTESIAN_POINT ( 'NONE',  ( 28.04563069813499254, 34.20672709930742883, -9.634527181935203188 ) ) ;
#73324=CARTESIAN_POINT ( 'NONE',  ( 22.43989698835544999, 28.20716416251315906, 30.97385700653301299 ) ) ;
#73355=CARTESIAN_POINT ( 'NONE',  ( 26.78474689927651653, 34.86756896202341238, -7.587912695338806301 ) ) ;
#73357=DIRECTION ( 'NONE',  ( -0.000000000000000000, 1.000000000000000000, -0.000000000000000000 ) ) ;
#73363=CARTESIAN_POINT ( 'NONE',  ( 0.7841136692415845433, 25.26116217180792489, 40.48719991889687719 ) ) ;
#73369=LINE ( 'NONE', #22221, #34580 ) ;
#73377=EDGE_CURVE ( 'NONE', #59035, #68982, #27274, .T. ) ;
#73405=FACE_OUTER_BOUND ( 'NONE', #85995, .T. ) ;
#73440=SURFACE_STYLE_FILL_AREA ( #1678 ) ;
#73471=CARTESIAN_POINT ( 'NONE',  ( -22.89193641261722689, 27.46073252125954411, -33.16577871831040625 ) ) ;
#73482=CARTESIAN_POINT ( 'NONE',  ( -37.88389991164935111, 27.77159677234703494, -10.98672745669020401 ) ) ;
#73483=ORIENTED_EDGE ( 'NONE', *, *, #36108, .F. ) ;
#73506=SHAPE_DEFINITION_REPRESENTATION ( #68139, #38413 ) ;
#73507=CARTESIAN_POINT ( 'NONE',  ( 48.15203510316958813, 9.493368196138895598, 16.85535821593427386 ) ) ;
#73516=CARTESIAN_POINT ( 'NONE',  ( -26.47069814182328784, 36.83824913210050767, -9.930511453896439633 ) ) ;
#73519=CARTESIAN_POINT ( 'NONE',  ( -9.306959991822290945, 51.55220751856156625, -1.766502984829542600 ) ) ;
#73524=EDGE_CURVE ( 'NONE', #32665, #85099, #87846, .T. ) ;
#73532=CARTESIAN_POINT ( 'NONE',  ( 37.56673239365841255, 27.88554838446202311, -10.95617127781092037 ) ) ;
#73551=CARTESIAN_POINT ( 'NONE',  ( 27.10511071441204578, 34.75829513984540142, 7.556984339685363317 ) ) ;
#73557=EDGE_CURVE ( 'NONE', #68982, #13191, #104005, .T. ) ;
#73577=VECTOR ( 'NONE', #70368, 1000.000000000000000 ) ;
#73582=CARTESIAN_POINT ( 'NONE',  ( 1.218732506510818103, 45.85998149243336286, 17.17911318258725117 ) ) ;
#73586=CARTESIAN_POINT ( 'NONE',  ( -11.07233799575505628, 45.30046846812411587, -15.14426123305350558 ) ) ;
#73606=CARTESIAN_POINT ( 'NONE',  ( 30.48935137155323716, 7.748232456196025630, 41.81352479775706854 ) ) ;
#73607=VERTEX_POINT ( 'NONE', #46839 ) ;
#73609=CARTESIAN_POINT ( 'NONE',  ( 9.734943007948952953, 51.35523771563250506, -2.348059683008551612 ) ) ;
#73622=CARTESIAN_POINT ( 'NONE',  ( 48.02835407290544367, 14.94086294439726892, 16.85535821593427386 ) ) ;
#73648=CARTESIAN_POINT ( 'NONE',  ( -4.237512335919120849E-14, 43.17555810750860701, 18.75000000000000355 ) ) ;
#73665=CARTESIAN_POINT ( 'NONE',  ( -8.559508646656370345, 53.68473964988125857, 4.031152949374564365 ) ) ;
#73670=CARTESIAN_POINT ( 'NONE',  ( 16.11128504972181119, 35.08385997426073288, 21.97063235475975063 ) ) ;
#73693=CARTESIAN_POINT ( 'NONE',  ( 9.721734870800576189, 46.20860777233757233, 13.03934063175024605 ) ) ;
#73705=AXIS2_PLACEMENT_3D ( 'NONE', #10060, #16562, #65646 ) ;
#73707=CARTESIAN_POINT ( 'NONE',  ( -0.7862528207961816396, 34.26448653555612367, -29.48533061255973564 ) ) ;
#73720=CARTESIAN_POINT ( 'NONE',  ( 23.38236582681999920, 25.21829724408700812, -33.20617127781077471 ) ) ;
#73771=FILL_AREA_STYLE_COLOUR ( '', #13132 ) ;
#73777=DIRECTION ( 'NONE',  ( 0.000000000000000000, 0.000000000000000000, -1.000000000000000000 ) ) ;
#73780=CARTESIAN_POINT ( 'NONE',  ( -28.43341640144473814, 17.76796145515719516, 40.78017990900028877 ) ) ;
#73783=CARTESIAN_POINT ( 'NONE',  ( -21.97265383647320292, 25.82522707506753790, 32.15451870283014557 ) ) ;
#73800=CARTESIAN_POINT ( 'NONE',  ( -25.89634907308706246, 35.00173212496974884, 9.164867755282383399 ) ) ;
#73803=ADVANCED_FACE ( 'NONE', ( #31228 ), #64116, .F. ) ;
#73812=DIRECTION ( 'NONE',  ( -0.000000000000000000, 1.000000000000000000, 0.000000000000000000 ) ) ;
#73813=CARTESIAN_POINT ( 'NONE',  ( -46.86248696599245989, 13.70470512780033978, 15.14813956650301385 ) ) ;
#73815=ORIENTED_EDGE ( 'NONE', *, *, #47989, .T. ) ;
#73821=CARTESIAN_POINT ( 'NONE',  ( 10.28624191511809371, -1.200000000000000030E-05, -14.15779740156171584 ) ) ;
#73823=CARTESIAN_POINT ( 'NONE',  ( 15.42941528477435398, 46.21391461311947779, -5.098611828030635174 ) ) ;
#73825=VECTOR ( 'NONE', #1074, 1000.000000000000000 ) ;
#73829=CARTESIAN_POINT ( 'NONE',  ( -29.68315524076957246, 18.29184282782463455, 39.60535821593508388 ) ) ;
#73831=CARTESIAN_POINT ( 'NONE',  ( 1.130019378125521223, 27.54905683648467729, -40.04036428441008155 ) ) ;
#73847=CARTESIAN_POINT ( 'NONE',  ( -6.309776332879510896, 51.28523556860736221, -8.023844445462220420 ) ) ;
#73851=CARTESIAN_POINT ( 'NONE',  ( -10.92836421268331293, 43.17363766063942165, -15.24329784724702996 ) ) ;
#73852=CARTESIAN_POINT ( 'NONE',  ( -28.94979900162252662, 13.71034195483037443, 39.84012157007414601 ) ) ;
#73859=CARTESIAN_POINT ( 'NONE',  ( 36.31383080563109189, 28.20116312085306731, -12.06289833560200009 ) ) ;
#73869=CARTESIAN_POINT ( 'NONE',  ( 21.99817791066577044, 28.09376123749147069, 31.66916887880059761 ) ) ;
#73875=ORIENTED_EDGE ( 'NONE', *, *, #52200, .F. ) ;
#73881=CARTESIAN_POINT ( 'NONE',  ( -4.278209688530829169, 54.28328794773042176, 6.542503565097912421 ) ) ;
#73883=CARTESIAN_POINT ( 'NONE',  ( -37.56673239365863282, 25.75719283951018568, -10.95617127781023648 ) ) ;
#73886=DIRECTION ( 'NONE',  ( 0.000000000000000000, 0.000000000000000000, -1.000000000000000000 ) ) ;
#73895=EDGE_LOOP ( 'NONE', ( #59711, #106002, #547, #72745 ) ) ;
#73899=FILL_AREA_STYLE ('',( #81983 ) ) ;
#73912=CARTESIAN_POINT ( 'NONE',  ( 23.30083868525793278, 25.23530067567654811, 33.20617127781017786 ) ) ;
#73917=VERTEX_POINT ( 'NONE', #84537 ) ;
#73920=CARTESIAN_POINT ( 'NONE',  ( -4.880198815736334517, 52.15761557286078443, 6.097275048993607172 ) ) ;
#73937=SURFACE_STYLE_FILL_AREA ( #97679 ) ;
#73970=CARTESIAN_POINT ( 'NONE',  ( 17.77044000761073050, 43.17862937570248505, -5.955230444982646532 ) ) ;
#73971=CARTESIAN_POINT ( 'NONE',  ( -5.934175881463731095, 53.39571318504778219, -8.365722538783465723 ) ) ;
#74015=ORIENTED_EDGE ( 'NONE', *, *, #54674, .F. ) ;
#74029=CYLINDRICAL_SURFACE ( 'NONE', #89858, 33.82893434829263413 ) ;
#74043=LINE ( 'NONE', #97787, #52859 ) ;
#74045=CARTESIAN_POINT ( 'NONE',  ( 48.80467726777884252, 9.660151405757227749, 14.61811727277425987 ) ) ;
#74057=CARTESIAN_POINT ( 'NONE',  ( 36.44116660230073990, 26.07456738169941701, 11.65597035723753372 ) ) ;
#74089=CARTESIAN_POINT ( 'NONE',  ( 28.18166793234509981, 34.32241243842408807, 8.150798923637601945 ) ) ;
#74105=CARTESIAN_POINT ( 'NONE',  ( -4.959638304640701101, 51.41909874265953562, -8.497456494351391498 ) ) ;
#74107=CARTESIAN_POINT ( 'NONE',  ( -0.1552019576139205825, 18.85513881606577158, 49.25764478663058554 ) ) ;
#74120=CARTESIAN_POINT ( 'NONE',  ( -9.076853247125740154, 45.89842957983099581, 14.51167170299874520 ) ) ;
#74133=CARTESIAN_POINT ( 'NONE',  ( -37.56673239365971284, 27.88554838446211548, -10.95617127780556466 ) ) ;
#74140=CARTESIAN_POINT ( 'NONE',  ( -9.184438934625386963, 44.03862627902407922, 13.56153005510785725 ) ) ;
#74145=AXIS2_PLACEMENT_3D ( 'NONE', #63075, #46358, #103527 ) ;
#74150=VERTEX_POINT ( 'NONE', #46199 ) ;
#74157=CARTESIAN_POINT ( 'NONE',  ( 10.28624191511840458, 43.99263840937192782, 12.90779740156148847 ) ) ;
#74178=CARTESIAN_POINT ( 'NONE',  ( -0.1694831974862292256, 26.07487419649228855, -38.25868201985088035 ) ) ;
#74179=CARTESIAN_POINT ( 'NONE',  ( -8.559508646656370345, 53.68473964988125857, 4.031152949374564365 ) ) ;
#74187=CARTESIAN_POINT ( 'NONE',  ( 0.8408997231841593978, 45.41398511527192738, -18.42850300921338658 ) ) ;
#74191=CARTESIAN_POINT ( 'NONE',  ( 29.77292113577873423, 13.34857726707554448, 42.10535821593450834 ) ) ;
#74224=CARTESIAN_POINT ( 'NONE',  ( 9.960122430517651893, 45.46309208840076366, 15.36726729605906527 ) ) ;
#74238=CARTESIAN_POINT ( 'NONE',  ( 0.4147425415936616955, 54.27900644350521020, -7.817881304308153645 ) ) ;
#74250=ORIENTED_EDGE ( 'NONE', *, *, #97134, .T. ) ;
#74254=CARTESIAN_POINT ( 'NONE',  ( 47.90305809253377589, 10.05329658600983400, 16.85535821593427386 ) ) ;
#74263=ORIENTED_EDGE ( 'NONE', *, *, #23247, .T. ) ;
#74280=CARTESIAN_POINT ( 'NONE',  ( -28.35805569942980497, 34.17680034679604262, -8.950141237612221801 ) ) ;
#74304=COLOUR_RGB ( '', 0.66274510, 0.83137255, 0.94901961) ;
#74306=CARTESIAN_POINT ( 'NONE',  ( 28.43253669899775815, 17.35855320307317129, 40.99008157358971971 ) ) ;
#74314=CARTESIAN_POINT ( 'NONE',  ( -28.58254312158966570, 16.23466659877849949, 41.45958612840279045 ) ) ;
#74330=( NAMED_UNIT ( * ) SI_UNIT ( $, .STERADIAN. ) SOLID_ANGLE_UNIT ( ) );
#74332=CARTESIAN_POINT ( 'NONE',  ( -26.48318267654033420, 34.96074735818669410, 7.710518002484812783 ) ) ;
#74341=CARTESIAN_POINT ( 'NONE',  ( -17.26536970378605318, 45.41327343741740918, 6.504208684746012104 ) ) ;
#74354=CARTESIAN_POINT ( 'NONE',  ( -30.87964800539037569, 13.48323453669521044, 41.23000148635482276 ) ) ;
#74361=ORIENTED_EDGE ( 'NONE', *, *, #12747, .F. ) ;
#74366=CARTESIAN_POINT ( 'NONE',  ( -17.99616949565368174, 34.41190775537305768, -22.85621917946001247 ) ) ;
#74375=CARTESIAN_POINT ( 'NONE',  ( 8.559508646656405872, 51.55638410492942825, 4.031152949374444461 ) ) ;
#74377=LINE ( 'NONE', #66839, #48409 ) ;
#74383=CARTESIAN_POINT ( 'NONE',  ( 36.32007205877684441, 28.16029012736642656, -12.39624372369306293 ) ) ;
#74392=FACE_OUTER_BOUND ( 'NONE', #397, .T. ) ;
#74405=EDGE_CURVE ( 'NONE', #100497, #34913, #19268, .T. ) ;
#74415=AXIS2_PLACEMENT_3D ( 'NONE', #22378, #39072, #46096 ) ;
#74421=VERTEX_POINT ( 'NONE', #60155 ) ;
#74439=VECTOR ( 'NONE', #48556, 1000.000000000000000 ) ;
#74444=CARTESIAN_POINT ( 'NONE',  ( 4.298171162025412606, 53.80428045674285187, 8.058306618997294279 ) ) ;
#74496=CARTESIAN_POINT ( 'NONE',  ( -10.36871714652622245, 45.36883139708662327, 15.40779740156165367 ) ) ;
#74498=CARTESIAN_POINT ( 'NONE',  ( 0.000000000000000000, 1.999999999999998224, 0.000000000000000000 ) ) ;
#74506=LINE ( 'NONE', #58332, #2010 ) ;
#74514=SURFACE_STYLE_USAGE ( .BOTH. , #98267 ) ;
#74524=LINE ( 'NONE', #68037, #67016 ) ;
#74528=CARTESIAN_POINT ( 'NONE',  ( 16.64348903516499334, 45.60392139269944067, 6.657797401562596917 ) ) ;
#74538=CARTESIAN_POINT ( 'NONE',  ( 26.49205890517669104, 36.83376193817070288, -9.907811712491993106 ) ) ;
#74540=FILL_AREA_STYLE_COLOUR ( '', #48346 ) ;
#74545=CARTESIAN_POINT ( 'NONE',  ( 16.75187969033515145, 37.11970326878314808, -21.80698433968624528 ) ) ;
#74555=CARTESIAN_POINT ( 'NONE',  ( -47.01788285976065396, 17.61616053603705723, 16.34433538609877345 ) ) ;
#74556=EDGE_CURVE ( 'NONE', #46369, #49037, #16834, .T. ) ;
#74557=CARTESIAN_POINT ( 'NONE',  ( 38.18871050945294598, 27.40971527590679102, -13.30253190289822918 ) ) ;
#74577=CARTESIAN_POINT ( 'NONE',  ( 0.7821289637610407963, 43.98379635595578208, 16.51122116237588244 ) ) ;
#74599=ORIENTED_EDGE ( 'NONE', *, *, #67679, .F. ) ;
#74600=CARTESIAN_POINT ( 'NONE',  ( -23.21751746555280249, 25.98869614573808207, -30.70617127781034839 ) ) ;
#74616=ORIENTED_EDGE ( 'NONE', *, *, #75268, .F. ) ;
#74619=FACE_BOUND ( 'NONE', #50863, .T. ) ;
#74645=CARTESIAN_POINT ( 'NONE',  ( 0.3334994693927795795, 45.31831760051831282, 18.70763632781319075 ) ) ;
#74647=VERTEX_POINT ( 'NONE', #85075 ) ;
#74649=CARTESIAN_POINT ( 'NONE',  ( -9.646320399536650214, 46.21287003049852871, 13.08069908581821572 ) ) ;
#74652=CARTESIAN_POINT ( 'NONE',  ( -46.96293930799764382, 18.79139706470984805, -14.94845605815084255 ) ) ;
#74655=ORIENTED_EDGE ( 'NONE', *, *, #37418, .T. ) ;
#74673=ORIENTED_EDGE ( 'NONE', *, *, #77233, .F. ) ;
#74687=CARTESIAN_POINT ( 'NONE',  ( 0.000000000000000000, 0.000000000000000000, 22.55262289886175964 ) ) ;
#74706=CARTESIAN_POINT ( 'NONE',  ( 38.81316105428458485, 25.21210130169110641, -12.01306034898426844 ) ) ;
#74708=CARTESIAN_POINT ( 'NONE',  ( -0.7769499151835902451, 25.97800031865995862, -38.51735009866241910 ) ) ;
#74712=CARTESIAN_POINT ( 'NONE',  ( -0.08530053327169842547, 43.17555810750862122, 18.75000000000000000 ) ) ;
#74716=CARTESIAN_POINT ( 'NONE',  ( 5.456272071277679991, 53.44287117986112889, 8.531152949374478212 ) ) ;
#74739=FILL_AREA_STYLE ('',( #65603 ) ) ;
#74753=CARTESIAN_POINT ( 'NONE',  ( 9.648094638230904962, 46.21279293231379626, 13.07965317076976319 ) ) ;
#74768=CARTESIAN_POINT ( 'NONE',  ( 7.800296835061319989, 54.21723526805532600, 1.774124769967747595 ) ) ;
#74781=CARTESIAN_POINT ( 'NONE',  ( 24.46392420078501218, 25.31575836906371890, -32.08127962606481987 ) ) ;
#74826=CARTESIAN_POINT ( 'NONE',  ( 16.12458315221519811, 34.43091553126765803, -24.15015252360366205 ) ) ;
#74830=CARTESIAN_POINT ( 'NONE',  ( 21.96335563855636863, 28.05277650238786080, -31.83030418064933897 ) ) ;
#74839=CARTESIAN_POINT ( 'NONE',  ( -23.05266710533800278, 25.28705973898638959, 33.20617127781060418 ) ) ;
#74868=CARTESIAN_POINT ( 'NONE',  ( 16.64348903516499334, 45.60392139269944067, 6.657797401562596917 ) ) ;
#74876=CARTESIAN_POINT ( 'NONE',  ( -30.04234920459634495, 13.07620473719203602, 42.05403970751757470 ) ) ;
#74877=FACE_BOUND ( 'NONE', #59163, .T. ) ;
#74894=CARTESIAN_POINT ( 'NONE',  ( 48.49215721461877848, 15.66554462475086495, 14.43870166537688249 ) ) ;
#74902=CARTESIAN_POINT ( 'NONE',  ( -28.56401049668894032, 13.37477103922272192, 40.29034081819133917 ) ) ;
#74909=CARTESIAN_POINT ( 'NONE',  ( 37.40778227969215664, 27.94108768513336472, -10.95617127781084399 ) ) ;
#74918=CARTESIAN_POINT ( 'NONE',  ( -0.3365330672310704596, 46.20030378422329420, -16.28442818836915862 ) ) ;
#74934=CARTESIAN_POINT ( 'NONE',  ( -4.151304510089519617, 54.24136489722235410, 6.759182313523147911 ) ) ;
#74948=EDGE_LOOP ( 'NONE', ( #23540, #47472, #92240, #89744 ) ) ;
#74963=FILL_AREA_STYLE ('',( #35088 ) ) ;
#74965=STYLED_ITEM ( 'NONE', ( #42112 ), #56276 ) ;
#74972=STYLED_ITEM ( 'NONE', ( #104683 ), #13822 ) ;
#74990=VERTEX_POINT ( 'NONE', #88265 ) ;
#74999=EDGE_CURVE ( 'NONE', #86218, #96995, #15417, .T. ) ;
#75003=CARTESIAN_POINT ( 'NONE',  ( -1.221109131435400341, 53.71017309888716085, 9.311974234608470624 ) ) ;
#75077=CARTESIAN_POINT ( 'NONE',  ( -16.64348903516517098, -1.200000000000000030E-05, 5.407797401561653672 ) ) ;
#75092=CARTESIAN_POINT ( 'NONE',  ( 8.399631981393785196, 51.60902835563812374, 4.031152949374444461 ) ) ;
#75110=FACE_BOUND ( 'NONE', #27410, .T. ) ;
#75112=CARTESIAN_POINT ( 'NONE',  ( 36.81747209427396683, 25.76191021544938664, 13.21972084597153696 ) ) ;
#75163=ORIENTED_EDGE ( 'NONE', *, *, #9213, .T. ) ;
#75178=ORIENTED_EDGE ( 'NONE', *, *, #31441, .F. ) ;
#75181=CARTESIAN_POINT ( 'NONE',  ( -9.956561055908920821, 45.46170052629869929, 15.37429631330336299 ) ) ;
#75202=CARTESIAN_POINT ( 'NONE',  ( 9.761447470195587783, 51.33896531949353914, -2.428010505629565330 ) ) ;
#75204=MECHANICAL_DESIGN_GEOMETRIC_PRESENTATION_REPRESENTATION('',(#104541),#32187);
#75213=AXIS2_PLACEMENT_3D ( 'NONE', #68387, #46097, #96772 ) ;
#75219=CARTESIAN_POINT ( 'NONE',  ( 5.933195299858810223, 51.26745231766517463, -8.366070215451848924 ) ) ;
#75229=SURFACE_STYLE_FILL_AREA ( #56917 ) ;
#75238=EDGE_LOOP ( 'NONE', ( #96521, #66300, #72485, #21633 ) ) ;
#75242=CARTESIAN_POINT ( 'NONE',  ( -9.803861187004121902, 53.40458980087238672, 2.926399253106211962 ) ) ;
#75244=CARTESIAN_POINT ( 'NONE',  ( -0.8415708020617345131, 43.28585517694735785, 18.42785063933127532 ) ) ;
#75249=CARTESIAN_POINT ( 'NONE',  ( 5.856562693840234424, 53.40179940001038972, 8.398636774803573957 ) ) ;
#75252=CARTESIAN_POINT ( 'NONE',  ( 30.04058829887667770, 13.07764605659135881, 42.05455409923722954 ) ) ;
#75254=PRESENTATION_STYLE_ASSIGNMENT (( #100603 ) ) ;
#75268=EDGE_CURVE ( 'NONE', #34743, #20894, #15478, .T. ) ;
#75278=AXIS2_PLACEMENT_3D ( 'NONE', #26399, #4737, #101828 ) ;
#75306=CARTESIAN_POINT ( 'NONE',  ( 48.02835407290504577, -1.200000000000000030E-05, -16.85535821593549954 ) ) ;
#75307=CARTESIAN_POINT ( 'NONE',  ( 8.559508646656407649, 53.68473964988125857, 4.031152949374444461 ) ) ;
#75312=CARTESIAN_POINT ( 'NONE',  ( -16.19972009820057934, 36.53460074923750511, -24.18132016187605160 ) ) ;
#75316=CARTESIAN_POINT ( 'NONE',  ( 46.79015243495871346, 13.37233443428286250, 15.81143384442388466 ) ) ;
#75324=CARTESIAN_POINT ( 'NONE',  ( -46.77684132781872961, 13.57955522726351383, -15.57752954476176477 ) ) ;
#75325=CARTESIAN_POINT ( 'NONE',  ( 0.000000000000000000, 47.77514352166374323, 0.000000000000000000 ) ) ;
#75345=B_SPLINE_CURVE_WITH_KNOTS ( 'NONE', 3,
 ( #5004, #37407, #63778, #96665, #23323, #29836, #86483, #22271, #95603, #103170, #12539, #87520, #46515, #30355, #63246, #55119, #88049, #14129, #40021, #83130, #74496, #24401 ),
 .UNSPECIFIED., .F., .F.,
 ( 4, 2, 2, 2, 2, 2, 2, 2, 2, 2, 4 ),
 ( 0.004989850371616175000, 0.005493891472670148560, 0.005997932573724122120, 0.006501973674778095680, 0.007006014775832068373, 0.007258035326359055586, 0.007510055876886042800, 0.008014096977940015493, 0.008518138078993989920, 0.008770158629520977134, 0.009022179180047966082 ),
 .UNSPECIFIED. ) ;
#75346=SURFACE_STYLE_FILL_AREA ( #101761 ) ;
#75360=ADVANCED_FACE ( 'NONE', ( #61212 ), #35906, .T. ) ;
#75365=CARTESIAN_POINT ( 'NONE',  ( 15.49793471085725471, 34.92650142558106552, -22.93080145367699174 ) ) ;
#75376=( GEOMETRIC_REPRESENTATION_CONTEXT ( 3 ) GLOBAL_UNCERTAINTY_ASSIGNED_CONTEXT ( ( #81832 ) ) GLOBAL_UNIT_ASSIGNED_CONTEXT ( ( #101047, #92956, #27745 ) ) REPRESENTATION_CONTEXT ( 'NONE', 'WORKASPACE' ) );
#75399=ORIENTED_EDGE ( 'NONE', *, *, #83243, .F. ) ;
#75410=B_SPLINE_CURVE_WITH_KNOTS ( 'NONE', 3,
 ( #47687, #56841, #106456, #80587, #32613, #49277, #97305, #48218, #82181, #8298, #81121, #89766, #31551, #74089, #48742, #6707, #7761, #40667, #64434, #73551 ),
 .UNSPECIFIED., .F., .F.,
 ( 4, 2, 2, 2, 2, 2, 2, 2, 2, 4 ),
 ( 0.003812777391809711244, 0.004316388813495462828, 0.004820000235181215280, 0.005071805946024091072, 0.005323611656866966864, 0.005827223078552714111, 0.006330834500238463093, 0.006834445921924211208, 0.007338057343609960190, 0.007841668765295708304 ),
 .UNSPECIFIED. ) ;
#75419=CARTESIAN_POINT ( 'NONE',  ( 16.48315964343914786, 45.94107222901599386, 4.157797401561416528 ) ) ;
#75425=CARTESIAN_POINT ( 'NONE',  ( -30.63784394300852654, 16.09242744237241496, 40.03992687782040605 ) ) ;
#75429=EDGE_CURVE ( 'NONE', #62158, #16331, #23125, .T. ) ;
#75444=CARTESIAN_POINT ( 'NONE',  ( -5.911416617705733678, 51.88615443309979014, -6.184768123105757631 ) ) ;
#75448=CARTESIAN_POINT ( 'NONE',  ( -11.49328356257545991, 43.46445839595169502, -13.79613624638143676 ) ) ;
#75458=EDGE_CURVE ( 'NONE', #54691, #50266, #6670, .T. ) ;
#75511=SURFACE_STYLE_USAGE ( .BOTH. , #49094 ) ;
#75518=CARTESIAN_POINT ( 'NONE',  ( 5.207846658090203640, 54.22815785865637395, 6.031152949374456007 ) ) ;
#75528=VECTOR ( 'NONE', #49362, 1000.000000000000000 ) ;
#75537=VECTOR ( 'NONE', #37584, 1000.000000000000000 ) ;
#75540=( NAMED_UNIT ( * ) PLANE_ANGLE_UNIT ( ) SI_UNIT ( $, .RADIAN. ) );
#75545=DIRECTION ( 'NONE',  ( -0.000000000000000000, 1.000000000000000000, -0.000000000000000000 ) ) ;
#75552=CARTESIAN_POINT ( 'NONE',  ( -0.3345853057524721952, 54.28960170381152750, 7.792663449346018290 ) ) ;
#75591=EDGE_LOOP ( 'NONE', ( #103974, #58844 ) ) ;
#75595=CARTESIAN_POINT ( 'NONE',  ( 16.58616928888088182, 36.42044334926447391, 24.29863715439284633 ) ) ;
#75601=CARTESIAN_POINT ( 'NONE',  ( 17.83392795039140566, 45.30293236282059866, 5.798433727367392265 ) ) ;
#75608=ORIENTED_EDGE ( 'NONE', *, *, #102592, .T. ) ;
#75615=CARTESIAN_POINT ( 'NONE',  ( 30.25691101598778943, 17.21809272184238893, -39.73659737107644219 ) ) ;
#75617=PRESENTATION_STYLE_ASSIGNMENT (( #58920 ) ) ;
#75652=CARTESIAN_POINT ( 'NONE',  ( -0.8349010936846665842, 12.93338910046981383, -49.56652387900988543 ) ) ;
#75654=SURFACE_STYLE_FILL_AREA ( #91335 ) ;
#75663=CARTESIAN_POINT ( 'NONE',  ( -5.124339073201918282, 53.50653926859659748, -8.531152949374524397 ) ) ;
#75676=ADVANCED_FACE ( 'NONE', ( #90791 ), #67581, .F. ) ;
#75692=ORIENTED_EDGE ( 'NONE', *, *, #4331, .T. ) ;
#75709=( NAMED_UNIT ( * ) SI_UNIT ( $, .STERADIAN. ) SOLID_ANGLE_UNIT ( ) );
#75714=CARTESIAN_POINT ( 'NONE',  ( -1.231557862076259280, 16.44676558348158224, 50.25324543889210815 ) ) ;
#75723=CARTESIAN_POINT ( 'NONE',  ( 0.7810335935915004857, 13.54372500177475835, -51.48049019060625398 ) ) ;
#75725=AXIS2_PLACEMENT_3D ( 'NONE', #12257, #27970, #59774 ) ;
#75727=CARTESIAN_POINT ( 'NONE',  ( -11.36440886748413881, 45.70401808670207799, -13.50555938308150594 ) ) ;
#75730=CARTESIAN_POINT ( 'NONE',  ( -48.02835407290534420, 14.94086294439724227, -16.85535821593460426 ) ) ;
#75732=DIRECTION ( 'NONE',  ( 1.150791560227848297E-16, -0.3420201433256725987, 0.9396926207859068736 ) ) ;
#75743=( LENGTH_UNIT ( ) NAMED_UNIT ( * ) SI_UNIT ( .MILLI., .METRE. ) );
#75759=MECHANICAL_DESIGN_GEOMETRIC_PRESENTATION_REPRESENTATION('',(#56804),#6917);
#75766=CARTESIAN_POINT ( 'NONE',  ( -36.32243474800993255, 28.19842941503742750, -12.06008965998136517 ) ) ;
#75798=ORIENTED_EDGE ( 'NONE', *, *, #25435, .T. ) ;
#75807=CARTESIAN_POINT ( 'NONE',  ( 0.1697127678336000367, 28.20321630628727760, 38.25871777383677852 ) ) ;
#75809=CONICAL_SURFACE ( 'NONE', #44808, 33.82893434829263413, 1.221730476396026610 ) ;
#75826=ORIENTED_EDGE ( 'NONE', *, *, #82415, .T. ) ;
#75827=SURFACE_STYLE_USAGE ( .BOTH. , #44543 ) ;
#75849=CARTESIAN_POINT ( 'NONE',  ( 7.345894760218278030, 54.30772485615508316, 2.470096959125457126 ) ) ;
#75856=CARTESIAN_POINT ( 'NONE',  ( -15.64272365568267631, 37.16721670561515367, -22.45732330511674490 ) ) ;
#75868=CARTESIAN_POINT ( 'NONE',  ( -48.02835407290533709, 11.61227450977237119, -14.35535821593460248 ) ) ;
#75869=CARTESIAN_POINT ( 'NONE',  ( 0.000000000000000000, 52.29617335651133914, 0.000000000000000000 ) ) ;
#75871=CARTESIAN_POINT ( 'NONE',  ( 48.02835407290544367, -1.200000000000000030E-05, 15.60535821593427563 ) ) ;
#75889=SURFACE_STYLE_USAGE ( .BOTH. , #27929 ) ;
#75924=AXIS2_PLACEMENT_3D ( 'NONE', #68606, #86915, #103607 ) ;
#75931=DIRECTION ( 'NONE',  ( -0.000000000000000000, 1.000000000000000000, 0.000000000000000000 ) ) ;
#75944=CARTESIAN_POINT ( 'NONE',  ( -7.944368338772524574, 53.91027570826472015, -3.880857395784224728 ) ) ;
#75949=ORIENTED_EDGE ( 'NONE', *, *, #87761, .T. ) ;
#75954=ORIENTED_EDGE ( 'NONE', *, *, #25694, .F. ) ;
#75956=( LENGTH_UNIT ( ) NAMED_UNIT ( * ) SI_UNIT ( .MILLI., .METRE. ) );
#75964=CARTESIAN_POINT ( 'NONE',  ( -7.482490643626594107, 52.00342315862429388, 3.436133781616750316 ) ) ;
#75999=CARTESIAN_POINT ( 'NONE',  ( -23.85927881108850457, 25.16624194764255762, -33.04187418837310020 ) ) ;
#76004=CARTESIAN_POINT ( 'NONE',  ( 1.250381663246963759, 36.68826934548923191, 28.65663572643696000 ) ) ;
#76009=CARTESIAN_POINT ( 'NONE',  ( -38.32871752026355239, 25.24414280242103459, -13.21120402984903031 ) ) ;
#76049=CARTESIAN_POINT ( 'NONE',  ( 27.26388569244345916, 36.83098433723539245, 7.556984339685507202 ) ) ;
#76055=SURFACE_STYLE_USAGE ( .BOTH. , #36718 ) ;
#76079=LINE ( 'NONE', #36212, #101091 ) ;
#76088=ORIENTED_EDGE ( 'NONE', *, *, #58436, .F. ) ;
#76100=LINE ( 'NONE', #83137, #47755 ) ;
#76105=CARTESIAN_POINT ( 'NONE',  ( -15.42241126771893889, 46.21736870922991613, -5.091656527549202060 ) ) ;
#76109=VECTOR ( 'NONE', #72879, 1000.000000000000114 ) ;
#76122=CARTESIAN_POINT ( 'NONE',  ( -48.48458519718469972, 8.810627846918883677, -16.77132102101082012 ) ) ;
#76126=DIRECTION ( 'NONE',  ( -0.000000000000000000, 1.000000000000000000, -0.000000000000000000 ) ) ;
#76130=EDGE_CURVE ( 'NONE', #88140, #32552, #41043, .T. ) ;
#76150=CARTESIAN_POINT ( 'NONE',  ( -47.44867487729145239, 16.35164899989666054, 16.71951642917255398 ) ) ;
#76151=CARTESIAN_POINT ( 'NONE',  ( 38.17803095905032507, 27.65683721262864125, -11.10447198242798272 ) ) ;
#76158=B_SPLINE_CURVE_WITH_KNOTS ( 'NONE', 3,
 ( #73047, #88734, #29476, #96312, #14826, #39664, #14290, #47194, #62353, #80094, #89268, #6200, #39137, #64468, #23492, #1279, #49308, #33170, #9377, #16426 ),
 .UNSPECIFIED., .F., .F.,
 ( 4, 2, 2, 2, 2, 2, 2, 2, 2, 4 ),
 ( 0.007186367946188911872, 0.007690128173786097560, 0.008193888401383284115, 0.008697648628980470670, 0.009201408856577655490, 0.009705169084174842045, 0.01020892931177202687, 0.01046080942557061841, 0.01071268953936920648, 0.01121644976696637569 ),
 .UNSPECIFIED. ) ;
#76168=CARTESIAN_POINT ( 'NONE',  ( -48.02835407290533709, 11.61227450977237119, -14.35535821593460248 ) ) ;
#76183=CARTESIAN_POINT ( 'NONE',  ( -1.251112176197288095, 10.43734136627239728, -50.60533220255923226 ) ) ;
#76185=CARTESIAN_POINT ( 'NONE',  ( 36.92547957880908882, 25.96841499943989362, 11.08204091492609322 ) ) ;
#76188=CARTESIAN_POINT ( 'NONE',  ( 9.268351869679383626, 44.06619222810213188, -13.41315172291116475 ) ) ;
#76192=CARTESIAN_POINT ( 'NONE',  ( -23.21751746555244722, -1.200000000000000030E-05, 31.95617127781060773 ) ) ;
#76200=CARTESIAN_POINT ( 'NONE',  ( -16.32412570343894131, 43.58760925489881544, 6.626709406305174355 ) ) ;
#76202=CARTESIAN_POINT ( 'NONE',  ( 28.29586762127448551, 36.29923524811977131, -9.196630039856511729 ) ) ;
#76214=CARTESIAN_POINT ( 'NONE',  ( 8.398714108050164384, 51.60933059333073913, -4.031152949374811278 ) ) ;
#76217=CARTESIAN_POINT ( 'NONE',  ( -0.3341299038094548424, 28.19050081788694229, -38.29257118597956122 ) ) ;
#76223=CARTESIAN_POINT ( 'NONE',  ( 46.79169002450413473, 18.53182619689592769, -15.81978731893121015 ) ) ;
#76233=CARTESIAN_POINT ( 'NONE',  ( 0.000000000000000000, 2.000000000000000000, 0.000000000000000000 ) ) ;
#76240=ORIENTED_EDGE ( 'NONE', *, *, #92748, .F. ) ;
#76242=CARTESIAN_POINT ( 'NONE',  ( -22.59054144479424409, 25.42936075388009343, -33.04960633241812928 ) ) ;
#76244=CARTESIAN_POINT ( 'NONE',  ( -26.78880536180239247, 34.86538589505409647, -7.595015278602215147 ) ) ;
#76245=CARTESIAN_POINT ( 'NONE',  ( -1.010569909552581080, 43.89392652721726762, -16.74618260332281139 ) ) ;
#76260=ORIENTED_EDGE ( 'NONE', *, *, #57320, .T. ) ;
#76275=CARTESIAN_POINT ( 'NONE',  ( 48.26938392169741121, 11.04962899253383313, -14.37319483549308785 ) ) ;
#76278=CARTESIAN_POINT ( 'NONE',  ( 5.929606399591413890, 51.27011112052321096, 8.358468156669783156 ) ) ;
#76281=ORIENTED_EDGE ( 'NONE', *, *, #6918, .F. ) ;
#76295=CARTESIAN_POINT ( 'NONE',  ( 0.000000000000000000, 29.08768991669519721, 0.000000000000000000 ) ) ;
#76335=CARTESIAN_POINT ( 'NONE',  ( 8.718949332298615573, 53.63223895871195879, -4.031152949375384154 ) ) ;
#76338=EDGE_LOOP ( 'NONE', ( #37887, #90160, #15734, #87219, #9952, #104810, #46799, #33276 ) ) ;
#76374=CARTESIAN_POINT ( 'NONE',  ( -15.64878411475348408, 36.78373704832288382, -23.72567384382504585 ) ) ;
#76389=MECHANICAL_DESIGN_GEOMETRIC_PRESENTATION_REPRESENTATION('',(#7459),#73198);
#76401=STYLED_ITEM ( 'NONE', ( #15664 ), #17835 ) ;
#76403=CARTESIAN_POINT ( 'NONE',  ( 29.28872172473180768, 8.962789800749073166, -42.04350091203807693 ) ) ;
#76423=CARTESIAN_POINT ( 'NONE',  ( -27.10511071441193565, 34.75829513984539432, -7.556984339685824281 ) ) ;
#76427=SURFACE_SIDE_STYLE ('',( #44624 ) ) ;
#76429=( NAMED_UNIT ( * ) SI_UNIT ( $, .STERADIAN. ) SOLID_ANGLE_UNIT ( ) );
#76453=FACE_OUTER_BOUND ( 'NONE', #23162, .T. ) ;
#76474=CARTESIAN_POINT ( 'NONE',  ( 9.653963884811064489, 53.40254541166815017, 3.408400523946627292 ) ) ;
#76482=B_SPLINE_CURVE_WITH_KNOTS ( 'NONE', 3,
 ( #54150, #15833, #31522, #65455, #14227, #104855, #81603, #7205, #47133, #48189, #105895, #64404, #32042, #24502, #97277, #63880, #55221, #64922, #88147, #80028, #23426, #55736 ),
 .UNSPECIFIED., .F., .F.,
 ( 4, 2, 2, 2, 2, 2, 2, 2, 2, 2, 4 ),
 ( 0.007110638423152015018, 0.007613994425099801511, 0.008117350427047587136, 0.008620706428995374496, 0.008872384429969270778, 0.009124062430943168794, 0.009375740431917065076, 0.009627418432890963093, 0.01013077443483876260, 0.01063413043678656383, 0.01113748643873436334 ),
 .UNSPECIFIED. ) ;
#76495=CARTESIAN_POINT ( 'NONE',  ( 0.000000000000000000, 52.29617335651133914, 0.000000000000000000 ) ) ;
#76497=ADVANCED_FACE ( 'NONE', ( #50444 ), #91981, .F. ) ;
#76509=CARTESIAN_POINT ( 'NONE',  ( -11.54078658013951397, 43.31764940862575486, -14.27918301262186063 ) ) ;
#76516=LINE ( 'NONE', #51706, #96199 ) ;
#76523=CARTESIAN_POINT ( 'NONE',  ( -16.75187969033532553, 34.99134772383131065, 21.80698433968612093 ) ) ;
#76542=CARTESIAN_POINT ( 'NONE',  ( 15.39058602336948667, 44.07990289552515151, -5.264532584975986751 ) ) ;
#76551=DIRECTION ( 'NONE',  ( -0.000000000000000000, 1.000000000000000000, 0.000000000000000000 ) ) ;
#76582=CARTESIAN_POINT ( 'NONE',  ( 30.55529413189656651, 11.20957620317260428, -39.95174307500007416 ) ) ;
#76593=AXIS2_PLACEMENT_3D ( 'NONE', #47173, #6724, #71993 ) ;
#76595=LINE ( 'NONE', #26505, #4702 ) ;
#76597=ORIENTED_EDGE ( 'NONE', *, *, #36297, .F. ) ;
#76637=( NAMED_UNIT ( * ) PLANE_ANGLE_UNIT ( ) SI_UNIT ( $, .RADIAN. ) );
#76670=VECTOR ( 'NONE', #71084, 1000.000000000000000 ) ;
#76686=CARTESIAN_POINT ( 'NONE',  ( 38.81305289857993301, 27.34046816746474562, -12.01329072166396372 ) ) ;
#76689=CARTESIAN_POINT ( 'NONE',  ( 0.9531427616335313990, 13.93692614003196262, 51.31255756095965381 ) ) ;
#76709=ORIENTED_EDGE ( 'NONE', *, *, #58820, .T. ) ;
#76710=FACE_BOUND ( 'NONE', #63524, .T. ) ;
#76715=CARTESIAN_POINT ( 'NONE',  ( -17.94999111897422495, 36.38767359518977429, 23.42285042635046466 ) ) ;
#76723=CARTESIAN_POINT ( 'NONE',  ( -4.727426639335938319, 54.30178277073695625, -6.161806174029161198 ) ) ;
#76734=CARTESIAN_POINT ( 'NONE',  ( 27.86843456301890853, 36.37502626979712517, -9.810812331909650297 ) ) ;
#76750=CARTESIAN_POINT ( 'NONE',  ( -1.101781001986523512, 27.52342745690481962, -40.11163141724147607 ) ) ;
#76755=CARTESIAN_POINT ( 'NONE',  ( 47.90297653514665654, 15.22282649863775283, -16.85535821593543560 ) ) ;
#76757=CARTESIAN_POINT ( 'NONE',  ( -10.93254357274233435, 43.80611415629375927, 13.04138954228639236 ) ) ;
#76759=CARTESIAN_POINT ( 'NONE',  ( -48.90230676976804602, 14.54998273526353358, 14.70096925929783716 ) ) ;
#76762=DIRECTION ( 'NONE',  ( -0.000000000000000000, 1.000000000000000000, -0.000000000000000000 ) ) ;
#76776=CARTESIAN_POINT ( 'NONE',  ( -25.89532866215253648, 35.00241476997732093, -9.162145777036789340 ) ) ;
#76784=CARTESIAN_POINT ( 'NONE',  ( -11.27248856952037315, 45.76231435389451718, -13.37350896801532230 ) ) ;
#76785=( NAMED_UNIT ( * ) SI_UNIT ( $, .STERADIAN. ) SOLID_ANGLE_UNIT ( ) );
#76788=CARTESIAN_POINT ( 'NONE',  ( -46.83658167332212230, 18.87978240383743156, -15.22028160905640171 ) ) ;
#76800=CARTESIAN_POINT ( 'NONE',  ( 9.953549941019165459, 46.18635266956800223, -12.94124874758495025 ) ) ;
#76803=ORIENTED_EDGE ( 'NONE', *, *, #9617, .F. ) ;
#76822=CARTESIAN_POINT ( 'NONE',  ( 5.373223245032201945, 51.33044523536907633, -8.531152949374597227 ) ) ;
#76829=LINE ( 'NONE', #3487, #9481 ) ;
#76839=CARTESIAN_POINT ( 'NONE',  ( 0.7798757358128801664, 8.372270557959069492, 51.48139209962896956 ) ) ;
#76860=VECTOR ( 'NONE', #96141, 1000.000000000000000 ) ;
#76871=CARTESIAN_POINT ( 'NONE',  ( 8.880941803279268854, 53.58345806519636056, -4.000118153562265633 ) ) ;
#76874=EDGE_LOOP ( 'NONE', ( #90447, #79159 ) ) ;
#76917=CARTESIAN_POINT ( 'NONE',  ( -15.97435091970899812, 37.21084721865047129, -22.07459719473156312 ) ) ;
#76958=B_SPLINE_CURVE_WITH_KNOTS ( 'NONE', 3,
 ( #11549, #44477, #68211, #45545, #77368, #95155, #78417, #102167, #4010, #86016, #2402, #3484, #36424, #53094, #77902, #43412, #36940, #4536, #37478, #62270, #87066, #101108, #27268, #60153, #93017, #89176, #63850, #105873, #14732, #80005 ),
 .UNSPECIFIED., .F., .F.,
 ( 4, 2, 2, 2, 2, 2, 2, 2, 2, 2, 2, 2, 2, 2, 4 ),
 ( 0.01036701337735199818, 0.01128271447498712179, 0.01219841557262224367, 0.01311411667025736728, 0.01357196721907492735, 0.01402981776789248743, 0.01448766831671004750, 0.01471659359111883100, 0.01494551886552761451, 0.01517444413993639801, 0.01540336941434517978, 0.01586121996316274332, 0.01631907051198030686, 0.01677692106079787041, 0.01769262215843298361 ),
 .UNSPECIFIED. ) ;
#76961=CARTESIAN_POINT ( 'NONE',  ( 17.96008057617807196, 36.59330496951920964, -22.69888471349237946 ) ) ;
#76978=DIRECTION ( 'NONE',  ( 0.000000000000000000, 1.000000000000000000, 0.000000000000000000 ) ) ;
#76989=EDGE_CURVE ( 'NONE', #58522, #16331, #105727, .T. ) ;
#76990=EDGE_LOOP ( 'NONE', ( #1265, #57540, #91987, #62583 ) ) ;
#76996=CARTESIAN_POINT ( 'NONE',  ( 0.7834951455711054447, 37.11066583794674756, -27.51244135688735071 ) ) ;
#77000=CYLINDRICAL_SURFACE ( 'NONE', #75725, 1.250000000000001110 ) ;
#77027=CARTESIAN_POINT ( 'NONE',  ( -8.559508646656370345, 51.55638410492942114, 4.031152949374564365 ) ) ;
#77029=MECHANICAL_DESIGN_GEOMETRIC_PRESENTATION_REPRESENTATION('',(#49691),#56531);
#77047=CARTESIAN_POINT ( 'NONE',  ( -11.38829015755950635, 43.21651619172995851, -14.75358294640981249 ) ) ;
#77048=CARTESIAN_POINT ( 'NONE',  ( -0.3379147738798968792, 37.19680971541975367, 27.28503007046158402 ) ) ;
#77058=VERTEX_POINT ( 'NONE', #17804 ) ;
#77067=AXIS2_PLACEMENT_3D ( 'NONE', #53032, #93504, #2336 ) ;
#77090=CARTESIAN_POINT ( 'NONE',  ( -15.43446081147251014, 46.13172121994918484, 5.765148793919729897 ) ) ;
#77129=CARTESIAN_POINT ( 'NONE',  ( 30.90717084365905976, 9.524046525576030930, -40.57283699552807121 ) ) ;
#77144=MECHANICAL_DESIGN_GEOMETRIC_PRESENTATION_REPRESENTATION('',(#78829),#22046);
#77145=CARTESIAN_POINT ( 'NONE',  ( 2.761899744546835519E-15, 0.000000000000000000, -22.55262289886175964 ) ) ;
#77191=ORIENTED_EDGE ( 'NONE', *, *, #53498, .T. ) ;
#77199=CYLINDRICAL_SURFACE ( 'NONE', #103802, 1.250000000000001110 ) ;
#77219=CARTESIAN_POINT ( 'NONE',  ( 29.85155995213039049, 18.03343143632517709, -39.61445771744218547 ) ) ;
#77227=CARTESIAN_POINT ( 'NONE',  ( 17.07926083379644311, 34.90888828800229504, 21.84001637439316568 ) ) ;
#77230=CARTESIAN_POINT ( 'NONE',  ( 0.2958821552773560626, 18.79221613348494913, 49.28340278884313364 ) ) ;
#77233=EDGE_CURVE ( 'NONE', #741, #73917, #85969, .T. ) ;
#77256=CARTESIAN_POINT ( 'NONE',  ( -7.562525622355496857, 52.15248883143013359, -2.008797297745641863 ) ) ;
#77261=CARTESIAN_POINT ( 'NONE',  ( -0.8446698455446330911, 8.504696595714664298, -51.42477032456711328 ) ) ;
#77263=( LENGTH_UNIT ( ) NAMED_UNIT ( * ) SI_UNIT ( .MILLI., .METRE. ) );
#77272=FILL_AREA_STYLE_COLOUR ( '', #41895 ) ;
#77302=DIRECTION ( 'NONE',  ( 0.000000000000000000, 0.000000000000000000, -1.000000000000000000 ) ) ;
#77308=EDGE_CURVE ( 'NONE', #22182, #61560, #35939, .T. ) ;
#77309=CARTESIAN_POINT ( 'NONE',  ( 23.21751746555144180, 27.38103382803512176, -33.20617127781698485 ) ) ;
#77312=ORIENTED_EDGE ( 'NONE', *, *, #42293, .T. ) ;
#77314=CARTESIAN_POINT ( 'NONE',  ( 5.126143460586249034, 52.11941149169467735, -6.031152949374488870 ) ) ;
#77317=ORIENTED_EDGE ( 'NONE', *, *, #91189, .F. ) ;
#77331=COLOUR_RGB ( '', 0.66274510, 0.83137255, 0.94901961) ;
#77352=CARTESIAN_POINT ( 'NONE',  ( 49.25933966097094441, 7.764757817614878377, -15.83577412118909677 ) ) ;
#77353=( NAMED_UNIT ( * ) PLANE_ANGLE_UNIT ( ) SI_UNIT ( $, .RADIAN. ) );
#77368=CARTESIAN_POINT ( 'NONE',  ( 48.60160210973891992, 15.38206115941115470, -14.48795722268628872 ) ) ;
#77374=DIRECTION ( 'NONE',  ( 0.000000000000000000, 0.000000000000000000, 1.000000000000000000 ) ) ;
#77381=CARTESIAN_POINT ( 'NONE',  ( 0.5336880547914685247, 8.009115710655695608, 51.63698046263905184 ) ) ;
#77389=EDGE_CURVE ( 'NONE', #91653, #41746, #9966, .T. ) ;
#77404=CARTESIAN_POINT ( 'NONE',  ( -7.316272466829250476, 54.23236173032573504, 3.143061027692354514 ) ) ;
#77408=CARTESIAN_POINT ( 'NONE',  ( -37.56673239365849781, -1.200000000000000030E-05, 10.95617127781066102 ) ) ;
#77413=LINE ( 'NONE', #33786, #34042 ) ;
#77414=CARTESIAN_POINT ( 'NONE',  ( 8.559508646656350805, 53.68473964988125857, -4.031152949374623873 ) ) ;
#77425=COLOUR_RGB ( '', 0.08235294, 0.09019608, 0.10196078) ;
#77428=UNCERTAINTY_MEASURE_WITH_UNIT (LENGTH_MEASURE( 1.000000000000000082E-05 ), #89013, 'distance_accuracy_value', 'NONE');
#77448=B_SPLINE_CURVE_WITH_KNOTS ( 'NONE', 3,
 ( #49782, #68652, #3369, #70228, #21185, #77256, #100992, #10377, #19600, #3902, #11434, #52431, #27150, #36314, #92897, #43818, #85348, #85902 ),
 .UNSPECIFIED., .F., .F.,
 ( 4, 2, 2, 2, 2, 2, 2, 2, 4 ),
 ( 0.003275144142300112030, 0.003781209443760275707, 0.004287274745220439817, 0.004793340046680603060, 0.005046372697410685983, 0.005299405348140768905, 0.005805470649600934750, 0.006311535951061099728, 0.007323666553981426214 ),
 .UNSPECIFIED. ) ;
#77450=FILL_AREA_STYLE ('',( #13755 ) ) ;
#77454=CARTESIAN_POINT ( 'NONE',  ( -1.251141718528236524, 51.63899026595163377, -9.149171384829717368 ) ) ;
#77472=CARTESIAN_POINT ( 'NONE',  ( -46.77752740700942979, 13.53072847091731035, -15.64014710929908780 ) ) ;
#77476=CARTESIAN_POINT ( 'NONE',  ( -17.40642114240819183, 43.24861748976680786, -6.412094953349521731 ) ) ;
#77491=CARTESIAN_POINT ( 'NONE',  ( 28.45522292534169395, 11.90502831567345865, -41.11935372236962394 ) ) ;
#77510=ORIENTED_EDGE ( 'NONE', *, *, #93296, .T. ) ;
#77512=( LENGTH_UNIT ( ) NAMED_UNIT ( * ) SI_UNIT ( .MILLI., .METRE. ) );
#77532=SURFACE_STYLE_FILL_AREA ( #68923 ) ;
#77533=CARTESIAN_POINT ( 'NONE',  ( 0.5678904221582695699, 36.34682479118509946, -29.61666878930105895 ) ) ;
#77549=VERTEX_POINT ( 'NONE', #90899 ) ;
#77551=ORIENTED_EDGE ( 'NONE', *, *, #95294, .F. ) ;
#77570=DIRECTION ( 'NONE',  ( -0.000000000000000000, 1.000000000000000000, -0.000000000000000000 ) ) ;
#77576=CARTESIAN_POINT ( 'NONE',  ( 0.3594682699208841536, 7.865263358805581362, -51.69874683107578051 ) ) ;
#77582=VERTEX_POINT ( 'NONE', #41799 ) ;
#77598=ORIENTED_EDGE ( 'NONE', *, *, #6324, .F. ) ;
#77628=CARTESIAN_POINT ( 'NONE',  ( -16.64348903516517098, 45.88445698070336221, 4.157797401561652784 ) ) ;
#77654=CARTESIAN_POINT ( 'NONE',  ( -23.21751746555244722, 28.11705169068991594, 30.70617127781060418 ) ) ;
#77695=FILL_AREA_STYLE ('',( #36744 ) ) ;
#77709=CARTESIAN_POINT ( 'NONE',  ( 36.35284819509398346, 26.07822863538820002, -11.89625673952615159 ) ) ;
#77715=AXIS2_PLACEMENT_3D ( 'NONE', #81684, #65534, #749 ) ;
#77718=CARTESIAN_POINT ( 'NONE',  ( -15.55855383130854364, 46.20420475984592201, -4.781350493801898693 ) ) ;
#77727=CARTESIAN_POINT ( 'NONE',  ( 1.990040563172386960E-15, 46.21383923812596350, 16.25000000000000000 ) ) ;
#77742=EDGE_CURVE ( 'NONE', #74990, #96186, #76958, .T. ) ;
#77761=ORIENTED_EDGE ( 'NONE', *, *, #42293, .F. ) ;
#77765=CARTESIAN_POINT ( 'NONE',  ( -29.14573983020256520, 13.65694994997194023, -39.72476874530827473 ) ) ;
#77775=ADVANCED_FACE ( 'NONE', ( #7176 ), #22875, .F. ) ;
#77782=EDGE_LOOP ( 'NONE', ( #9748, #31499, #100315, #89806 ) ) ;
#77792=FACE_OUTER_BOUND ( 'NONE', #93556, .T. ) ;
#77796=CARTESIAN_POINT ( 'NONE',  ( -0.1556861026017113125, 7.763710170093361285, -51.74238828694827674 ) ) ;
#77801=CARTESIAN_POINT ( 'NONE',  ( 5.931261341847957169, 53.39841463849090530, -8.357466982193816563 ) ) ;
#77802=EDGE_CURVE ( 'NONE', #31379, #6418, #39577, .T. ) ;
#77803=CARTESIAN_POINT ( 'NONE',  ( 17.89153430032353143, 34.22757668435322387, -23.57710181514798009 ) ) ;
#77830=CARTESIAN_POINT ( 'NONE',  ( -0.7828025612222084817, 28.10837865791959800, -38.51177607868886810 ) ) ;
#77834=CARTESIAN_POINT ( 'NONE',  ( 0.000000000000000000, -1.200000000000000030E-05, 18.75000000000000355 ) ) ;
#77836=CARTESIAN_POINT ( 'NONE',  ( -11.52585092648323162, 43.45746737603746368, 13.79532806417373614 ) ) ;
#77845=CARTESIAN_POINT ( 'NONE',  ( 4.512137457764992199, 52.17996906692113157, -6.299107601609536644 ) ) ;
#77850=CARTESIAN_POINT ( 'NONE',  ( -22.57862130244024002, 26.07716137114785226, -30.87848508644228929 ) ) ;
#77886=CARTESIAN_POINT ( 'NONE',  ( 49.02571528365142939, 7.903708718522375776, -16.36159347772493078 ) ) ;
#77889=ORIENTED_EDGE ( 'NONE', *, *, #4277, .F. ) ;
#77902=CARTESIAN_POINT ( 'NONE',  ( 49.27995299967488307, 13.03636147101435050, -15.63012893017262250 ) ) ;
#77906=VECTOR ( 'NONE', #47204, 1000.000000000000000 ) ;
#77920=CARTESIAN_POINT ( 'NONE',  ( 22.10841373170462987, 28.16423242622106216, -31.35595207099958159 ) ) ;
#77943=EDGE_LOOP ( 'NONE', ( #47008, #81921, #104060, #98936 ) ) ;
#77947=CARTESIAN_POINT ( 'NONE',  ( 9.687386010480340204, 53.40046982867094982, -3.326548872099157172 ) ) ;
#77967=CARTESIAN_POINT ( 'NONE',  ( -24.23713502960758603, 27.31419257049583038, -32.69873751732588119 ) ) ;
#77977=ORIENTED_EDGE ( 'NONE', *, *, #73188, .T. ) ;
#77982=CARTESIAN_POINT ( 'NONE',  ( -0.6428164758118281030, 52.11010785308932469, -7.915233080243755381 ) ) ;
#77992=EDGE_CURVE ( 'NONE', #49001, #15279, #62638, .T. ) ;
#77999=CARTESIAN_POINT ( 'NONE',  ( -37.24792026525560118, 25.58915884325793044, -13.42514790916754919 ) ) ;
#78012=VECTOR ( 'NONE', #20980, 1000.000000000000000 ) ;
#78054=VERTEX_POINT ( 'NONE', #99912 ) ;
#78058=PRESENTATION_STYLE_ASSIGNMENT (( #3650 ) ) ;
#78097=ORIENTED_EDGE ( 'NONE', *, *, #89452, .F. ) ;
#78110=CARTESIAN_POINT ( 'NONE',  ( -1.005228751829300160, 36.47691725556884990, 29.24735311802084681 ) ) ;
#78136=CARTESIAN_POINT ( 'NONE',  ( -26.00996381060643969, 37.20445080285505668, 8.181011038402493440 ) ) ;
#78148=CARTESIAN_POINT ( 'NONE',  ( -38.74305977430618242, 27.39011302538496295, 11.77545443400052605 ) ) ;
#78149=CARTESIAN_POINT ( 'NONE',  ( -15.54898481255693454, 46.20784644949144138, 4.780735607413708621 ) ) ;
#78150=ORIENTED_EDGE ( 'NONE', *, *, #39875, .T. ) ;
#78155=CARTESIAN_POINT ( 'NONE',  ( -30.25640691047282616, 12.05011699928720503, 39.73625916528160928 ) ) ;
#78197=CARTESIAN_POINT ( 'NONE',  ( 10.28624191511840458, -1.200000000000000030E-05, 14.15779740156149025 ) ) ;
#78222=EDGE_LOOP ( 'NONE', ( #84770, #104377 ) ) ;
#78225=CARTESIAN_POINT ( 'NONE',  ( -30.59355846057999884, 12.96027739219344532, -41.71512601614534077 ) ) ;
#78231=CARTESIAN_POINT ( 'NONE',  ( -3.840629472727446691E-14, -1.200000000000000030E-05, -28.50000000000000000 ) ) ;
#78245=EDGE_CURVE ( 'NONE', #89428, #4091, #35759, .T. ) ;
#78264=FACE_OUTER_BOUND ( 'NONE', #66265, .T. ) ;
#78297=( NAMED_UNIT ( * ) SI_UNIT ( $, .STERADIAN. ) SOLID_ANGLE_UNIT ( ) );
#78313=UNCERTAINTY_MEASURE_WITH_UNIT (LENGTH_MEASURE( 1.000000000000000082E-05 ), #35137, 'distance_accuracy_value', 'NONE');
#78363=CARTESIAN_POINT ( 'NONE',  ( -9.538946952600159790, 53.58200059918309677, -1.988036826341423646 ) ) ;
#78365=CARTESIAN_POINT ( 'NONE',  ( 4.650850488836845820, 52.17814524009082788, -6.203660599199528392 ) ) ;
#78371=CARTESIAN_POINT ( 'NONE',  ( -22.43980529875399554, 26.07880074899891909, -30.97394950045124418 ) ) ;
#78393=LINE ( 'NONE', #70841, #22798 ) ;
#78398=CARTESIAN_POINT ( 'NONE',  ( -16.75187969033532553, 34.99134772383131065, 21.80698433968612093 ) ) ;
#78417=CARTESIAN_POINT ( 'NONE',  ( 48.90230676976855051, 14.54998273526172170, -14.70096925929882659 ) ) ;
#78481=CARTESIAN_POINT ( 'NONE',  ( -15.64282023038923697, 37.16738321503569864, 22.45670599646769006 ) ) ;
#78486=CARTESIAN_POINT ( 'NONE',  ( 25.88368638486081252, 37.21352445278208165, 8.492507970579360688 ) ) ;
#78497=ORIENTED_EDGE ( 'NONE', *, *, #7044, .T. ) ;
#78512=AXIS2_PLACEMENT_3D ( 'NONE', #6481, #79317, #5438 ) ;
#78524=CARTESIAN_POINT ( 'NONE',  ( 8.559508646656407649, -1.200000000000000030E-05, 4.031152949374444461 ) ) ;
#78533=LINE ( 'NONE', #88235, #92349 ) ;
#78543=ORIENTED_EDGE ( 'NONE', *, *, #91059, .F. ) ;
#78562=CARTESIAN_POINT ( 'NONE',  ( 9.058705124515451956, 43.97099215302630171, 13.86878051210034180 ) ) ;
#78563=FACE_BOUND ( 'NONE', #5889, .T. ) ;
#78569=B_SPLINE_CURVE_WITH_KNOTS ( 'NONE', 3,
 ( #96981, #78650, #30683, #103477, #63028, #55435, #5323, #13387, #55956, #13918, #63570, #61986, #5834, #78136, #103996, #94878, #87304, #12858, #46309, #79200 ),
 .UNSPECIFIED., .F., .F.,
 ( 4, 2, 2, 2, 2, 2, 2, 2, 2, 4 ),
 ( 0.003027256308175210915, 0.003532084672752785343, 0.004036913037330358903, 0.004541741401907933330, 0.005046569766485507758, 0.005298983948774298007, 0.005551398131063089124, 0.006056226495640661817, 0.006561054860218235377, 0.007065883224795808069 ),
 .UNSPECIFIED. ) ;
#78578=CARTESIAN_POINT ( 'NONE',  ( 0.6444270201114900010, 37.14712638292468228, -27.41604988274115939 ) ) ;
#78594=ORIENTED_EDGE ( 'NONE', *, *, #23247, .F. ) ;
#78599=VERTEX_POINT ( 'NONE', #62528 ) ;
#78600=DIRECTION ( 'NONE',  ( 0.000000000000000000, 0.000000000000000000, 1.000000000000000000 ) ) ;
#78612=CARTESIAN_POINT ( 'NONE',  ( 0.000000000000000000, 34.08768991669519721, -35.82893434829263413 ) ) ;
#78614=CARTESIAN_POINT ( 'NONE',  ( 4.733165431326070832E-26, 13.70447791526910919, -49.25000000000000000 ) ) ;
#78633=ORIENTED_EDGE ( 'NONE', *, *, #92768, .F. ) ;
#78646=ORIENTED_EDGE ( 'NONE', *, *, #59087, .T. ) ;
#78650=CARTESIAN_POINT ( 'NONE',  ( -26.94510944316361645, 36.66031116801333667, 10.05698433968617245 ) ) ;
#78652=CARTESIAN_POINT ( 'NONE',  ( -5.125978502509880741, 54.24780662741380866, 6.031152949374397387 ) ) ;
#78661=VECTOR ( 'NONE', #15424, 1000.000000000000000 ) ;
#78666=CARTESIAN_POINT ( 'NONE',  ( -49.24306615471302706, 8.188742177551265655, 15.29695692017770803 ) ) ;
#78674=CARTESIAN_POINT ( 'NONE',  ( -30.64348173561394617, 7.829960647508013238, 41.65811975367132902 ) ) ;
#78703=CARTESIAN_POINT ( 'NONE',  ( 30.59734358679082789, 7.793378852367167653, -41.71107540015051285 ) ) ;
#78708=FILL_AREA_STYLE ('',( #21070 ) ) ;
#78734=EDGE_LOOP ( 'NONE', ( #29592, #73182, #43378, #54884 ) ) ;
#78746=CARTESIAN_POINT ( 'NONE',  ( 37.24599997783883509, 25.86608068541391958, -10.98719536802521368 ) ) ;
#78763=CARTESIAN_POINT ( 'NONE',  ( -1.231536178911134094, 11.27772218784141423, 50.25311877652383430 ) ) ;
#78771=CARTESIAN_POINT ( 'NONE',  ( 10.68704811846494351, 43.88291023799746426, 12.97108649491024579 ) ) ;
#78779=CARTESIAN_POINT ( 'NONE',  ( -15.55430219785582935, 34.98758788652926910, 22.68934981201532963 ) ) ;
#78781=EDGE_CURVE ( 'NONE', #90588, #4091, #10399, .T. ) ;
#78790=SURFACE_STYLE_FILL_AREA ( #22724 ) ;
#78805=EDGE_CURVE ( 'NONE', #12797, #41885, #9041, .T. ) ;
#78806=CARTESIAN_POINT ( 'NONE',  ( -46.92395915124596684, 18.83177588379273004, 15.01493731818062294 ) ) ;
#78810=CARTESIAN_POINT ( 'NONE',  ( 0.2959367164359796853, 12.99314498399917639, 51.71656300685955898 ) ) ;
#78813=AXIS2_PLACEMENT_3D ( 'NONE', #69601, #69074, #93343 ) ;
#78822=AXIS2_PLACEMENT_3D ( 'NONE', #78197, #59917, #43703 ) ;
#78829=STYLED_ITEM ( 'NONE', ( #320 ), #9022 ) ;
#78840=AXIS2_PLACEMENT_3D ( 'NONE', #4352, #84742, #10306 ) ;
#78842=CARTESIAN_POINT ( 'NONE',  ( -17.37779721166338476, 36.93489020264717482, 21.96297318349773775 ) ) ;
#78880=CARTESIAN_POINT ( 'NONE',  ( 46.86052085224882546, 18.87480283624687161, -15.15319613412887279 ) ) ;
#78913=CARTESIAN_POINT ( 'NONE',  ( 29.68315524076926337, -1.200000000000000030E-05, -40.85535821593530414 ) ) ;
#78916=FACE_BOUND ( 'NONE', #33799, .T. ) ;
#78921=ORIENTED_EDGE ( 'NONE', *, *, #48109, .T. ) ;
#78922=CYLINDRICAL_SURFACE ( 'NONE', #2191, 1.250000000000001110 ) ;
#78923=DIRECTION ( 'NONE',  ( -0.000000000000000000, 1.000000000000000000, -0.000000000000000000 ) ) ;
#78947=FACE_OUTER_BOUND ( 'NONE', #39275, .T. ) ;
#78949=VECTOR ( 'NONE', #103332, 1000.000000000000000 ) ;
#78954=CARTESIAN_POINT ( 'NONE',  ( -37.24675868481172358, 25.86585418676965276, 10.98683038162339010 ) ) ;
#78956=DIRECTION ( 'NONE',  ( 0.000000000000000000, 1.000000000000000000, 0.000000000000000000 ) ) ;
#78959=CARTESIAN_POINT ( 'NONE',  ( 37.88459826976592382, 27.77132929239739312, 10.98695786631084914 ) ) ;
#78990=EDGE_CURVE ( 'NONE', #17653, #12439, #83055, .T. ) ;
#78994=LINE ( 'NONE', #77408, #63206 ) ;
#79017=FILL_AREA_STYLE_COLOUR ( '', #9564 ) ;
#79025=CARTESIAN_POINT ( 'NONE',  ( -17.64329382111517575, 45.32481993297742662, -6.176472982800969902 ) ) ;
#79036=VERTEX_POINT ( 'NONE', #87210 ) ;
#79044=VERTEX_POINT ( 'NONE', #13285 ) ;
#79054=EDGE_CURVE ( 'NONE', #31379, #78599, #102342, .T. ) ;
#79057=LINE ( 'NONE', #55293, #77906 ) ;
#79059=CARTESIAN_POINT ( 'NONE',  ( -37.40770385488823280, 25.53062906199498983, -13.45617127781034839 ) ) ;
#79060=CARTESIAN_POINT ( 'NONE',  ( -8.559508646656389885, -1.200000000000000030E-05, -1.531152949374502859 ) ) ;
#79065=LINE ( 'NONE', #78524, #9860 ) ;
#79068=DIRECTION ( 'NONE',  ( 0.000000000000000000, 0.000000000000000000, 1.000000000000000000 ) ) ;
#79072=DIRECTION ( 'NONE',  ( 1.150791560227848297E-16, -0.3420201433256725987, 0.9396926207859068736 ) ) ;
#79079=CARTESIAN_POINT ( 'NONE',  ( -9.108279475058850494, 51.39276620778235838, 3.907239883328841312 ) ) ;
#79150=CARTESIAN_POINT ( 'NONE',  ( -7.620083193376602892, 52.13705811446491367, 1.952270494569938952 ) ) ;
#79158=SURFACE_STYLE_FILL_AREA ( #87268 ) ;
#79159=ORIENTED_EDGE ( 'NONE', *, *, #2268, .T. ) ;
#79188=B_SPLINE_CURVE_WITH_KNOTS ( 'NONE', 3,
 ( #82169, #81110, #105911, #23989, #56831, #1774, #51395, #17994, #44931, #43320, #35253, #68676, #76202, #67071, #20155, #76734, #26126, #43843, #11460, #3393 ),
 .UNSPECIFIED., .F., .F.,
 ( 4, 2, 2, 2, 2, 2, 2, 2, 2, 4 ),
 ( 0.003094771980465663586, 0.003598513203823375511, 0.004102254427181087001, 0.004605995650538798926, 0.005109736873896510850, 0.005361607485575363777, 0.005613478097254216703, 0.006117219320611923424, 0.006620960543969630144, 0.007124701767327335997 ),
 .UNSPECIFIED. ) ;
#79194=B_SPLINE_CURVE_WITH_KNOTS ( 'NONE', 3,
 ( #91835, #42210, #8778, #84272, #33094, #42748, #34695, #24995, #43281, #41684, #51360, #99367, #58404, #65959, #67569, #10368, #100450, #17957, #75092, #25545 ),
 .UNSPECIFIED., .F., .F.,
 ( 4, 2, 2, 2, 2, 2, 2, 2, 2, 4 ),
 ( 0.007623009076049266745, 0.008128762804230848030, 0.008381639668321639106, 0.008634516532412430181, 0.009140270260594005394, 0.009646023988775582342, 0.01015177771695715755, 0.01065753144513873450, 0.01116328517332031145, 0.01166903890150188666 ),
 .UNSPECIFIED. ) ;
#79200=CARTESIAN_POINT ( 'NONE',  ( -27.10511071441183262, 36.88665068479722464, 7.556984339686156460 ) ) ;
#79212=CARTESIAN_POINT ( 'NONE',  ( -48.15068916914997033, 11.33291430652583465, 14.35535821593516559 ) ) ;
#79218=CARTESIAN_POINT ( 'NONE',  ( -30.55529413189687915, 11.20957620317258474, 39.95174307499986099 ) ) ;
#79246=CARTESIAN_POINT ( 'NONE',  ( 30.10549840784159770, 7.858493733726954922, -42.03383688247146921 ) ) ;
#79267=CARTESIAN_POINT ( 'NONE',  ( 16.32418145836348700, 45.71594865110100869, -6.626690021756291848 ) ) ;
#79273=PRESENTATION_STYLE_ASSIGNMENT (( #62066 ) ) ;
#79274=CARTESIAN_POINT ( 'NONE',  ( -17.99621717127797993, 36.54019273113858191, -22.85642881224880796 ) ) ;
#79284=CARTESIAN_POINT ( 'NONE',  ( -30.90097930193297415, 13.60840423680624589, -41.14831600716862425 ) ) ;
#79317=DIRECTION ( 'NONE',  ( -0.000000000000000000, 1.000000000000000000, -0.000000000000000000 ) ) ;
#79335=VERTEX_POINT ( 'NONE', #14086 ) ;
#79339=CARTESIAN_POINT ( 'NONE',  ( 36.81804884527923605, 27.89004356318390876, 13.21991692395683771 ) ) ;
#79342=CARTESIAN_POINT ( 'NONE',  ( 17.53698998713263890, 34.16838527846118723, 24.04404631791792823 ) ) ;
#79375=DIRECTION ( 'NONE',  ( -0.000000000000000000, 1.000000000000000000, 0.000000000000000000 ) ) ;
#79411=PRODUCT ( '11. Strainer', '11. Strainer', '', ( #81586 ) ) ;
#79444=CARTESIAN_POINT ( 'NONE',  ( 27.26371139070421279, 34.70268990229791228, -7.556984339686200869 ) ) ;
#79446=FACE_BOUND ( 'NONE', #19893, .T. ) ;
#79453=PRESENTATION_STYLE_ASSIGNMENT (( #70315 ) ) ;
#79474=CARTESIAN_POINT ( 'NONE',  ( 10.28624191511840458, 45.38549880562042205, 15.40779740156149202 ) ) ;
#79488=CARTESIAN_POINT ( 'NONE',  ( -36.43961512855968010, 26.07474805434645049, 11.65918951012361582 ) ) ;
#79495=CARTESIAN_POINT ( 'NONE',  ( 11.30425253726989787, 43.19231108733225710, 14.90234394683685082 ) ) ;
#79519=EDGE_CURVE ( 'NONE', #79761, #20102, #11017, .T. ) ;
#79544=CARTESIAN_POINT ( 'NONE',  ( -15.52419239919893101, 37.09839268680908475, 22.76866006007168863 ) ) ;
#79551=CARTESIAN_POINT ( 'NONE',  ( 26.12466916459994337, 36.99826655557325950, 9.598780014887051237 ) ) ;
#79553=CARTESIAN_POINT ( 'NONE',  ( -23.84332598391540614, 27.93368204320126935, -30.86206213703136214 ) ) ;
#79554=ORIENTED_EDGE ( 'NONE', *, *, #83951, .F. ) ;
#79559=CARTESIAN_POINT ( 'NONE',  ( -24.45749910306381025, 25.45711128933222867, 31.59697626135422865 ) ) ;
#79562=UNCERTAINTY_MEASURE_WITH_UNIT (LENGTH_MEASURE( 1.000000000000000082E-05 ), #51343, 'distance_accuracy_value', 'NONE');
#79566=CARTESIAN_POINT ( 'NONE',  ( -0.3336719003891429058, 51.28288261117670288, -10.20757999058579379 ) ) ;
#79576=ORIENTED_EDGE ( 'NONE', *, *, #4254, .T. ) ;
#79581=VERTEX_POINT ( 'NONE', #92221 ) ;
#79602=CARTESIAN_POINT ( 'NONE',  ( -9.749599596588822692, 51.26841084474641974, 3.172565964336790056 ) ) ;
#79604=EDGE_LOOP ( 'NONE', ( #89338, #14001 ) ) ;
#79624=CARTESIAN_POINT ( 'NONE',  ( -0.6476328880971240487, 25.22743360806496682, -40.58242577266638307 ) ) ;
#79635=ORIENTED_EDGE ( 'NONE', *, *, #59618, .T. ) ;
#79643=ORIENTED_EDGE ( 'NONE', *, *, #32312, .F. ) ;
#79665=ORIENTED_EDGE ( 'NONE', *, *, #52359, .T. ) ;
#79684=ORIENTED_EDGE ( 'NONE', *, *, #40207, .T. ) ;
#79685=CARTESIAN_POINT ( 'NONE',  ( 1.116109309485880940, 9.313441320552295011, -51.08022315653880696 ) ) ;
#79687=CARTESIAN_POINT ( 'NONE',  ( 1.944839216437187431E-15, 45.30391365246044444, 18.75000000000001066 ) ) ;
#79702=ORIENTED_EDGE ( 'NONE', *, *, #86746, .F. ) ;
#79704=CARTESIAN_POINT ( 'NONE',  ( -27.42282820131847743, 36.77223311657368043, 7.587759719706580697 ) ) ;
#79721=CARTESIAN_POINT ( 'NONE',  ( -23.21751746555235840, 25.25267828308461304, -33.20617127781177658 ) ) ;
#79727=LINE ( 'NONE', #46129, #44376 ) ;
#79733=CARTESIAN_POINT ( 'NONE',  ( 0.000000000000000000, 41.79151656018385097, 0.000000000000000000 ) ) ;
#79761=VERTEX_POINT ( 'NONE', #57074 ) ;
#79775=FACE_BOUND ( 'NONE', #54926, .T. ) ;
#79780=CARTESIAN_POINT ( 'NONE',  ( -8.400871283442178594, 54.02033344610075005, -1.531152949374503525 ) ) ;
#79784=ADVANCED_FACE ( 'NONE', ( #42498 ), #57597, .F. ) ;
#79791=ORIENTED_EDGE ( 'NONE', *, *, #13692, .T. ) ;
#79804=CARTESIAN_POINT ( 'NONE',  ( 0.5678151344441708659, 27.34366627386414450, -40.61670413013122527 ) ) ;
#79808=ORIENTED_EDGE ( 'NONE', *, *, #27480, .F. ) ;
#79812=CARTESIAN_POINT ( 'NONE',  ( -30.22667580650565711, 12.95764659710599709, -41.98307762325180192 ) ) ;
#79813=EDGE_LOOP ( 'NONE', ( #1842, #42671, #85656, #70937 ) ) ;
#79814=CARTESIAN_POINT ( 'NONE',  ( -16.75187969033531132, 34.25544727262101219, -24.30698433968676753 ) ) ;
#79818=UNCERTAINTY_MEASURE_WITH_UNIT (LENGTH_MEASURE( 1.000000000000000082E-05 ), #31621, 'distance_accuracy_value', 'NONE');
#79854=DIRECTION ( 'NONE',  ( 0.000000000000000000, 0.000000000000000000, 1.000000000000000000 ) ) ;
#79863=ORIENTED_EDGE ( 'NONE', *, *, #104872, .T. ) ;
#79873=CIRCLE ( 'NONE', #33397, 24.55262289886175964 ) ;
#79882=LINE ( 'NONE', #80405, #86239 ) ;
#79895=EDGE_CURVE ( 'NONE', #3716, #79761, #91074, .T. ) ;
#79896=CARTESIAN_POINT ( 'NONE',  ( -28.20028738399506096, 34.17715485567774181, 9.432562058334550414 ) ) ;
#79915=FACE_BOUND ( 'NONE', #102881, .T. ) ;
#79934=LINE ( 'NONE', #103693, #76860 ) ;
#79959=CARTESIAN_POINT ( 'NONE',  ( 15.97435091970916510, 37.21084721865046419, 22.07459719473141746 ) ) ;
#79968=FACE_BOUND ( 'NONE', #67248, .T. ) ;
#79970=EDGE_CURVE ( 'NONE', #24510, #43850, #99779, .T. ) ;
#79981=( LENGTH_UNIT ( ) NAMED_UNIT ( * ) SI_UNIT ( .MILLI., .METRE. ) );
#79988=EDGE_LOOP ( 'NONE', ( #48181, #29988 ) ) ;
#79992=CARTESIAN_POINT ( 'NONE',  ( -38.81492354314366366, 27.33048476904497548, -12.09895268554974379 ) ) ;
#79995=CARTESIAN_POINT ( 'NONE',  ( -0.9985759808268045434, 14.07160882109565314, -51.25515926415730661 ) ) ;
#79997=CARTESIAN_POINT ( 'NONE',  ( 10.61948831387149461, 45.32774727476012799, 15.37414989828174861 ) ) ;
#80005=CARTESIAN_POINT ( 'NONE',  ( 48.02835407290414338, 14.94086294439859408, -16.85535821593631667 ) ) ;
#80009=CARTESIAN_POINT ( 'NONE',  ( 5.290067270632160756, 52.08006895350504806, -6.031152949374595451 ) ) ;
#80013=ADVANCED_FACE ( 'NONE', ( #76453 ), #84027, .F. ) ;
#80014=CARTESIAN_POINT ( 'NONE',  ( 37.72553331254036380, 27.55007976727166508, 13.45617127781008016 ) ) ;
#80025=CARTESIAN_POINT ( 'NONE',  ( -3.312116827214752676E-14, 12.91535575336970965, 51.75000000000017764 ) ) ;
#80028=CARTESIAN_POINT ( 'NONE',  ( -5.624108760328526913, 53.41997841376465317, 8.497405280055550847 ) ) ;
#80044=ORIENTED_EDGE ( 'NONE', *, *, #97411, .T. ) ;
#80059=CARTESIAN_POINT ( 'NONE',  ( 16.75187969033571989, 37.11970326878314097, 21.80698433968582961 ) ) ;
#80075=FILL_AREA_STYLE ('',( #88188 ) ) ;
#80080=CARTESIAN_POINT ( 'NONE',  ( 23.29983671023130398, 28.09898118347550877, -30.70617127781076405 ) ) ;
#80085=CARTESIAN_POINT ( 'NONE',  ( -0.1697841580037205145, 43.17852052592515832, -18.74127414289921845 ) ) ;
#80090=CARTESIAN_POINT ( 'NONE',  ( 6.692326732991420724E-21, 18.87382441218278828, -49.25000000000000000 ) ) ;
#80094=CARTESIAN_POINT ( 'NONE',  ( 21.96352229986338145, 25.92428843650098358, -31.83062960408818753 ) ) ;
#80105=CARTESIAN_POINT ( 'NONE',  ( 0.3378883892481922002, 54.29263816026539047, 7.785150801134277820 ) ) ;
#80129=CARTESIAN_POINT ( 'NONE',  ( 46.78679791479564898, 18.82552674760553657, 15.44534812371287913 ) ) ;
#80156=CYLINDRICAL_SURFACE ( 'NONE', #53018, 1.250000000000001110 ) ;
#80169=CARTESIAN_POINT ( 'NONE',  ( 26.78389989157783191, 34.86784115625223990, 7.588158416758067126 ) ) ;
#80177=ORIENTED_EDGE ( 'NONE', *, *, #65157, .T. ) ;
#80185=VECTOR ( 'NONE', #54137, 1000.000000000000000 ) ;
#80187=ORIENTED_EDGE ( 'NONE', *, *, #74999, .T. ) ;
#80198=CARTESIAN_POINT ( 'NONE',  ( 0.6420822604574439874, 26.01275107339925086, -38.42434469679283637 ) ) ;
#80209=AXIS2_PLACEMENT_3D ( 'NONE', #24378, #49125, #82576 ) ;
#80210=( NAMED_UNIT ( * ) PLANE_ANGLE_UNIT ( ) SI_UNIT ( $, .RADIAN. ) );
#80212=CARTESIAN_POINT ( 'NONE',  ( 37.56673239365870387, -1.200000000000000030E-05, 13.45617127780999134 ) ) ;
#80249=CARTESIAN_POINT ( 'NONE',  ( 7.482513037750662122, 54.13169591394895974, -3.436679040787894657 ) ) ;
#80265=CARTESIAN_POINT ( 'NONE',  ( 28.88581594204435632, 13.70410095367685877, 39.88976374582048834 ) ) ;
#80268=CARTESIAN_POINT ( 'NONE',  ( 29.09632818934771947, 14.54213905807124441, 41.96777332363164703 ) ) ;
#80275=CARTESIAN_POINT ( 'NONE',  ( -15.82358155159817947, 44.01628288912645814, -4.460636615200937349 ) ) ;
#80279=AXIS2_PLACEMENT_3D ( 'NONE', #75869, #870, #100671 ) ;
#80280=COLOUR_RGB ( '', 0.72549020, 0.75294118, 0.79215686) ;
#80284=LINE ( 'NONE', #5869, #14237 ) ;
#80316=CARTESIAN_POINT ( 'NONE',  ( -1.100444924853492656, 25.84109709204356520, 38.88573747810594483 ) ) ;
#80327=CARTESIAN_POINT ( 'NONE',  ( -30.55657801806768603, 16.37492758275029914, -39.95287151819763238 ) ) ;
#80339=CARTESIAN_POINT ( 'NONE',  ( 4.447904436602727607, 52.17731337436469374, -6.353523366743629275 ) ) ;
#80357=( GEOMETRIC_REPRESENTATION_CONTEXT ( 3 ) GLOBAL_UNCERTAINTY_ASSIGNED_CONTEXT ( ( #61090 ) ) GLOBAL_UNIT_ASSIGNED_CONTEXT ( ( #24212, #33896, #15549 ) ) REPRESENTATION_CONTEXT ( 'NONE', 'WORKASPACE' ) );
#80362=FILL_AREA_STYLE_COLOUR ( '', #103420 ) ;
#80367=FILL_AREA_STYLE ('',( #21650 ) ) ;
#80390=VERTEX_POINT ( 'NONE', #81945 ) ;
#80397=CARTESIAN_POINT ( 'NONE',  ( -28.61324058441433849, 13.48935699407721245, -40.19649855359993040 ) ) ;
#80404=CARTESIAN_POINT ( 'NONE',  ( -29.50183317260367488, 13.72085623994617798, -42.10535821593475703 ) ) ;
#80405=CARTESIAN_POINT ( 'NONE',  ( 7.715274834628325378E-15, 0.000000000000000000, -63.00000000000000000 ) ) ;
#80414=EDGE_CURVE ( 'NONE', #25485, #5108, #51586, .T. ) ;
#80434=ORIENTED_EDGE ( 'NONE', *, *, #9943, .T. ) ;
#80474=EDGE_LOOP ( 'NONE', ( #32109, #65600, #7703, #7033 ) ) ;
#80481=ORIENTED_EDGE ( 'NONE', *, *, #99537, .T. ) ;
#80510=EDGE_CURVE ( 'NONE', #86218, #93736, #67585, .T. ) ;
#80515=ORIENTED_EDGE ( 'NONE', *, *, #19193, .F. ) ;
#80521=CARTESIAN_POINT ( 'NONE',  ( -1.251098771870337023, 15.60329354122197110, -50.60675712933594639 ) ) ;
#80537=CARTESIAN_POINT ( 'NONE',  ( 0.7834125968129763695, 52.06998597394611750, -8.012555785356894944 ) ) ;
#80544=CARTESIAN_POINT ( 'NONE',  ( 10.36965645692189142, 43.24028602702204438, 15.40779740156149913 ) ) ;
#80587=CARTESIAN_POINT ( 'NONE',  ( 27.72817644236535983, 34.28350906085407956, 9.902989610335730220 ) ) ;
#80601=FILL_AREA_STYLE ('',( #30497 ) ) ;
#80605=CARTESIAN_POINT ( 'NONE',  ( 10.28624191511809371, 45.38549880562041494, -15.40779740156171762 ) ) ;
#80607=CARTESIAN_POINT ( 'NONE',  ( -23.21751746555247919, 25.98869614573810694, 30.70617127781050471 ) ) ;
#80609=MECHANICAL_DESIGN_GEOMETRIC_PRESENTATION_REPRESENTATION('',(#16888),#23760);
#80612=CARTESIAN_POINT ( 'NONE',  ( -1.218675684878021359, 43.73169810651692302, -17.17891848071411687 ) ) ;
#80617=CARTESIAN_POINT ( 'NONE',  ( 0.000000000000000000, 27.68727484027578356, 0.000000000000000000 ) ) ;
#80624=CARTESIAN_POINT ( 'NONE',  ( 46.96202111036839710, 13.62308641270886156, -14.94990935055657033 ) ) ;
#80682=( NAMED_UNIT ( * ) SI_UNIT ( $, .STERADIAN. ) SOLID_ANGLE_UNIT ( ) );
#80707=B_SPLINE_CURVE_WITH_KNOTS ( 'NONE', 3,
 ( #26226, #83876, #33226, #56926, #73099, #82277, #42355, #15956, #106012, #17033, #75242, #8389, #17571, #32158, #90376, #25693, #16489, #65572, #66101, #90920, #34303, #74179 ),
 .UNSPECIFIED., .F., .F.,
 ( 4, 2, 2, 2, 2, 2, 2, 2, 2, 2, 4 ),
 ( 0.006818712227115011036, 0.007321396069163314813, 0.007824079911211617722, 0.008326763753259920631, 0.008829447595308225274, 0.009080789516332376729, 0.009332131437356529918, 0.009583473358380681373, 0.009834815279404836297, 0.01033749912145313921, 0.01084018296350144211 ),
 .UNSPECIFIED. ) ;
#80719=EDGE_CURVE ( 'NONE', #32552, #38588, #3586, .T. ) ;
#80733=CARTESIAN_POINT ( 'NONE',  ( 0.3332995494436070127, 54.28974409543867097, -7.792324729589695131 ) ) ;
#80735=CARTESIAN_POINT ( 'NONE',  ( -1.012641722624960217, 34.34730419169671478, -29.25075072817579169 ) ) ;
#80737=EDGE_CURVE ( 'NONE', #100740, #5108, #54761, .T. ) ;
#80758=B_SPLINE_CURVE_WITH_KNOTS ( 'NONE', 3,
 ( #39989, #41045, #105770, #24881, #23292, #49113, #57735, #66375, #15169, #97670, #23836, #91211, #10, #8136, #82013, #32450, #56681, #97145, #49657, #15697, #65322, #98210, #90659, #24363, #80958, #89603, #48586, #72862, #7592, #7073 ),
 .UNSPECIFIED., .F., .F.,
 ( 4, 2, 2, 2, 2, 2, 2, 2, 2, 2, 2, 2, 2, 2, 4 ),
 ( 0.0006904739626665574049, 0.001153765004792713707, 0.001617056046918869793, 0.002543638131171178061, 0.003470220215423487631, 0.004396802299675795465, 0.005323384383928104167, 0.005786675426054258518, 0.006249966468180413737, 0.006713257510306568088, 0.006944903031369652202, 0.007176548552432735449, 0.007408194073495819564, 0.007639839594558903678, 0.008103130636685064100 ),
 .UNSPECIFIED. ) ;
#80762=CARTESIAN_POINT ( 'NONE',  ( 21.96335440039715436, 25.92421299530558798, 31.83099838201997756 ) ) ;
#80775=B_SPLINE_CURVE_WITH_KNOTS ( 'NONE', 3,
 ( #67774, #99050, #25768, #91526, #100660, #16025, #33298, #25216, #26821, #33837, #74781, #34379, #106623, #7925, #59693, #49982, #67252, #40830, #100130, #24677, #73720, #98531 ),
 .UNSPECIFIED., .F., .F.,
 ( 4, 2, 2, 2, 2, 2, 2, 2, 2, 2, 4 ),
 ( 0.003156676467191279339, 0.003660387902065995007, 0.004164099336940710674, 0.004667810771815426342, 0.005171522206690142009, 0.005423377924127489869, 0.005675233641564837728, 0.005927089359002185587, 0.006178945076439534313, 0.006682656511314223093, 0.007186367946188911872 ),
 .UNSPECIFIED. ) ;
#80778=SURFACE_STYLE_USAGE ( .BOTH. , #103471 ) ;
#80813=CARTESIAN_POINT ( 'NONE',  ( -15.66240720622342053, 43.86916268644461070, -6.198733367779965420 ) ) ;
#80814=CARTESIAN_POINT ( 'NONE',  ( -27.26388916004784235, 36.55153124001466836, -10.05698433968606054 ) ) ;
#80830=CARTESIAN_POINT ( 'NONE',  ( 11.07247204453428147, 43.17212549673661925, -15.14411814079721452 ) ) ;
#80837=CARTESIAN_POINT ( 'NONE',  ( -16.75187969033554936, -1.200000000000000030E-05, -24.30698433968596106 ) ) ;
#80848=ORIENTED_EDGE ( 'NONE', *, *, #46795, .F. ) ;
#80868=CARTESIAN_POINT ( 'NONE',  ( -17.25401547865008212, 43.52747190215453088, 4.305687115457426550 ) ) ;
#80899=DIRECTION ( 'NONE',  ( -0.000000000000000000, 1.000000000000000000, -0.000000000000000000 ) ) ;
#80902=CARTESIAN_POINT ( 'NONE',  ( -15.96643448957893874, 35.08561881503606372, 22.07017619469237246 ) ) ;
#80915=DIRECTION ( 'NONE',  ( 0.000000000000000000, 1.000000000000000000, 0.000000000000000000 ) ) ;
#80935=STYLED_ITEM ( 'NONE', ( #23945 ), #77775 ) ;
#80937=CARTESIAN_POINT ( 'NONE',  ( 0.3380568183126133053, 26.06491301246339987, 38.28514637226837891 ) ) ;
#80942=CARTESIAN_POINT ( 'NONE',  ( -28.98628617572742527, 14.82338180310327225, -41.90038909576689008 ) ) ;
#80958=CARTESIAN_POINT ( 'NONE',  ( 29.14598918812165351, 18.82621124954753000, -39.72463063980563902 ) ) ;
#80965=( LENGTH_UNIT ( ) NAMED_UNIT ( * ) SI_UNIT ( .MILLI., .METRE. ) );
#80998=CARTESIAN_POINT ( 'NONE',  ( -6.366267295126388781, 53.78408749334437999, -6.625582353314952044 ) ) ;
#81009=ORIENTED_EDGE ( 'NONE', *, *, #8471, .T. ) ;
#81013=ORIENTED_EDGE ( 'NONE', *, *, #20547, .T. ) ;
#81016=DIRECTION ( 'NONE',  ( 0.000000000000000000, 0.000000000000000000, -1.000000000000000000 ) ) ;
#81018=CARTESIAN_POINT ( 'NONE',  ( 1.093953403843523242, 43.39644527504638916, -18.11016995274446373 ) ) ;
#81025=FACE_BOUND ( 'NONE', #92737, .T. ) ;
#81091=CARTESIAN_POINT ( 'NONE',  ( -9.781457975134252081, 51.26649664470197365, -3.093893760390039827 ) ) ;
#81110=CARTESIAN_POINT ( 'NONE',  ( 27.26387865205136762, 36.83098680558968852, -7.556984339686136920 ) ) ;
#81112=EDGE_CURVE ( 'NONE', #91653, #100209, #14706, .T. ) ;
#81121=CARTESIAN_POINT ( 'NONE',  ( 28.35788784190019385, 34.17668351136055804, 8.951742554474883207 ) ) ;
#81133=CARTESIAN_POINT ( 'NONE',  ( 0.6437396368863147478, 35.01890123696630042, 27.41570566740858794 ) ) ;
#81134=CARTESIAN_POINT ( 'NONE',  ( -16.96000587140901317, 45.76999459631175426, -4.188133835394263649 ) ) ;
#81140=CARTESIAN_POINT ( 'NONE',  ( -4.963060401946981948, 52.14582460415977749, -6.071815141832103357 ) ) ;
#81156=CARTESIAN_POINT ( 'NONE',  ( 46.79100380508914725, 13.36652303332992275, -15.81652940118055284 ) ) ;
#81162=SURFACE_SIDE_STYLE ('',( #106502 ) ) ;
#81170=CARTESIAN_POINT ( 'NONE',  ( -9.147602679903698686, 44.02377986342360572, 13.63549886291783508 ) ) ;
#81182=CARTESIAN_POINT ( 'NONE',  ( 0.000000000000000000, 0.000000000000000000, 63.00000000000000000 ) ) ;
#81184=CARTESIAN_POINT ( 'NONE',  ( 47.57405721301110901, 17.76112721455492505, 14.43871205879827180 ) ) ;
#81185=AXIS2_PLACEMENT_3D ( 'NONE', #47569, #88054, #5529 ) ;
#81202=CARTESIAN_POINT ( 'NONE',  ( -0.3344869795709685123, 26.06211867389157177, -38.29264199900394772 ) ) ;
#81209=CARTESIAN_POINT ( 'NONE',  ( 6.134138981404819724, 53.39921523940185466, 8.206960596703554600 ) ) ;
#81214=CARTESIAN_POINT ( 'NONE',  ( 30.29343180852530537, 12.93058661249367702, 41.94895705695244459 ) ) ;
#81223=CARTESIAN_POINT ( 'NONE',  ( 15.49777301142466968, 34.92625999296609507, 22.93171183856468787 ) ) ;
#81283=CARTESIAN_POINT ( 'NONE',  ( 22.45593966533183306, 25.48384861978522409, 32.96011743078131673 ) ) ;
#81287=ADVANCED_FACE ( 'NONE', ( #9271 ), #83694, .F. ) ;
#81294=CARTESIAN_POINT ( 'NONE',  ( 9.522120649308408957, 45.61249502152110580, -15.15976961885343499 ) ) ;
#81330=DIRECTION ( 'NONE',  ( -0.000000000000000000, 1.000000000000000000, -0.000000000000000000 ) ) ;
#81332=CARTESIAN_POINT ( 'NONE',  ( -28.45521705596416950, 17.07436234393353303, 41.11936415921380927 ) ) ;
#81334=CARTESIAN_POINT ( 'NONE',  ( -27.42214779293654203, 36.77249561759260388, -7.587514376366431890 ) ) ;
#81346=B_SPLINE_CURVE_WITH_KNOTS ( 'NONE', 3,
 ( #74528, #604, #9258, #23902, #24953, #41115, #32518, #26047, #65390, #75601, #91797, #1699, #90730, #16846, #66447, #50261, #83163, #24439, #25499, #1147, #66994, #34655 ),
 .UNSPECIFIED., .F., .F.,
 ( 4, 2, 2, 2, 2, 2, 2, 2, 2, 2, 4 ),
 ( 0.006964068074043565891, 0.007215909760093224858, 0.007467751446142882957, 0.007971434818242206094, 0.008475118190341527497, 0.008726959876391188198, 0.008978801562440848899, 0.009482484934540168567, 0.009986168306639488235, 0.01048985167873880964, 0.01099353505083812930 ),
 .UNSPECIFIED. ) ;
#81350=CARTESIAN_POINT ( 'NONE',  ( 10.69678357099577859, 43.19292212010790877, -15.34149409327725877 ) ) ;
#81357=AXIS2_PLACEMENT_3D ( 'NONE', #88171, #22926, #55247 ) ;
#81374=STYLED_ITEM ( 'NONE', ( #88224 ), #13026 ) ;
#81377=CARTESIAN_POINT ( 'NONE',  ( -1.219990203180580712, 25.73133127544792842, 39.18389656347510197 ) ) ;
#81389=CARTESIAN_POINT ( 'NONE',  ( -17.88153669719137540, 43.22040693656918364, 5.216588465419869536 ) ) ;
#81396=CARTESIAN_POINT ( 'NONE',  ( -10.28624191511816832, 43.25714326066847804, -15.40779740156204980 ) ) ;
#81400=ORIENTED_EDGE ( 'NONE', *, *, #45715, .F. ) ;
#81405=CARTESIAN_POINT ( 'NONE',  ( 36.34514833454822735, 28.20980986297035997, -11.89218482807859623 ) ) ;
#81406=ORIENTED_EDGE ( 'NONE', *, *, #46154, .T. ) ;
#81415=CARTESIAN_POINT ( 'NONE',  ( 23.05189055320607849, 27.41800202946304310, 33.19783182242376540 ) ) ;
#81451=CARTESIAN_POINT ( 'NONE',  ( 38.50591796967749758, 25.20373685550617182, 13.03523540767606370 ) ) ;
#81461=CARTESIAN_POINT ( 'NONE',  ( 23.61912243982836301, 25.88172202072039241, 30.76971916150039377 ) ) ;
#81468=AXIS2_PLACEMENT_3D ( 'NONE', #32800, #82382, #47875 ) ;
#81478=B_SPLINE_CURVE_WITH_KNOTS ( 'NONE', 3,
 ( #97006, #80814, #97516, #63602, #23146, #7444, #48443, #64138, #6927, #30715, #40360, #105107, #72203, #31248, #20664, #23681, #88922, #88397, #56528, #81334, #89458, #73239 ),
 .UNSPECIFIED., .F., .F.,
 ( 4, 2, 2, 2, 2, 2, 2, 2, 2, 2, 4 ),
 ( 0.007109265277489604240, 0.007613110377180124996, 0.008116955476870645753, 0.008368878026715901794, 0.008620800576561156101, 0.009124645676251668183, 0.009376568226096925959, 0.009628490775942183735, 0.01013233587563269408, 0.01063618097532320617, 0.01114002607501371825 ),
 .UNSPECIFIED. ) ;
#81511=CARTESIAN_POINT ( 'NONE',  ( 17.63841679208134394, 43.19886265510177026, -6.169146188730260327 ) ) ;
#81513=CARTESIAN_POINT ( 'NONE',  ( -5.453027751480597374, 54.16931316411591979, -6.031152949374162020 ) ) ;
#81515=CARTESIAN_POINT ( 'NONE',  ( -23.54225815529405708, 28.03385386361086873, 30.74635459162657014 ) ) ;
#81549=CARTESIAN_POINT ( 'NONE',  ( -22.88936581296984585, 28.17682283790767173, -30.74716342950141623 ) ) ;
#81560=ORIENTED_EDGE ( 'NONE', *, *, #80737, .F. ) ;
#81582=CARTESIAN_POINT ( 'NONE',  ( 0.3342036119824616791, 52.16127839274962952, -7.792586909974158260 ) ) ;
#81586=PRODUCT_CONTEXT ( 'NONE', #82395, 'mechanical' ) ;
#81592=COLOUR_RGB ( '', 0.66274510, 0.83137255, 0.94901961) ;
#81596=DIRECTION ( 'NONE',  ( 1.150791560227848297E-16, -0.3420201433256725987, 0.9396926207859068736 ) ) ;
#81601=CARTESIAN_POINT ( 'NONE',  ( -9.635262854140592026, 51.40918690193957019, -2.123770696076897391 ) ) ;
#81603=CARTESIAN_POINT ( 'NONE',  ( -6.368327914470341966, 53.78267287650600537, 6.628995654898029777 ) ) ;
#81644=SURFACE_STYLE_FILL_AREA ( #82189 ) ;
#81654=CARTESIAN_POINT ( 'NONE',  ( -4.063202461714976899, 52.05771371934300618, -6.989737321421222838 ) ) ;
#81656=EDGE_CURVE ( 'NONE', #93736, #86218, #88141, .T. ) ;
#81660=CARTESIAN_POINT ( 'NONE',  ( 0.6465847505401471906, 51.32305258032151585, 10.08284153374933467 ) ) ;
#81665=CARTESIAN_POINT ( 'NONE',  ( 0.4150347205025879394, 45.32703121288628978, 18.68203640562379064 ) ) ;
#81678=CARTESIAN_POINT ( 'NONE',  ( 1.248908473850341538, 53.88172734546416365, 8.832198851183429511 ) ) ;
#81680=CARTESIAN_POINT ( 'NONE',  ( -37.56673239365849781, 27.88554838446201600, 10.95617127781066102 ) ) ;
#81684=CARTESIAN_POINT ( 'NONE',  ( 27.10511071441176867, -1.200000000000000030E-05, -8.806984339686344754 ) ) ;
#81685=ORIENTED_EDGE ( 'NONE', *, *, #95627, .T. ) ;
#81686=CARTESIAN_POINT ( 'NONE',  ( -10.20362117609958474, 43.27384007481603589, 15.40779740156164834 ) ) ;
#81691=FACE_OUTER_BOUND ( 'NONE', #85676, .T. ) ;
#81729=CARTESIAN_POINT ( 'NONE',  ( 16.75187969033441604, 36.38380281757147827, -24.30698433969211791 ) ) ;
#81759=( LENGTH_UNIT ( ) NAMED_UNIT ( * ) SI_UNIT ( .MILLI., .METRE. ) );
#81764=UNCERTAINTY_MEASURE_WITH_UNIT (LENGTH_MEASURE( 1.000000000000000082E-05 ), #56235, 'distance_accuracy_value', 'NONE');
#81771=CARTESIAN_POINT ( 'NONE',  ( 10.28624191511840280, 46.12099395432375104, 12.90779740156148847 ) ) ;
#81784=B_SPLINE_CURVE_WITH_KNOTS ( 'NONE', 3,
 ( #57408, #82764, #65525, #100535, #26698, #33705, #98412, #98925, #25086, #16980, #49858, #65530, #39148, #96323, #39674, #90330, #97348, #72028, #15908, #81680 ),
 .UNSPECIFIED., .F., .F.,
 ( 4, 2, 2, 2, 2, 2, 2, 2, 2, 4 ),
 ( 0.003017764547143146799, 0.003522452000831426643, 0.004027139454519706487, 0.004531826908207986331, 0.005036514361896267042, 0.005288858088740406097, 0.005541201815584546886, 0.006045889269272826730, 0.006550576722961107441, 0.007055264176649387285 ),
 .UNSPECIFIED. ) ;
#81798=CARTESIAN_POINT ( 'NONE',  ( 46.86466781827407857, 13.70365495135300016, 15.14281811549618340 ) ) ;
#81807=CARTESIAN_POINT ( 'NONE',  ( 22.13738121435902428, 25.65584458174092930, 32.60528274926500814 ) ) ;
#81809=( NAMED_UNIT ( * ) PLANE_ANGLE_UNIT ( ) SI_UNIT ( $, .RADIAN. ) );
#81810=ORIENTED_EDGE ( 'NONE', *, *, #21161, .T. ) ;
#81828=VERTEX_POINT ( 'NONE', #60916 ) ;
#81831=CARTESIAN_POINT ( 'NONE',  ( 7.315042831255333944, 54.29841258322443309, -2.636459647254548511 ) ) ;
#81832=UNCERTAINTY_MEASURE_WITH_UNIT (LENGTH_MEASURE( 1.000000000000000082E-05 ), #101047, 'distance_accuracy_value', 'NONE');
#81849=CARTESIAN_POINT ( 'NONE',  ( 29.49969761086837039, 8.554442461696856626, 42.10535821593482808 ) ) ;
#81853=CARTESIAN_POINT ( 'NONE',  ( 28.43348347353515493, 17.76907357228465756, 40.77956405912743065 ) ) ;
#81858=CYLINDRICAL_SURFACE ( 'NONE', #28757, 1.250000000000001110 ) ;
#81859=CARTESIAN_POINT ( 'NONE',  ( -29.07959870117770862, 18.85554092054060149, 39.75803059074582535 ) ) ;
#81860=CARTESIAN_POINT ( 'NONE',  ( -15.43380028733834841, 44.00385025579843301, -5.763122072303904275 ) ) ;
#81865=B_SPLINE_CURVE_WITH_KNOTS ( 'NONE', 3,
 ( #768, #90356, #57434, #33735, #82256, #97372, #241, #56370, #39699, #23533, #42868, #10493, #52015, #18624, #36421, #94080, #75219, #51484, #50939, #92474, #76822, #18080 ),
 .UNSPECIFIED., .F., .F.,
 ( 4, 2, 2, 2, 2, 2, 2, 2, 2, 2, 4 ),
 ( 0.002861759807556418182, 0.003365147677020101629, 0.003868535546483784643, 0.004875311285411144599, 0.005127005220142985889, 0.005378699154874826312, 0.005630393089606666734, 0.005882087024338508024, 0.006385474893802188870, 0.006637168828534030160, 0.006888862763265871450 ),
 .UNSPECIFIED. ) ;
#81894=CARTESIAN_POINT ( 'NONE',  ( -46.89572507581434024, 12.86406951795958520, 16.16260000396507834 ) ) ;
#81902=CYLINDRICAL_SURFACE ( 'NONE', #31168, 1.250000000000001110 ) ;
#81911=CARTESIAN_POINT ( 'NONE',  ( 1.011040197152363929, 28.02085159631482369, -38.74701891561100098 ) ) ;
#81921=ORIENTED_EDGE ( 'NONE', *, *, #53077, .T. ) ;
#81925=CARTESIAN_POINT ( 'NONE',  ( -5.612570156906559582, 51.99084277534022647, -6.070783327326104484 ) ) ;
#81938=CARTESIAN_POINT ( 'NONE',  ( 9.323069064330987032, 51.33816002439836268, 3.784642684411407831 ) ) ;
#81945=CARTESIAN_POINT ( 'NONE',  ( -27.10511071441183617, 34.75829513984614039, 7.556984339678626483 ) ) ;
#81958=( GEOMETRIC_REPRESENTATION_CONTEXT ( 3 ) GLOBAL_UNCERTAINTY_ASSIGNED_CONTEXT ( ( #15994 ) ) GLOBAL_UNIT_ASSIGNED_CONTEXT ( ( #104552, #96999, #88907 ) ) REPRESENTATION_CONTEXT ( 'NONE', 'WORKASPACE' ) );
#81961=CARTESIAN_POINT ( 'NONE',  ( -4.044615342289579196, 54.03559733567681178, 7.473308606069148929 ) ) ;
#81963=CARTESIAN_POINT ( 'NONE',  ( -38.54780640362174893, 25.36754422839498702, -11.41492091183227586 ) ) ;
#81971=( GEOMETRIC_REPRESENTATION_CONTEXT ( 3 ) GLOBAL_UNCERTAINTY_ASSIGNED_CONTEXT ( ( #60228 ) ) GLOBAL_UNIT_ASSIGNED_CONTEXT ( ( #106042, #88301, #39747 ) ) REPRESENTATION_CONTEXT ( 'NONE', 'WORKASPACE' ) );
#81983=FILL_AREA_STYLE_COLOUR ( '', #2614 ) ;
#81989=CARTESIAN_POINT ( 'NONE',  ( 0.5674423241763830728, 26.02818786376027660, 38.38311945757907040 ) ) ;
#82003=CARTESIAN_POINT ( 'NONE',  ( 4.036225360327396317, 54.13868825708020438, 7.154357340812832255 ) ) ;
#82006=CARTESIAN_POINT ( 'NONE',  ( -4.093111970549610845, 52.07643660103700256, 6.911618801915782484 ) ) ;
#82009=EDGE_CURVE ( 'NONE', #9858, #41746, #31305, .T. ) ;
#82013=CARTESIAN_POINT ( 'NONE',  ( 28.43952395724156190, 17.90362770311681828, -40.70652153699805353 ) ) ;
#82020=VECTOR ( 'NONE', #47218, 1000.000000000000227 ) ;
#82036=CARTESIAN_POINT ( 'NONE',  ( -3.311033882356798252E-14, 37.21016666119783167, -27.24999999999961986 ) ) ;
#82040=VECTOR ( 'NONE', #9446, 1000.000000000000000 ) ;
#82051=EDGE_LOOP ( 'NONE', ( #32635, #29315, #87433, #71204 ) ) ;
#82062=CARTESIAN_POINT ( 'NONE',  ( 16.64348903516512834, 43.75610143575153899, -4.157797401561768247 ) ) ;
#82068=CARTESIAN_POINT ( 'NONE',  ( -24.29723907929130178, 27.70462894893682204, 31.30642834101307770 ) ) ;
#82080=CARTESIAN_POINT ( 'NONE',  ( -49.19734730806123224, 7.744866885593231665, -16.05423930868188265 ) ) ;
#82081=EDGE_CURVE ( 'NONE', #101431, #67639, #38763, .T. ) ;
#82084=CARTESIAN_POINT ( 'NONE',  ( -37.88754858252848834, 25.36997296304242511, 13.42524253834038284 ) ) ;
#82109=AXIS2_PLACEMENT_3D ( 'NONE', #98430, #7816, #106516 ) ;
#82116=CARTESIAN_POINT ( 'NONE',  ( 11.53045486031959754, 45.53936973856496451, 13.95636496209353794 ) ) ;
#82117=EDGE_CURVE ( 'NONE', #12173, #86477, #58301, .T. ) ;
#82118=EDGE_LOOP ( 'NONE', ( #86026, #98173 ) ) ;
#82152=CARTESIAN_POINT ( 'NONE',  ( 36.62770931978901956, 26.04034622320522274, 11.37685887764211046 ) ) ;
#82169=CARTESIAN_POINT ( 'NONE',  ( 27.10511071441177222, 36.88665068479793518, -7.556984339679249985 ) ) ;
#82181=CARTESIAN_POINT ( 'NONE',  ( 28.23128044651457458, 34.17513526713322847, 9.355917131510365081 ) ) ;
#82189=FILL_AREA_STYLE ('',( #31562 ) ) ;
#82192=CARTESIAN_POINT ( 'NONE',  ( -17.89001738438791733, 45.34603189753767083, -5.216234635019829646 ) ) ;
#82193=( NAMED_UNIT ( * ) PLANE_ANGLE_UNIT ( ) SI_UNIT ( $, .RADIAN. ) );
#82199=CARTESIAN_POINT ( 'NONE',  ( -4.206614587654213366, 51.73457005021325017, -7.924384222582498971 ) ) ;
#82205=CARTESIAN_POINT ( 'NONE',  ( 0.3340480107103283580, 52.16129231206663519, 7.792553844401801655 ) ) ;
#82207=( LENGTH_UNIT ( ) NAMED_UNIT ( * ) SI_UNIT ( .MILLI., .METRE. ) );
#82211=CARTESIAN_POINT ( 'NONE',  ( 8.559508646656350805, 53.68473964988125857, -4.031152949374623873 ) ) ;
#82217=DIRECTION ( 'NONE',  ( -0.000000000000000000, 1.000000000000000000, -0.000000000000000000 ) ) ;
#82227=CARTESIAN_POINT ( 'NONE',  ( -8.559508646656370345, 53.68473964988125857, -4.031152949374577688 ) ) ;
#82235=LINE ( 'NONE', #16994, #99392 ) ;
#82253=LINE ( 'NONE', #239, #59249 ) ;
#82256=CARTESIAN_POINT ( 'NONE',  ( 6.047133232705633965, 51.82847809756811586, -6.273795380418080825 ) ) ;
#82265=DIRECTION ( 'NONE',  ( 0.000000000000000000, 0.000000000000000000, 1.000000000000000000 ) ) ;
#82271=EDGE_CURVE ( 'NONE', #17374, #44553, #11675, .T. ) ;
#82277=CARTESIAN_POINT ( 'NONE',  ( -9.540057778879830863, 53.58151691157907948, 1.989242606643393474 ) ) ;
#82301=CARTESIAN_POINT ( 'NONE',  ( 16.75187969033571989, 34.99134772383131065, 21.80698433968582961 ) ) ;
#82315=CARTESIAN_POINT ( 'NONE',  ( 8.559508646656407649, -1.200000000000000030E-05, 1.531152949374444239 ) ) ;
#82340=CARTESIAN_POINT ( 'NONE',  ( -0.1696942726969380422, 35.07848972003357346, -27.25872117772604852 ) ) ;
#82366=FILL_AREA_STYLE_COLOUR ( '', #20409 ) ;
#82368=ORIENTED_EDGE ( 'NONE', *, *, #96960, .T. ) ;
#82382=DIRECTION ( 'NONE',  ( -0.000000000000000000, 1.000000000000000000, -0.000000000000000000 ) ) ;
#82386=CARTESIAN_POINT ( 'NONE',  ( 7.370082443888056112, 54.30877847509226086, -2.387610232865688520 ) ) ;
#82395=APPLICATION_CONTEXT ( 'automotive_design' ) ;
#82405=CARTESIAN_POINT ( 'NONE',  ( 29.35352825446852165, 8.824359840618530626, 42.06917583815489081 ) ) ;
#82410=CARTESIAN_POINT ( 'NONE',  ( 28.88579667808768647, 18.87341229088494643, 39.88979553324821836 ) ) ;
#82415=EDGE_CURVE ( 'NONE', #101117, #67401, #31491, .T. ) ;
#82416=CARTESIAN_POINT ( 'NONE',  ( -48.02835407290534420, -1.200000000000000030E-05, -15.60535821593460248 ) ) ;
#82417=CARTESIAN_POINT ( 'NONE',  ( -28.52991250593621331, 16.51520549712914132, 41.35291476382062115 ) ) ;
#82422=ADVANCED_FACE ( 'NONE', ( #57302 ), #74029, .F. ) ;
#82430=CARTESIAN_POINT ( 'NONE',  ( 5.290067270632322405, -1.200000000000000030E-05, 6.031152949374479100 ) ) ;
#82433=( NAMED_UNIT ( * ) PLANE_ANGLE_UNIT ( ) SI_UNIT ( $, .RADIAN. ) );
#82444=CARTESIAN_POINT ( 'NONE',  ( -47.44718022415302272, 11.18620753528886524, 16.71882890723488302 ) ) ;
#82459=CARTESIAN_POINT ( 'NONE',  ( -30.75723595955501111, 13.12755156482207397, 41.50738620754120944 ) ) ;
#82466=EDGE_CURVE ( 'NONE', #33697, #89914, #10354, .T. ) ;
#82475=EDGE_LOOP ( 'NONE', ( #100127, #88428, #52734, #95365 ) ) ;
#82478=DIRECTION ( 'NONE',  ( -0.000000000000000000, 1.000000000000000000, -0.000000000000000000 ) ) ;
#82486=CARTESIAN_POINT ( 'NONE',  ( -28.88699125077563679, 13.70431814614562249, 39.88880000601581344 ) ) ;
#82492=CARTESIAN_POINT ( 'NONE',  ( 9.807764809528846328, 51.30006693791943917, 2.674187944274665441 ) ) ;
#82535=( GEOMETRIC_REPRESENTATION_CONTEXT ( 3 ) GLOBAL_UNCERTAINTY_ASSIGNED_CONTEXT ( ( #7420 ) ) GLOBAL_UNIT_ASSIGNED_CONTEXT ( ( #62957, #45194, #21983 ) ) REPRESENTATION_CONTEXT ( 'NONE', 'WORKASPACE' ) );
#82553=CARTESIAN_POINT ( 'NONE',  ( 4.649619579745470688, 54.30983937696358055, 6.194660934072837577 ) ) ;
#82556=VECTOR ( 'NONE', #49350, 1000.000000000000000 ) ;
#82576=DIRECTION ( 'NONE',  ( 0.000000000000000000, 0.000000000000000000, -1.000000000000000000 ) ) ;
#82578=EDGE_LOOP ( 'NONE', ( #98493, #43291, #39169, #78543 ) ) ;
#82585=DIRECTION ( 'NONE',  ( 0.000000000000000000, 1.000000000000000000, 0.000000000000000000 ) ) ;
#82600=CARTESIAN_POINT ( 'NONE',  ( 0.000000000000000000, 38.67090180175566871, -23.23666318551310539 ) ) ;
#82614=CARTESIAN_POINT ( 'NONE',  ( -24.41558313457672469, 27.38491394452228533, 32.32218024782103072 ) ) ;
#82620=DIRECTION ( 'NONE',  ( 0.000000000000000000, 0.000000000000000000, 1.000000000000000000 ) ) ;
#82629=CARTESIAN_POINT ( 'NONE',  ( 15.64878411475365638, 36.78373704832291224, 23.72567384382491795 ) ) ;
#82638=CARTESIAN_POINT ( 'NONE',  ( -5.290067270632216712, -1.200000000000000030E-05, 7.281152949374556371 ) ) ;
#82642=ORIENTED_EDGE ( 'NONE', *, *, #53315, .F. ) ;
#82644=CARTESIAN_POINT ( 'NONE',  ( 25.97856261898818531, 37.20666516320237349, -8.258827374226497042 ) ) ;
#82660=DIRECTION ( 'NONE',  ( 0.000000000000000000, 1.000000000000000000, -0.000000000000000000 ) ) ;
#82661=CARTESIAN_POINT ( 'NONE',  ( 38.56639310406619359, 27.31833143340870507, -12.97492099455193149 ) ) ;
#82677=CARTESIAN_POINT ( 'NONE',  ( 49.26505482459812413, 8.072780847947159444, 15.39015249100645732 ) ) ;
#82686=SURFACE_STYLE_USAGE ( .BOTH. , #8791 ) ;
#82706=B_SPLINE_CURVE_WITH_KNOTS ( 'NONE', 3,
 ( #81771, #7893, #40800, #73693, #74753, #106596, #32745, #8433, #98500, #65617, #832, #33803, #24650, #301, #57503, #90425, #41332, #58043, #74224, #33269, #99022, #53682 ),
 .UNSPECIFIED., .F., .F.,
 ( 4, 2, 2, 2, 2, 2, 2, 2, 2, 2, 4 ),
 ( 0.003083058008555209992, 0.003587558145623159604, 0.003839808214157137880, 0.004092058282691116156, 0.004596558419759067503, 0.004848808488293042743, 0.005101058556827017983, 0.006110058830962923279, 0.006614558968030877228, 0.006866809036564849866, 0.007119059105098823372 ),
 .UNSPECIFIED. ) ;
#82745=B_SPLINE_CURVE_WITH_KNOTS ( 'NONE', 3,
 ( #41423, #74839, #18240, #51095, #84015, #32831, #393, #33360, #73783, #106684, #65710, #98592, #24738, #90510, #91063, #48223, #55768, #63914, #88177, #104895 ),
 .UNSPECIFIED., .F., .F.,
 ( 4, 2, 2, 2, 2, 2, 2, 2, 2, 4 ),
 ( 0.002817615579195576793, 0.003321638736722653390, 0.003825661894249729553, 0.004329685051776806584, 0.004833708209303882314, 0.005337731366830958911, 0.005589742945594498510, 0.005841754524358047651, 0.006345777681885138993, 0.006849800839412230336 ),
 .UNSPECIFIED. ) ;
#82746=CARTESIAN_POINT ( 'NONE',  ( -0.9990332814551574625, 14.07295282070545994, 51.25458646076748437 ) ) ;
#82753=CARTESIAN_POINT ( 'NONE',  ( 1.248878403638263412, 16.16541945263409019, -50.37088816262370727 ) ) ;
#82754=ORIENTED_EDGE ( 'NONE', *, *, #67974, .T. ) ;
#82755=B_SPLINE_CURVE_WITH_KNOTS ( 'NONE', 3,
 ( #43719, #3271, #37263, #102498, #60469, #4328, #36211, #94419, #52876, #19499, #70659, #53418, #103033, #103553, #70126, #93874, #93347, #68548 ),
 .UNSPECIFIED., .F., .F.,
 ( 4, 2, 2, 2, 2, 2, 2, 2, 4 ),
 ( 0.007125446813973600017, 0.007629686116325595964, 0.008133925418677592778, 0.008638164721029588725, 0.009142404023381584671, 0.009646643325733580618, 0.01015088262808557656, 0.01065512193043757251, 0.01115936123278956846 ),
 .UNSPECIFIED. ) ;
#82757=CARTESIAN_POINT ( 'NONE',  ( -9.295423129716056110, 45.72519545954835962, 14.93632663516901893 ) ) ;
#82764=CARTESIAN_POINT ( 'NONE',  ( -37.40675222085440055, 27.65931068607314458, 13.45617127781066458 ) ) ;
#82776=CARTESIAN_POINT ( 'NONE',  ( -9.088874843304111550, 43.98892613297807230, 13.78954861775553731 ) ) ;
#82778=ADVANCED_FACE ( 'NONE', ( #20648 ), #61598, .F. ) ;
#82783=EDGE_LOOP ( 'NONE', ( #72884, #51315, #104708, #99167 ) ) ;
#82831=CARTESIAN_POINT ( 'NONE',  ( -27.10511071441183262, -1.200000000000000030E-05, 8.806984339686158236 ) ) ;
#82838=CARTESIAN_POINT ( 'NONE',  ( 15.76197929006133869, 34.59888885235105960, 23.83685467299613592 ) ) ;
#82873=EDGE_CURVE ( 'NONE', #77549, #98888, #88513, .T. ) ;
#82888=CARTESIAN_POINT ( 'NONE',  ( 48.02835407290544367, 9.771516447483593382, 16.85535821593427386 ) ) ;
#82893=ORIENTED_EDGE ( 'NONE', *, *, #91814, .T. ) ;
#82899=CARTESIAN_POINT ( 'NONE',  ( 22.00881591061976650, 25.77023098277651414, 32.31265490242656568 ) ) ;
#82921=UNCERTAINTY_MEASURE_WITH_UNIT (LENGTH_MEASURE( 1.000000000000000082E-05 ), #8237, 'distance_accuracy_value', 'NONE');
#82941=CARTESIAN_POINT ( 'NONE',  ( 21.97272370781259099, 27.95363515319932191, -32.15429476237004280 ) ) ;
#82943=CARTESIAN_POINT ( 'NONE',  ( -48.02835407290534420, -1.200000000000000030E-05, -16.85535821593460426 ) ) ;
#82949=CARTESIAN_POINT ( 'NONE',  ( -28.43265695612109312, 17.35407036237647560, 40.99228818888992976 ) ) ;
#82958=FACE_OUTER_BOUND ( 'NONE', #90115, .T. ) ;
#82962=DIRECTION ( 'NONE',  ( -0.000000000000000000, 1.000000000000000000, -0.000000000000000000 ) ) ;
#82968=CARTESIAN_POINT ( 'NONE',  ( -26.94600335556788195, 34.81407801978571825, 7.556984339686089847 ) ) ;
#82978=CARTESIAN_POINT ( 'NONE',  ( -47.07197767030570645, 13.48831169381985084, 14.79015211622733084 ) ) ;
#82984=CARTESIAN_POINT ( 'NONE',  ( 16.02938566285138222, 45.83159863292936365, 6.508120059605595920 ) ) ;
#82992=CARTESIAN_POINT ( 'NONE',  ( -29.77121734509604778, 18.16596778899117126, 39.60535821593506967 ) ) ;
#83005=ORIENTED_EDGE ( 'NONE', *, *, #71779, .T. ) ;
#83006=CARTESIAN_POINT ( 'NONE',  ( -17.76478578597574298, 34.19219417800617578, -23.79420372548796436 ) ) ;
#83009=CARTESIAN_POINT ( 'NONE',  ( -6.388374826136157481, 51.65551423085587857, -6.604895695859905658 ) ) ;
#83017=CARTESIAN_POINT ( 'NONE',  ( -28.46830025707812339, 12.99948816575241395, 40.55052036360838486 ) ) ;
#83034=SURFACE_SIDE_STYLE ('',( #66313 ) ) ;
#83035=CARTESIAN_POINT ( 'NONE',  ( 5.974456367264334036E-20, 45.30391365246044444, -18.75000000000000355 ) ) ;
#83040=ORIENTED_EDGE ( 'NONE', *, *, #68691, .F. ) ;
#83043=CARTESIAN_POINT ( 'NONE',  ( 0.08415458823012109124, 37.21016666119768246, 27.24999999999999645 ) ) ;
#83055=B_SPLINE_CURVE_WITH_KNOTS ( 'NONE', 3,
 ( #62405, #54268, #86692, #30047, #55338, #61346, #71009, #45684, #88268, #78562, #70492, #46734, #95300, #94237, #53245, #95828, #14347, #12234, #103902, #45164 ),
 .UNSPECIFIED., .F., .F.,
 ( 4, 2, 2, 2, 2, 2, 2, 2, 2, 4 ),
 ( 0.006350122368084452386, 0.006854238585709724989, 0.007358354803334996724, 0.007610412912147635628, 0.007862471020960272797, 0.008366587238585540195, 0.008870703456210805860, 0.009374819673836073258, 0.009878935891461340657, 0.01038305210908660806 ),
 .UNSPECIFIED. ) ;
#83077=EDGE_LOOP ( 'NONE', ( #19788, #98830, #88493, #99738 ) ) ;
#83083=MECHANICAL_DESIGN_GEOMETRIC_PRESENTATION_REPRESENTATION('',(#24601),#102100);
#83087=VERTEX_POINT ( 'NONE', #39835 ) ;
#83107=ORIENTED_EDGE ( 'NONE', *, *, #31133, .F. ) ;
#83128=MECHANICAL_DESIGN_GEOMETRIC_PRESENTATION_REPRESENTATION('',(#55467),#17700);
#83130=CARTESIAN_POINT ( 'NONE',  ( -10.45288716919457528, 45.35420570811798768, 15.39944944803833415 ) ) ;
#83137=CARTESIAN_POINT ( 'NONE',  ( 16.64348903516523848, -1.200000000000000030E-05, 6.657797401561421857 ) ) ;
#83149=EDGE_LOOP ( 'NONE', ( #9681, #79665, #104267, #44036, #24765, #54600, #46325, #18884 ) ) ;
#83157=CARTESIAN_POINT ( 'NONE',  ( -48.15203510316950286, 9.493368196138860071, -16.85535821593460781 ) ) ;
#83163=CARTESIAN_POINT ( 'NONE',  ( 17.62344211657773485, 45.49768958935467822, 4.615364168318392579 ) ) ;
#83171=CARTESIAN_POINT ( 'NONE',  ( 25.99487131622766611, 37.06902177658768238, -9.387104646514996986 ) ) ;
#83185=SURFACE_STYLE_USAGE ( .BOTH. , #100429 ) ;
#83199=CARTESIAN_POINT ( 'NONE',  ( 0.7840960880508188735, 34.26388638539432918, -29.48703832395431235 ) ) ;
#83223=CARTESIAN_POINT ( 'NONE',  ( 9.956455291700471832, 43.33337594337394449, -15.37426330073998315 ) ) ;
#83229=CARTESIAN_POINT ( 'NONE',  ( -5.290067270632268226, 54.20842449845686417, -6.031152949374520844 ) ) ;
#83236=CARTESIAN_POINT ( 'NONE',  ( -16.32324275503853883, 43.86644259902494980, 4.188645491725135450 ) ) ;
#83243=EDGE_CURVE ( 'NONE', #100740, #8098, #92085, .T. ) ;
#83263=DIRECTION ( 'NONE',  ( 0.000000000000000000, 0.000000000000000000, 1.000000000000000000 ) ) ;
#83297=CARTESIAN_POINT ( 'NONE',  ( -16.18668061311517548, 35.07678708169574122, -21.93884963083486284 ) ) ;
#83309=CARTESIAN_POINT ( 'NONE',  ( 6.488158982472050695, 51.34994349244383471, 7.647142150206464706 ) ) ;
#83321=CARTESIAN_POINT ( 'NONE',  ( -36.81712109022876689, 27.89045283345510740, -13.21917306905795009 ) ) ;
#83325=CARTESIAN_POINT ( 'NONE',  ( -36.32890656491792214, 26.02848181329492405, 12.39893532009519816 ) ) ;
#83351=CARTESIAN_POINT ( 'NONE',  ( 0.5680901257217666478, 45.34938084280606319, -18.61657585049056962 ) ) ;
#83375=CARTESIAN_POINT ( 'NONE',  ( -48.02835407290516656, -1.200000000000000030E-05, 15.60535821593516737 ) ) ;
#83400=UNCERTAINTY_MEASURE_WITH_UNIT (LENGTH_MEASURE( 1.000000000000000082E-05 ), #48821, 'distance_accuracy_value', 'NONE');
#83403=CARTESIAN_POINT ( 'NONE',  ( 8.399370414911262017, 53.73747002930334560, 4.031152949374445349 ) ) ;
#83412=CARTESIAN_POINT ( 'NONE',  ( 47.77500202626908532, 12.17856325595020195, 14.37326074422635003 ) ) ;
#83420=ORIENTED_EDGE ( 'NONE', *, *, #51762, .T. ) ;
#83438=EDGE_LOOP ( 'NONE', ( #16029, #11070, #102389, #19462 ) ) ;
#83439=CARTESIAN_POINT ( 'NONE',  ( 16.64348903516512834, 45.88445698070336931, -4.157797401561768247 ) ) ;
#83456=CARTESIAN_POINT ( 'NONE',  ( 16.83431405849833951, 36.36677671467317907, -24.30698433968626304 ) ) ;
#83462=CARTESIAN_POINT ( 'NONE',  ( 16.42263527633062026, 34.33311419812763177, -24.27358441403828948 ) ) ;
#83469=ADVANCED_FACE ( 'NONE', ( #61338 ), #10628, .F. ) ;
#83490=ORIENTED_EDGE ( 'NONE', *, *, #73557, .T. ) ;
#83491=CARTESIAN_POINT ( 'NONE',  ( -26.01822098816688467, 35.07276571059547621, 8.183900759913079526 ) ) ;
#83547=EDGE_LOOP ( 'NONE', ( #97570, #9322 ) ) ;
#83568=CARTESIAN_POINT ( 'NONE',  ( 16.64348903516512834, 43.75610143575153899, -4.157797401561768247 ) ) ;
#83571=CARTESIAN_POINT ( 'NONE',  ( -37.88465841952032065, 27.77130359203633958, 10.98700391011192679 ) ) ;
#83592=CARTESIAN_POINT ( 'NONE',  ( -37.56673239365849781, -1.200000000000000030E-05, 12.20617127781066102 ) ) ;
#83608=CARTESIAN_POINT ( 'NONE',  ( -4.277917525292022738, 52.15487555894509342, 6.542882894562609408 ) ) ;
#83621=ORIENTED_EDGE ( 'NONE', *, *, #102523, .T. ) ;
#83634=CARTESIAN_POINT ( 'NONE',  ( -1.250712992818178160, 53.76598346644076543, 9.153008886931235821 ) ) ;
#83656=CYLINDRICAL_SURFACE ( 'NONE', #78840, 1.250000000000001110 ) ;
#83658=AXIS2_PLACEMENT_3D ( 'NONE', #22044, #47871, #29621 ) ;
#83664=FILL_AREA_STYLE_COLOUR ( '', #16217 ) ;
#83676=AXIS2_PLACEMENT_3D ( 'NONE', #48644, #72408, #81016 ) ;
#83680=STYLED_ITEM ( 'NONE', ( #96398 ), #36367 ) ;
#83685=ADVANCED_FACE ( 'NONE', ( #1870 ), #16478, .F. ) ;
#83692=CARTESIAN_POINT ( 'NONE',  ( 26.01879166445673874, 37.20103050938880784, -8.182916409703022254 ) ) ;
#83694=CYLINDRICAL_SURFACE ( 'NONE', #75924, 1.250000000000000000 ) ;
#83703=CYLINDRICAL_SURFACE ( 'NONE', #71255, 1.250000000000000222 ) ;
#83711=CARTESIAN_POINT ( 'NONE',  ( 11.04468709431039564, 45.87751353276773614, 13.15154111190456021 ) ) ;
#83735=CONICAL_SURFACE ( 'NONE', #28921, 2747.477419454587107, 1.221730476396026610 ) ;
#83737=SURFACE_SIDE_STYLE ('',( #91847 ) ) ;
#83740=( GEOMETRIC_REPRESENTATION_CONTEXT ( 3 ) GLOBAL_UNCERTAINTY_ASSIGNED_CONTEXT ( ( #4891 ) ) GLOBAL_UNIT_ASSIGNED_CONTEXT ( ( #30005, #69913, #95258 ) ) REPRESENTATION_CONTEXT ( 'NONE', 'WORKASPACE' ) );
#83741=CARTESIAN_POINT ( 'NONE',  ( 37.56673239365870387, 25.75719283951018923, 10.95617127780998956 ) ) ;
#83750=ORIENTED_EDGE ( 'NONE', *, *, #92257, .F. ) ;
#83763=CARTESIAN_POINT ( 'NONE',  ( -22.13642162920451639, 27.78492472323463502, 32.60352800065667367 ) ) ;
#83774=B_SPLINE_CURVE_WITH_KNOTS ( 'NONE', 3,
 ( #13892, #87816, #79704, #21505, #54341, #61025, #2759, #101991, #36249, #11371, #18999, #28149, #46810, #38735, #22028, #6329, #104508, #31197, #13362, #96440 ),
 .UNSPECIFIED., .F., .F.,
 ( 4, 2, 2, 2, 2, 2, 2, 2, 2, 4 ),
 ( 0.007065883224795808069, 0.007569382595898239974, 0.008072881967000671011, 0.008576381338103105517, 0.008828131023654322770, 0.009079880709205540024, 0.009583380080307965856, 0.01008687945141039342, 0.01059037882251281926, 0.01109387819361524682 ),
 .UNSPECIFIED. ) ;
#83783=CARTESIAN_POINT ( 'NONE',  ( -48.80564935039983965, 14.82671221253059279, 14.61894534951832192 ) ) ;
#83807=CARTESIAN_POINT ( 'NONE',  ( 10.28624191511840458, 43.25714326066859172, 15.40779740156149202 ) ) ;
#83809=CARTESIAN_POINT ( 'NONE',  ( 0.8444424525834832718, 13.67360963902750903, -51.42495577429150444 ) ) ;
#83824=CARTESIAN_POINT ( 'NONE',  ( -16.42642030348412518, 34.33441478758428644, -24.26661104398729663 ) ) ;
#83835=CARTESIAN_POINT ( 'NONE',  ( 9.182800793770848458, 51.37232910640911854, -3.876820685372471154 ) ) ;
#83864=DIRECTION ( 'NONE',  ( 0.000000000000000000, 1.000000000000000000, -0.000000000000000000 ) ) ;
#83869=CARTESIAN_POINT ( 'NONE',  ( 0.9981243769357334150, 8.900829104547275605, 51.25576959928475418 ) ) ;
#83873=CARTESIAN_POINT ( 'NONE',  ( 37.72778265019833555, 25.42095348269468857, -13.45617127781092215 ) ) ;
#83876=CARTESIAN_POINT ( 'NONE',  ( -8.719197186943313582, 53.90628269159294206, 1.531152949374563699 ) ) ;
#83883=CONICAL_SURFACE ( 'NONE', #82109, 22.55262289886175964, 1.221730476396026388 ) ;
#83885=VERTEX_POINT ( 'NONE', #103769 ) ;
#83886=CARTESIAN_POINT ( 'NONE',  ( 30.74966693359977299, 13.13370859069518204, 41.50962874632922706 ) ) ;
#83895=CARTESIAN_POINT ( 'NONE',  ( 0.5680194430980197717, 28.15644683432188700, 38.38337714611267870 ) ) ;
#83919=CARTESIAN_POINT ( 'NONE',  ( 16.64348903516512834, -1.200000000000000030E-05, -5.407797401561770023 ) ) ;
#83944=CARTESIAN_POINT ( 'NONE',  ( -15.90885615318869029, 37.20836610827222302, -22.13023378396306384 ) ) ;
#83947=CARTESIAN_POINT ( 'NONE',  ( 47.29503607946699617, 13.12332669628137438, 14.58854632476099766 ) ) ;
#83951=EDGE_CURVE ( 'NONE', #23889, #1638, #8052, .T. ) ;
#83958=( GEOMETRIC_REPRESENTATION_CONTEXT ( 3 ) GLOBAL_UNCERTAINTY_ASSIGNED_CONTEXT ( ( #100913 ) ) GLOBAL_UNIT_ASSIGNED_CONTEXT ( ( #40443, #15101, #105186 ) ) REPRESENTATION_CONTEXT ( 'NONE', 'WORKASPACE' ) );
#83959=CARTESIAN_POINT ( 'NONE',  ( -46.97231841192009227, 12.59348177918413825, -16.28806988207291440 ) ) ;
#83982=CARTESIAN_POINT ( 'NONE',  ( 8.013529827547630546, 54.15025421630311087, -1.653736085047024851 ) ) ;
#83983=UNCERTAINTY_MEASURE_WITH_UNIT (LENGTH_MEASURE( 1.000000000000000082E-05 ), #9844, 'distance_accuracy_value', 'NONE');
#83995=B_SPLINE_CURVE_WITH_KNOTS ( 'NONE', 3,
 ( #47640, #61746, #103245, #71932, #45552, #104837, #39586, #102711, #28875, #29390, #13146, #62275, #94644, #20788, #53622, #95162, #86557, #12615, #21295, #54131 ),
 .UNSPECIFIED., .F., .F.,
 ( 4, 2, 2, 2, 2, 2, 2, 2, 2, 4 ),
 ( 0.006339153383469499359, 0.006843475872017545751, 0.007347798360565592143, 0.007599959604839613171, 0.007852120849113634199, 0.008356443337661681459, 0.008860765826209728718, 0.009365088314757775978, 0.009869410803305823238, 0.01037373329185387050 ),
 .UNSPECIFIED. ) ;
#84001=CARTESIAN_POINT ( 'NONE',  ( 16.11237705540419185, 35.08085309292203391, -21.97963608747229358 ) ) ;
#84010=CIRCLE ( 'NONE', #59941, 11.27631144943088337 ) ;
#84015=CARTESIAN_POINT ( 'NONE',  ( -22.45489971457653766, 25.48429075023468471, 32.95935593634655447 ) ) ;
#84019=EDGE_CURVE ( 'NONE', #45240, #89868, #6725, .T. ) ;
#84027=CYLINDRICAL_SURFACE ( 'NONE', #69180, 1.250000000000001110 ) ;
#84033=CIRCLE ( 'NONE', #73705, 55.00000000000000000 ) ;
#84038=CARTESIAN_POINT ( 'NONE',  ( -7.577625347064596895, 54.07946387534607879, -3.571027979463019975 ) ) ;
#84040=COLOUR_RGB ( '', 0.31764706, 0.68627451, 0.89019608) ;
#84049=CARTESIAN_POINT ( 'NONE',  ( 9.806233215530133052, 53.43715092910265696, 2.591038554327974364 ) ) ;
#84055=CARTESIAN_POINT ( 'NONE',  ( -30.10126468112073184, 13.03072330106369492, 42.03538192853101663 ) ) ;
#84062=CARTESIAN_POINT ( 'NONE',  ( 29.68315524077034695, -1.200000000000000030E-05, 40.85535821593451544 ) ) ;
#84067=VECTOR ( 'NONE', #31095, 1000.000000000000000 ) ;
#84082=VERTEX_POINT ( 'NONE', #69965 ) ;
#84086=CARTESIAN_POINT ( 'NONE',  ( 48.02835407290545078, 16.78162100668605206, 14.35535821593427386 ) ) ;
#84101=CARTESIAN_POINT ( 'NONE',  ( -23.38332460214670050, 25.95229859289731422, -30.70617127781034483 ) ) ;
#84106=CARTESIAN_POINT ( 'NONE',  ( 5.974456367264334036E-20, 45.30391365246044444, -18.75000000000000355 ) ) ;
#84108=ORIENTED_EDGE ( 'NONE', *, *, #17746, .F. ) ;
#84156=CARTESIAN_POINT ( 'NONE',  ( 27.42283046010333436, 36.77223446253648120, 7.587737780918474506 ) ) ;
#84157=CARTESIAN_POINT ( 'NONE',  ( -4.205845516828716768, 51.73505483899108981, 7.923285039163679322 ) ) ;
#84165=DIRECTION ( 'NONE',  ( 1.150791560227848544E-16, -0.3420201433256727652, 0.9396926207859068736 ) ) ;
#84172=DIRECTION ( 'NONE',  ( 4.738110706560371839E-17, -0.9221233147934838614, 0.3868961001538753219 ) ) ;
#84187=CARTESIAN_POINT ( 'NONE',  ( -0.1698863216407462684, 53.40045558394650982, 10.24124536584039902 ) ) ;
#84189=DIRECTION ( 'NONE',  ( 0.000000000000000000, 0.000000000000000000, 1.000000000000000000 ) ) ;
#84195=ORIENTED_EDGE ( 'NONE', *, *, #77802, .F. ) ;
#84203=CARTESIAN_POINT ( 'NONE',  ( 37.56673239365841255, 25.47613764497371136, -13.45617127781092215 ) ) ;
#84205=CARTESIAN_POINT ( 'NONE',  ( -0.3375803178940949278, 36.31236650232811769, -29.71517349513863948 ) ) ;
#84220=CARTESIAN_POINT ( 'NONE',  ( -0.6419814643516539299, 45.36335988269765807, 18.57571296656996296 ) ) ;
#84230=LINE ( 'NONE', #59979, #72151 ) ;
#84239=CARTESIAN_POINT ( 'NONE',  ( 0.000000000000000000, 0.000000000000000000, 0.000000000000000000 ) ) ;
#84253=DIRECTION ( 'NONE',  ( 0.000000000000000000, 0.000000000000000000, 1.000000000000000000 ) ) ;
#84254=ORIENTED_EDGE ( 'NONE', *, *, #106341, .F. ) ;
#84256=CARTESIAN_POINT ( 'NONE',  ( -0.7711376685623203553, 18.23545326243540643, -49.51189540388887877 ) ) ;
#84257=CARTESIAN_POINT ( 'NONE',  ( 37.56673239365841255, 27.88554838446202311, -10.95617127781092037 ) ) ;
#84272=CARTESIAN_POINT ( 'NONE',  ( 8.012708964559053015, 52.02215964811360038, 1.654162217208905883 ) ) ;
#84274=LINE ( 'NONE', #10369, #61506 ) ;
#84276=CARTESIAN_POINT ( 'NONE',  ( 1.098491644507098242, 43.84235381817760668, 16.88236719228266125 ) ) ;
#84283=CARTESIAN_POINT ( 'NONE',  ( 0.000000000000000000, 29.56666008184760130, 0.000000000000000000 ) ) ;
#84288=( LENGTH_UNIT ( ) NAMED_UNIT ( * ) SI_UNIT ( .MILLI., .METRE. ) );
#84294=COLOUR_RGB ( '', 0.66274510, 0.83137255, 0.94901961) ;
#84307=CIRCLE ( 'NONE', #37856, 33.82893434829263413 ) ;
#84308=CARTESIAN_POINT ( 'NONE',  ( -15.42152358372385557, 44.08893209364050136, 5.095058633600949349 ) ) ;
#84311=CARTESIAN_POINT ( 'NONE',  ( -22.19860641359375819, 28.18788469371687455, 31.21259335822219683 ) ) ;
#84313=VECTOR ( 'NONE', #61068, 1000.000000000000000 ) ;
#84322=CARTESIAN_POINT ( 'NONE',  ( 7.799693306582752506, 52.08906168172599394, -1.774544900689356774 ) ) ;
#84325=CARTESIAN_POINT ( 'NONE',  ( -1.219019397738882127, 27.86094505705872137, -39.18046835220320645 ) ) ;
#84344=SURFACE_SIDE_STYLE ('',( #18568 ) ) ;
#84350=CARTESIAN_POINT ( 'NONE',  ( -22.45608800630787627, 25.48376296471925073, -32.96030118683280108 ) ) ;
#84352=CARTESIAN_POINT ( 'NONE',  ( -27.02532652597945884, 34.78626739604272444, -7.556984339685866026 ) ) ;
#84362=FILL_AREA_STYLE ('',( #51973 ) ) ;
#84373=CARTESIAN_POINT ( 'NONE',  ( -16.42070475374124783, 35.05495340490914913, -21.83980561103319218 ) ) ;
#84379=CARTESIAN_POINT ( 'NONE',  ( -16.91669820832276727, 34.22140543898331799, 24.30698433968612804 ) ) ;
#84384=CARTESIAN_POINT ( 'NONE',  ( 49.26574068698166542, 8.068653426789120786, -15.39376958037598619 ) ) ;
#84413=CARTESIAN_POINT ( 'NONE',  ( 0.9524862760789143401, 8.765895626014080122, 51.31327605337367714 ) ) ;
#84435=CARTESIAN_POINT ( 'NONE',  ( 29.85995211472236832, 18.03913124950667424, 39.60535821593451544 ) ) ;
#84437=ADVANCED_FACE ( 'NONE', ( #37777, #70104, #103011, #45312, #36191 ), #40267, .F. ) ;
#84440=CARTESIAN_POINT ( 'NONE',  ( -7.943938681556293346, 53.91044595262783901, 3.880671334416982976 ) ) ;
#84442=CARTESIAN_POINT ( 'NONE',  ( 1.220173976448186481, 27.62999424518777047, 39.81527922047737889 ) ) ;
#84443=CARTESIAN_POINT ( 'NONE',  ( -30.29801405241517998, 7.759806510565432802, -41.94638970127596878 ) ) ;
#84455=APPLICATION_CONTEXT ( 'automotive_design' ) ;
#84459=ORIENTED_EDGE ( 'NONE', *, *, #5205, .F. ) ;
#84479=UNCERTAINTY_MEASURE_WITH_UNIT (LENGTH_MEASURE( 1.000000000000000082E-05 ), #77512, 'distance_accuracy_value', 'NONE');
#84481=DIRECTION ( 'NONE',  ( -0.000000000000000000, 1.000000000000000000, -0.000000000000000000 ) ) ;
#84482=CARTESIAN_POINT ( 'NONE',  ( 7.482955433003800394, 54.13148333495901454, 3.437080708373401183 ) ) ;
#84488=CARTESIAN_POINT ( 'NONE',  ( -16.42383576958760472, 37.18011179812618394, -21.84794872343122307 ) ) ;
#84502=CARTESIAN_POINT ( 'NONE',  ( -47.44481056709870614, 11.19259812317955927, -16.71748578406464958 ) ) ;
#84512=B_SPLINE_CURVE_WITH_KNOTS ( 'NONE', 3,
 ( #103619, #39952, #72824, #105215, #97630, #56095, #63173, #105729, #5459, #55570, #31361, #14584, #70725, #79339, #89031, #47493, #23794, #45924 ),
 .UNSPECIFIED., .F., .F.,
 ( 4, 2, 2, 2, 2, 2, 2, 2, 4 ),
 ( 0.007150400357696743217, 0.007655146576508041652, 0.008159892795319340086, 0.008664639014130639388, 0.009169385232941936956, 0.009674131451753234523, 0.01017887767056453382, 0.01068362388937583313, 0.01118837010818713069 ),
 .UNSPECIFIED. ) ;
#84521=VERTEX_POINT ( 'NONE', #102476 ) ;
#84522=CARTESIAN_POINT ( 'NONE',  ( 28.71516359314587064, 10.50242333429324582, -41.65501769021862799 ) ) ;
#84528=( LENGTH_UNIT ( ) NAMED_UNIT ( * ) SI_UNIT ( .MILLI., .METRE. ) );
#84533=( GEOMETRIC_REPRESENTATION_CONTEXT ( 3 ) GLOBAL_UNCERTAINTY_ASSIGNED_CONTEXT ( ( #88461 ) ) GLOBAL_UNIT_ASSIGNED_CONTEXT ( ( #31891, #64259, #104160 ) ) REPRESENTATION_CONTEXT ( 'NONE', 'WORKASPACE' ) );
#84537=CARTESIAN_POINT ( 'NONE',  ( -37.56673239365849781, 27.60449318992554169, 13.45617127781067168 ) ) ;
#84577=AXIS2_PLACEMENT_3D ( 'NONE', #47939, #87902, #46890 ) ;
#84590=CARTESIAN_POINT ( 'NONE',  ( 15.39075092899655317, 46.20845424323130146, 5.262406961020114515 ) ) ;
#84593=FILL_AREA_STYLE ('',( #42522 ) ) ;
#84616=CARTESIAN_POINT ( 'NONE',  ( -10.61258144643682577, 43.90877112545464911, -12.94048881062180811 ) ) ;
#84617=ADVANCED_FACE ( 'NONE', ( #45836 ), #94934, .F. ) ;
#84640=ORIENTED_EDGE ( 'NONE', *, *, #97910, .F. ) ;
#84658=CARTESIAN_POINT ( 'NONE',  ( -16.48303619537882625, 45.94111582078982536, 4.157797401561652784 ) ) ;
#84676=DIRECTION ( 'NONE',  ( 0.000000000000000000, 1.000000000000000000, -0.000000000000000000 ) ) ;
#84693=DIRECTION ( 'NONE',  ( 0.000000000000000000, 0.000000000000000000, 1.000000000000000000 ) ) ;
#84702=CYLINDRICAL_SURFACE ( 'NONE', #66071, 1.249999999999999778 ) ;
#84703=( GEOMETRIC_REPRESENTATION_CONTEXT ( 3 ) GLOBAL_UNCERTAINTY_ASSIGNED_CONTEXT ( ( #68297 ) ) GLOBAL_UNIT_ASSIGNED_CONTEXT ( ( #102024, #28185, #53991 ) ) REPRESENTATION_CONTEXT ( 'NONE', 'WORKASPACE' ) );
#84709=EDGE_LOOP ( 'NONE', ( #52198, #35592, #24236, #49319 ) ) ;
#84712=CARTESIAN_POINT ( 'NONE',  ( -23.21751746555244722, 25.25267828308493634, 33.20617127781060418 ) ) ;
#84724=SURFACE_SIDE_STYLE ('',( #59943 ) ) ;
#84729=EDGE_CURVE ( 'NONE', #92720, #10253, #86416, .T. ) ;
#84734=CARTESIAN_POINT ( 'NONE',  ( 36.39102669964498915, 25.97871626027877667, -12.63845754337161864 ) ) ;
#84742=DIRECTION ( 'NONE',  ( -0.000000000000000000, 1.000000000000000000, 0.000000000000000000 ) ) ;
#84743=UNCERTAINTY_MEASURE_WITH_UNIT (LENGTH_MEASURE( 1.000000000000000082E-05 ), #47502, 'distance_accuracy_value', 'NONE');
#84755=DIRECTION ( 'NONE',  ( 0.000000000000000000, 0.000000000000000000, 1.000000000000000000 ) ) ;
#84769=CYLINDRICAL_SURFACE ( 'NONE', #91749, 11.27631144943088515 ) ;
#84770=ORIENTED_EDGE ( 'NONE', *, *, #36687, .F. ) ;
#84774=( NAMED_UNIT ( * ) SI_UNIT ( $, .STERADIAN. ) SOLID_ANGLE_UNIT ( ) );
#84779=UNCERTAINTY_MEASURE_WITH_UNIT (LENGTH_MEASURE( 1.000000000000000082E-05 ), #24041, 'distance_accuracy_value', 'NONE');
#84790=SURFACE_STYLE_FILL_AREA ( #27661 ) ;
#84795=CARTESIAN_POINT ( 'NONE',  ( 16.64348903516524203, 43.75610143575153188, 4.157797401561407646 ) ) ;
#84822=CARTESIAN_POINT ( 'NONE',  ( -1.160479916384425936, 11.83769311796837975, -50.01979920269963742 ) ) ;
#84824=DIRECTION ( 'NONE',  ( -0.000000000000000000, 1.000000000000000000, 0.000000000000000000 ) ) ;
#84838=CARTESIAN_POINT ( 'NONE',  ( -15.89310649718362534, 43.76126840433826004, 6.420194468478833905 ) ) ;
#84862=LINE ( 'NONE', #100502, #20974 ) ;
#84865=AXIS2_PLACEMENT_3D ( 'NONE', #52176, #102330, #19871 ) ;
#84894=CARTESIAN_POINT ( 'NONE',  ( -46.79057916015437257, 18.53868985150237236, -15.81409158839457518 ) ) ;
#84899=ORIENTED_EDGE ( 'NONE', *, *, #42627, .T. ) ;
#84914=CARTESIAN_POINT ( 'NONE',  ( 49.27910061723706292, 7.914421806211205279, -15.56686240200417259 ) ) ;
#84926=B_SPLINE_CURVE_WITH_KNOTS ( 'NONE', 3,
 ( #83229, #27700, #44375, #76723, #68107, #101005, #20144, #52445, #85363, #3383, #27163, #2834, #11452, #67062, #60055, #28225, #75663, #10391 ),
 .UNSPECIFIED., .F., .F.,
 ( 4, 2, 2, 2, 2, 2, 2, 2, 4 ),
 ( 0.002862744142489912630, 0.003367451191158993620, 0.003619804715493535850, 0.003872158239828078080, 0.004376865288497162540, 0.004881572337166247000, 0.005890986434504425460, 0.006395693483173519461, 0.006900400531842612595 ),
 .UNSPECIFIED. ) ;
#84935=CARTESIAN_POINT ( 'NONE',  ( 0.000000000000000000, 34.08768991669519721, 0.000000000000000000 ) ) ;
#84944=EDGE_CURVE ( 'NONE', #66879, #73917, #37120, .T. ) ;
#84961=CARTESIAN_POINT ( 'NONE',  ( 30.25727950662361820, 17.21737621059157064, 39.73669541984489229 ) ) ;
#84963=FILL_AREA_STYLE_COLOUR ( '', #106571 ) ;
#84972=CARTESIAN_POINT ( 'NONE',  ( -30.90685644053160885, 9.526079354490862627, -40.57200395206852050 ) ) ;
#84978=CARTESIAN_POINT ( 'NONE',  ( 9.627423004282553265, 53.53986113459780682, -2.126428460392088216 ) ) ;
#84989=CARTESIAN_POINT ( 'NONE',  ( 4.957729184102722009, 53.54793516222699878, -8.497043709396882250 ) ) ;
#84998=DIRECTION ( 'NONE',  ( -0.000000000000000000, 1.000000000000000000, -0.000000000000000000 ) ) ;
#85006=UNCERTAINTY_MEASURE_WITH_UNIT (LENGTH_MEASURE( 1.000000000000000082E-05 ), #82207, 'distance_accuracy_value', 'NONE');
#85015=CARTESIAN_POINT ( 'NONE',  ( -15.99452815637125447, 36.61440916976220450, -24.05462502184712648 ) ) ;
#85032=CARTESIAN_POINT ( 'NONE',  ( 1.530808498934191324E-16, -1.200000000000000030E-05, 7.749999999999999112 ) ) ;
#85038=ORIENTED_EDGE ( 'NONE', *, *, #29149, .T. ) ;
#85047=AXIS2_PLACEMENT_3D ( 'NONE', #7562, #73357, #24332 ) ;
#85050=CARTESIAN_POINT ( 'NONE',  ( 29.50913623581959300, 8.560131685753185948, -42.09559527950068514 ) ) ;
#85053=( GEOMETRIC_REPRESENTATION_CONTEXT ( 3 ) GLOBAL_UNCERTAINTY_ASSIGNED_CONTEXT ( ( #84779 ) ) GLOBAL_UNIT_ASSIGNED_CONTEXT ( ( #24041, #56882, #24569 ) ) REPRESENTATION_CONTEXT ( 'NONE', 'WORKASPACE' ) );
#85066=CARTESIAN_POINT ( 'NONE',  ( 16.75187969033441604, 36.38380281757147827, -24.30698433969211791 ) ) ;
#85068=EDGE_LOOP ( 'NONE', ( #74250, #4056 ) ) ;
#85074=AXIS2_PLACEMENT_3D ( 'NONE', #4339, #40284, #73160 ) ;
#85075=CARTESIAN_POINT ( 'NONE',  ( -29.68315524076956535, 13.47185074185901499, 42.10535821593508388 ) ) ;
#85078=CARTESIAN_POINT ( 'NONE',  ( 0.000000000000000000, 29.56666008184760130, 0.000000000000000000 ) ) ;
#85099=VERTEX_POINT ( 'NONE', #16517 ) ;
#85118=( GEOMETRIC_REPRESENTATION_CONTEXT ( 3 ) GLOBAL_UNCERTAINTY_ASSIGNED_CONTEXT ( ( #10308 ) ) GLOBAL_UNIT_ASSIGNED_CONTEXT ( ( #12986, #103608, #63162 ) ) REPRESENTATION_CONTEXT ( 'NONE', 'WORKASPACE' ) );
#85136=CARTESIAN_POINT ( 'NONE',  ( 49.28001195564470294, 13.04047724765487537, 15.62422648183673957 ) ) ;
#85142=CARTESIAN_POINT ( 'NONE',  ( -1.011281213726471728, 37.02243808088083199, 27.74757158266077539 ) ) ;
#85152=ADVANCED_FACE ( 'NONE', ( #99009 ), #58587, .F. ) ;
#85159=CARTESIAN_POINT ( 'NONE',  ( -1.013051998863770953, 45.47574100367069150, -18.25019877145031799 ) ) ;
#85163=CARTESIAN_POINT ( 'NONE',  ( -23.62769831312177971, 25.18629417231644396, -33.13992749466611798 ) ) ;
#85171=CARTESIAN_POINT ( 'NONE',  ( 15.49776003472984343, 37.05489105806098138, -22.93080861416551031 ) ) ;
#85214=AXIS2_PLACEMENT_3D ( 'NONE', #31982, #30396, #64857 ) ;
#85241=( NAMED_UNIT ( * ) PLANE_ANGLE_UNIT ( ) SI_UNIT ( $, .RADIAN. ) );
#85246=CARTESIAN_POINT ( 'NONE',  ( 27.10511071441197117, -1.200000000000000030E-05, 10.05698433968570704 ) ) ;
#85250=DIRECTION ( 'NONE',  ( 0.000000000000000000, 0.000000000000000000, 1.000000000000000000 ) ) ;
#85259=CARTESIAN_POINT ( 'NONE',  ( -6.308794298586568594, 51.28513677629712220, 8.024939188852076910 ) ) ;
#85266=CARTESIAN_POINT ( 'NONE',  ( -1.012588390450172460, 36.47564902558247013, -29.25078143156558141 ) ) ;
#85267=DIRECTION ( 'NONE',  ( 0.000000000000000000, -0.3420201433256725987, -0.9396926207859068736 ) ) ;
#85292=B_SPLINE_CURVE_WITH_KNOTS ( 'NONE', 3,
 ( #84203, #51819, #61007, #51282, #93891, #43213, #85819, #84734, #18428, #10817, #11896, #35692, #44823, #77709, #34093, #1668, #34625, #66966, #67496, #59410, #92274, #78746, #4344, #4880 ),
 .UNSPECIFIED., .F., .F.,
 ( 4, 2, 2, 2, 2, 2, 2, 2, 2, 2, 2, 4 ),
 ( 0.007801886282271855259, 0.008306033261743405588, 0.008810180241214956784, 0.009314327220686507980, 0.009566400710422282710, 0.009818474200158055706, 0.01007054768989382870, 0.01032262117962960343, 0.01057469466936537643, 0.01082676815910114942, 0.01133091513857269715, 0.01183506211804424488 ),
 .UNSPECIFIED. ) ;
#85322=CARTESIAN_POINT ( 'NONE',  ( -47.90320435033602564, 17.06740859345675787, 14.35535821593516559 ) ) ;
#85323=CARTESIAN_POINT ( 'NONE',  ( 37.72605696939957909, 27.54990033529972138, -13.45617127781096123 ) ) ;
#85326=CARTESIAN_POINT ( 'NONE',  ( 0.7723747150160921171, 18.23314980831915122, 49.51284287117157135 ) ) ;
#85327=DIRECTION ( 'NONE',  ( 0.000000000000000000, 0.000000000000000000, 1.000000000000000000 ) ) ;
#85348=CARTESIAN_POINT ( 'NONE',  ( -8.235963203755042983, 51.66292127458935823, -4.031152949374507521 ) ) ;
#85362=VECTOR ( 'NONE', #36951, 1000.000000000000000 ) ;
#85363=CARTESIAN_POINT ( 'NONE',  ( -4.181427851358347603, 54.26024483359611139, -6.680433775739387237 ) ) ;
#85365=CARTESIAN_POINT ( 'NONE',  ( -9.508921847869125088, 46.21454289499524037, -13.17524946764681282 ) ) ;
#85383=ORIENTED_EDGE ( 'NONE', *, *, #90298, .F. ) ;
#85392=CARTESIAN_POINT ( 'NONE',  ( -1.099210409027892466, 27.97021247871829175, -38.88368413723794959 ) ) ;
#85395=CARTESIAN_POINT ( 'NONE',  ( 46.77666182531591943, 18.74137236369644910, -15.58806238568051228 ) ) ;
#85399=CARTESIAN_POINT ( 'NONE',  ( -48.02835407290516656, 16.78162100668608048, 14.35535821593516559 ) ) ;
#85415=CARTESIAN_POINT ( 'NONE',  ( -26.94599015477662363, 34.53165509030868918, -10.05698433968608896 ) ) ;
#85424=( LENGTH_UNIT ( ) NAMED_UNIT ( * ) SI_UNIT ( .MILLI., .METRE. ) );
#85448=( LENGTH_UNIT ( ) NAMED_UNIT ( * ) SI_UNIT ( .MILLI., .METRE. ) );
#85449=CARTESIAN_POINT ( 'NONE',  ( -2.324561895696642773E-13, 53.39766064372246746, 10.25000000000230038 ) ) ;
#85471=CARTESIAN_POINT ( 'NONE',  ( -37.24861026655265306, 25.58887987570736655, 13.42549399110521335 ) ) ;
#85480=LINE ( 'NONE', #13152, #85362 ) ;
#85489=CARTESIAN_POINT ( 'NONE',  ( -26.78474277083682864, 36.99592048761888208, -7.587964203663859486 ) ) ;
#85500=ORIENTED_EDGE ( 'NONE', *, *, #65697, .F. ) ;
#85577=CARTESIAN_POINT ( 'NONE',  ( -47.07447497471051889, 13.47837589781632417, -14.79567547011589923 ) ) ;
#85581=CARTESIAN_POINT ( 'NONE',  ( -16.64348903516521005, 43.47556584774768140, -6.657797401561535544 ) ) ;
#85597=CARTESIAN_POINT ( 'NONE',  ( -8.559508646656389885, -1.200000000000000030E-05, -4.031152949374503081 ) ) ;
#85638=CARTESIAN_POINT ( 'NONE',  ( -0.6447843993400577123, 28.14413779556368667, 38.41621468030491826 ) ) ;
#85656=ORIENTED_EDGE ( 'NONE', *, *, #102003, .T. ) ;
#85676=EDGE_LOOP ( 'NONE', ( #16650, #25409, #60274, #33387, #54700, #60921, #58067, #72185 ) ) ;
#85715=CARTESIAN_POINT ( 'NONE',  ( -24.35720706066873475, 25.22454029369766104, -32.47622240156568552 ) ) ;
#85738=AXIS2_PLACEMENT_3D ( 'NONE', #20983, #53816, #12819 ) ;
#85763=ORIENTED_EDGE ( 'NONE', *, *, #19278, .T. ) ;
#85798=VERTEX_POINT ( 'NONE', #10130 ) ;
#85806=CARTESIAN_POINT ( 'NONE',  ( -17.95946947111402991, 36.59397683629514830, -22.69701383365361380 ) ) ;
#85815=VECTOR ( 'NONE', #46289, 1000.000000000000000 ) ;
#85819=CARTESIAN_POINT ( 'NONE',  ( 36.49026554367495834, 25.91778114966158242, -12.86217455386831432 ) ) ;
#85867=CARTESIAN_POINT ( 'NONE',  ( 30.75723595955470557, 13.12755156482208108, -41.50738620754143682 ) ) ;
#85880=CARTESIAN_POINT ( 'NONE',  ( 17.86498552253326366, 43.17254421777826678, 5.722207910555678900 ) ) ;
#85902=CARTESIAN_POINT ( 'NONE',  ( -8.559508646656389885, 51.55638410492942825, -4.031152949374503081 ) ) ;
#85904=VERTEX_POINT ( 'NONE', #84712 ) ;
#85906=CARTESIAN_POINT ( 'NONE',  ( -27.42256603292173267, 34.64699562455260207, 7.556984339685873131 ) ) ;
#85908=CARTESIAN_POINT ( 'NONE',  ( -16.91704105317864659, 37.08060170114688248, 21.81528127871682798 ) ) ;
#85909=UNCERTAINTY_MEASURE_WITH_UNIT (LENGTH_MEASURE( 1.000000000000000082E-05 ), #28104, 'distance_accuracy_value', 'NONE');
#85912=CARTESIAN_POINT ( 'NONE',  ( 6.310175713569941003, 53.41366202879699188, -8.023280885595736933 ) ) ;
#85920=CARTESIAN_POINT ( 'NONE',  ( -10.20373343965778545, 45.40217293244035091, -15.40779740156157374 ) ) ;
#85947=LINE ( 'NONE', #77834, #40675 ) ;
#85948=CARTESIAN_POINT ( 'NONE',  ( 47.14503195514078016, 18.54431490493022494, -14.71570748879639190 ) ) ;
#85952=CARTESIAN_POINT ( 'NONE',  ( -49.03498469565148099, 14.13689777146986870, 14.86104782056252205 ) ) ;
#85965=CARTESIAN_POINT ( 'NONE',  ( -22.11381839868240107, 25.65490958513800734, -32.62441910024401892 ) ) ;
#85967=EDGE_CURVE ( 'NONE', #36049, #32988, #28109, .T. ) ;
#85969=B_SPLINE_CURVE_WITH_KNOTS ( 'NONE', 3,
 ( #3207, #50655, #83571, #9679, #30696, #95942, #29129, #78148, #62000, #38771, #62516, #63583, #4268, #22612, #95399, #37196, #46321, #6370, #54373, #86271 ),
 .UNSPECIFIED., .F., .F.,
 ( 4, 2, 2, 2, 2, 2, 2, 2, 2, 4 ),
 ( 0.007055264176649387285, 0.007558908847143414045, 0.008062553517637439937, 0.008566198188131465829, 0.008818020523378480510, 0.009069842858625493456, 0.009573487529119514144, 0.01007713219961353657, 0.01058077687010755726, 0.01108442154060157794 ),
 .UNSPECIFIED. ) ;
#85989=CARTESIAN_POINT ( 'NONE',  ( 0.000000000000000000, 23.58303312036771615, -45.10524579772351217 ) ) ;
#85995=EDGE_LOOP ( 'NONE', ( #6219, #24019, #36172, #93570 ) ) ;
#85999=CARTESIAN_POINT ( 'NONE',  ( 49.27997219161959919, 7.868281554635434105, -15.62830927991629792 ) ) ;
#86016=CARTESIAN_POINT ( 'NONE',  ( 49.15269216906074234, 13.73471152902317272, -15.05374764292056078 ) ) ;
#86026=ORIENTED_EDGE ( 'NONE', *, *, #61711, .T. ) ;
#86029=CARTESIAN_POINT ( 'NONE',  ( 0.1550192221702281492, 7.763576898078555111, 51.74244561565719636 ) ) ;
#86039=CARTESIAN_POINT ( 'NONE',  ( 29.68315524077034695, -1.200000000000000030E-05, 42.10535821593451544 ) ) ;
#86045=ORIENTED_EDGE ( 'NONE', *, *, #26804, .T. ) ;
#86097=CARTESIAN_POINT ( 'NONE',  ( -16.75187969033532553, -1.200000000000000030E-05, 23.05698433968612093 ) ) ;
#86121=CARTESIAN_POINT ( 'NONE',  ( 5.912233003206735837, 54.01420674394145749, 6.185142564729861903 ) ) ;
#86125=CARTESIAN_POINT ( 'NONE',  ( 29.87444201908948216, 8.057352084660386993, 42.09618695302963687 ) ) ;
#86134=ORIENTED_EDGE ( 'NONE', *, *, #5809, .F. ) ;
#86135=CARTESIAN_POINT ( 'NONE',  ( 28.79545026039418332, 10.21913446882435750, -41.74404769594831066 ) ) ;
#86139=MECHANICAL_DESIGN_GEOMETRIC_PRESENTATION_REPRESENTATION('',(#60271),#101583);
#86155=FILL_AREA_STYLE ('',( #3624 ) ) ;
#86178=FILL_AREA_STYLE_COLOUR ( '', #32995 ) ;
#86179=CARTESIAN_POINT ( 'NONE',  ( 1.249887406536827505, 36.80358475306034194, -28.33952629896104369 ) ) ;
#86218=VERTEX_POINT ( 'NONE', #98124 ) ;
#86221=CARTESIAN_POINT ( 'NONE',  ( 0.07858671332656751163, 13.70447791526909143, -49.25000000000000711 ) ) ;
#86239=VECTOR ( 'NONE', #39970, 1000.000000000000000 ) ;
#86271=CARTESIAN_POINT ( 'NONE',  ( -37.56673239365849781, 27.60449318992554169, 13.45617127781067168 ) ) ;
#86332=CARTESIAN_POINT ( 'NONE',  ( -21.96335563855659601, 28.05277650238785725, 31.83030418064915779 ) ) ;
#86338=DIRECTION ( 'NONE',  ( 0.000000000000000000, 0.000000000000000000, 1.000000000000000000 ) ) ;
#86341=EDGE_CURVE ( 'NONE', #73607, #59854, #51388, .T. ) ;
#86350=CARTESIAN_POINT ( 'NONE',  ( -1.098815040102374185, 51.92265547973028816, 8.383320812314803305 ) ) ;
#86357=CARTESIAN_POINT ( 'NONE',  ( 27.10511071441176867, 36.60571256639526894, -10.05698433968634653 ) ) ;
#86363=( NAMED_UNIT ( * ) SI_UNIT ( $, .STERADIAN. ) SOLID_ANGLE_UNIT ( ) );
#86399=CARTESIAN_POINT ( 'NONE',  ( 30.29489621385904385, 12.93001532776398577, -41.94819669044333210 ) ) ;
#86400=CYLINDRICAL_SURFACE ( 'NONE', #16750, 1.250000000000001110 ) ;
#86413=CARTESIAN_POINT ( 'NONE',  ( -29.07948315939603745, 13.68628896012808838, -39.75806671536133763 ) ) ;
#86414=CARTESIAN_POINT ( 'NONE',  ( 1.115575871468929448, 14.48101611498047703, 51.08097729577264090 ) ) ;
#86416=B_SPLINE_CURVE_WITH_KNOTS ( 'NONE', 3,
 ( #13970, #79780, #104584, #63626, #22648, #88420, #47405, #6410, #39348, #72227, #64154, #25855, #100741, #2042, #84038, #33925, #75944, #18815, #51120, #91612 ),
 .UNSPECIFIED., .F., .F.,
 ( 4, 2, 2, 2, 2, 2, 2, 2, 2, 4 ),
 ( 0.003145779775862817158, 0.003652023435422363865, 0.004158267094981910571, 0.004411388924761685225, 0.004664510754541460746, 0.005170754414101012657, 0.005676998073660564567, 0.006183241733220117345, 0.006689485392779668388, 0.007195729052339221166 ),
 .UNSPECIFIED. ) ;
#86430=CARTESIAN_POINT ( 'NONE',  ( -5.290067270632269114, -1.200000000000000030E-05, -6.031152949374520844 ) ) ;
#86445=( NAMED_UNIT ( * ) SI_UNIT ( $, .STERADIAN. ) SOLID_ANGLE_UNIT ( ) );
#86450=CARTESIAN_POINT ( 'NONE',  ( 6.509902245423385914, 53.49555288916370444, -7.566134441555309564 ) ) ;
#86456=CARTESIAN_POINT ( 'NONE',  ( -9.177191262247262671, 46.16966304056472126, -13.55798985375341204 ) ) ;
#86471=MECHANICAL_DESIGN_GEOMETRIC_PRESENTATION_REPRESENTATION('',(#46858),#17551);
#86477=VERTEX_POINT ( 'NONE', #88860 ) ;
#86483=CARTESIAN_POINT ( 'NONE',  ( -11.36508313652864821, 45.70357710343880342, 13.50657646266319567 ) ) ;
#86511=CARTESIAN_POINT ( 'NONE',  ( -49.26518742571406761, 13.24133944401902419, -15.39083778843300720 ) ) ;
#86513=ORIENTED_EDGE ( 'NONE', *, *, #92544, .F. ) ;
#86519=ORIENTED_EDGE ( 'NONE', *, *, #30370, .T. ) ;
#86521=VERTEX_POINT ( 'NONE', #6864 ) ;
#86556=CARTESIAN_POINT ( 'NONE',  ( 0.000000000000000000, 0.000000000000000000, 0.000000000000000000 ) ) ;
#86557=CARTESIAN_POINT ( 'NONE',  ( 4.659745271205086858, 51.51257451253292885, 8.372825955202660708 ) ) ;
#86562=CARTESIAN_POINT ( 'NONE',  ( 3.006829104376306210E-15, 0.000000000000000000, -24.55262289886175964 ) ) ;
#86571=EDGE_CURVE ( 'NONE', #89868, #45240, #33272, .T. ) ;
#86597=CARTESIAN_POINT ( 'NONE',  ( 9.768254851146028983, 53.46555892738330584, -2.423069053207274504 ) ) ;
#86645=EDGE_LOOP ( 'NONE', ( #29203, #94335, #95438, #103770 ) ) ;
#86648=CARTESIAN_POINT ( 'NONE',  ( 4.142849616820252293E-15, 27.68727484027578356, -33.82893434829263413 ) ) ;
#86652=DIRECTION ( 'NONE',  ( 0.000000000000000000, 0.000000000000000000, 1.000000000000000000 ) ) ;
#86670=CARTESIAN_POINT ( 'NONE',  ( -9.306844948305085907, 51.55227296925463776, 1.766188453538026559 ) ) ;
#86692=CARTESIAN_POINT ( 'NONE',  ( 9.954115923268258115, 44.05789748778097703, 12.94115310699293531 ) ) ;
#86716=FILL_AREA_STYLE ('',( #12264 ) ) ;
#86741=CARTESIAN_POINT ( 'NONE',  ( -8.400598463031300867, 51.89207564805971629, 1.531152949374564365 ) ) ;
#86746=EDGE_CURVE ( 'NONE', #68169, #69676, #350, .T. ) ;
#86762=LINE ( 'NONE', #21500, #89704 ) ;
#86830=STYLED_ITEM ( 'NONE', ( #63703 ), #16277 ) ;
#86838=EDGE_LOOP ( 'NONE', ( #34854, #77977, #50572, #52555 ) ) ;
#86852=CARTESIAN_POINT ( 'NONE',  ( 16.64348903516512834, 45.60392139269950462, -6.657797401561770911 ) ) ;
#86869=CARTESIAN_POINT ( 'NONE',  ( -30.71756172600976953, 13.08262462249239633, -41.56006324341318958 ) ) ;
#86872=( GEOMETRIC_REPRESENTATION_CONTEXT ( 3 ) GLOBAL_UNCERTAINTY_ASSIGNED_CONTEXT ( ( #43350 ) ) GLOBAL_UNIT_ASSIGNED_CONTEXT ( ( #81759, #90414, #17064 ) ) REPRESENTATION_CONTEXT ( 'NONE', 'WORKASPACE' ) );
#86888=VERTEX_POINT ( 'NONE', #12729 ) ;
#86896=CARTESIAN_POINT ( 'NONE',  ( 11.04004868613161072, 43.74858494517264518, 13.15750084466564118 ) ) ;
#86915=DIRECTION ( 'NONE',  ( -0.000000000000000000, 1.000000000000000000, -0.000000000000000000 ) ) ;
#86916=( NAMED_UNIT ( * ) PLANE_ANGLE_UNIT ( ) SI_UNIT ( $, .RADIAN. ) );
#86939=CARTESIAN_POINT ( 'NONE',  ( 37.72560624927822914, 25.42169923041442559, 13.45617127781006950 ) ) ;
#86961=EDGE_LOOP ( 'NONE', ( #33434, #26781 ) ) ;
#86963=CARTESIAN_POINT ( 'NONE',  ( -27.72495481923087368, 34.28547018021359349, 9.895597501992106970 ) ) ;
#86976=MECHANICAL_DESIGN_GEOMETRIC_PRESENTATION_REPRESENTATION('',(#39691),#58625);
#86978=CARTESIAN_POINT ( 'NONE',  ( 10.28624191511840280, 46.12099395432375104, 12.90779740156148847 ) ) ;
#86999=CARTESIAN_POINT ( 'NONE',  ( 10.28624191512063746, 46.12099395432516502, -12.90779740155508826 ) ) ;
#87000=CARTESIAN_POINT ( 'NONE',  ( 47.77442396816185521, 17.34920168383012040, -14.37330342454831289 ) ) ;
#87010=SURFACE_STYLE_FILL_AREA ( #43872 ) ;
#87014=CARTESIAN_POINT ( 'NONE',  ( -9.812456964692255923, 53.40207289977589511, -2.924987046467517171 ) ) ;
#87018=ORIENTED_EDGE ( 'NONE', *, *, #92768, .T. ) ;
#87024=CARTESIAN_POINT ( 'NONE',  ( -23.21751746555244722, -1.200000000000000030E-05, 30.70617127781060418 ) ) ;
#87026=( GEOMETRIC_REPRESENTATION_CONTEXT ( 3 ) GLOBAL_UNCERTAINTY_ASSIGNED_CONTEXT ( ( #102060 ) ) GLOBAL_UNIT_ASSIGNED_CONTEXT ( ( #23306, #23848, #89616 ) ) REPRESENTATION_CONTEXT ( 'NONE', 'WORKASPACE' ) );
#87049=CARTESIAN_POINT ( 'NONE',  ( 10.12154985177016364, 46.15835141668620878, -12.90779740156137123 ) ) ;
#87056=VERTEX_POINT ( 'NONE', #38122 ) ;
#87066=CARTESIAN_POINT ( 'NONE',  ( 49.09761780907516027, 12.98984206366268701, -16.25597134832139901 ) ) ;
#87069=CARTESIAN_POINT ( 'NONE',  ( -36.34489372084551206, 26.08142535203068135, 11.89321794026316681 ) ) ;
#87083=STYLED_ITEM ( 'NONE', ( #55431 ), #63566 ) ;
#87125=CARTESIAN_POINT ( 'NONE',  ( 4.522409606147229866, 53.69437142520751394, -8.280415083304497159 ) ) ;
#87127=CARTESIAN_POINT ( 'NONE',  ( -15.97269242673987932, 37.21081289561242755, 22.07591361862206014 ) ) ;
#87135=CARTESIAN_POINT ( 'NONE',  ( 26.94607068127204386, 36.65998315651609829, 10.05698433968586691 ) ) ;
#87166=DIRECTION ( 'NONE',  ( -0.000000000000000000, 1.000000000000000000, -0.000000000000000000 ) ) ;
#87187=CARTESIAN_POINT ( 'NONE',  ( -8.876313894634513701, 51.71968240765218638, 1.561724931196740274 ) ) ;
#87210=CARTESIAN_POINT ( 'NONE',  ( 1.380949872273418549E-15, 50.89575828009192549, 11.27631144943088692 ) ) ;
#87213=CARTESIAN_POINT ( 'NONE',  ( -0.1687174074039889671, 44.08548369317415450, 16.24999999999993250 ) ) ;
#87219=ORIENTED_EDGE ( 'NONE', *, *, #33675, .F. ) ;
#87232=CARTESIAN_POINT ( 'NONE',  ( -0.1682904726799566431, 53.39766064372320642, -10.24999999999999822 ) ) ;
#87234=CARTESIAN_POINT ( 'NONE',  ( -5.290067270632269114, -1.200000000000000030E-05, -7.281152949374520844 ) ) ;
#87266=CARTESIAN_POINT ( 'NONE',  ( 1.235451739553820927, 10.14988630190398311, -50.72637377003573533 ) ) ;
#87268=FILL_AREA_STYLE ('',( #15487 ) ) ;
#87304=CARTESIAN_POINT ( 'NONE',  ( -26.48391857604995892, 37.08887766516708950, 7.710198647837219532 ) ) ;
#87316=CARTESIAN_POINT ( 'NONE',  ( 16.64348903516512834, -1.200000000000000030E-05, -4.157797401561768247 ) ) ;
#87319=CARTESIAN_POINT ( 'NONE',  ( -48.49490330227218493, 10.48921555948077611, 14.43974515805995829 ) ) ;
#87327=CARTESIAN_POINT ( 'NONE',  ( -30.23165830866663129, 7.786015354292214141, 41.98067155130487293 ) ) ;
#87330=ADVANCED_FACE ( 'NONE', ( #19694 ), #1844, .F. ) ;
#87339=CARTESIAN_POINT ( 'NONE',  ( -15.39222209860203883, 44.06956899279646933, -5.345204092738742752 ) ) ;
#87349=CARTESIAN_POINT ( 'NONE',  ( 0.000000000000000000, -1.200000000000000030E-05, 10.24999999999999822 ) ) ;
#87386=SURFACE_SIDE_STYLE ('',( #3804 ) ) ;
#87394=DIRECTION ( 'NONE',  ( -0.000000000000000000, 1.000000000000000000, 0.000000000000000000 ) ) ;
#87400=CARTESIAN_POINT ( 'NONE',  ( -0.6457514547323006671, 51.32291280783120158, 10.08327392035491599 ) ) ;
#87410=CARTESIAN_POINT ( 'NONE',  ( -0.6420036228809623546, 34.23282312928377991, 29.57568823882862219 ) ) ;
#87433=ORIENTED_EDGE ( 'NONE', *, *, #48254, .T. ) ;
#87443=CYLINDRICAL_SURFACE ( 'NONE', #105743, 1.249999999999999334 ) ;
#87448=DIRECTION ( 'NONE',  ( 0.000000000000000000, 0.000000000000000000, 1.000000000000000000 ) ) ;
#87456=CARTESIAN_POINT ( 'NONE',  ( 17.08031957351993668, 34.19942078064286761, 24.26593081561334486 ) ) ;
#87481=ORIENTED_EDGE ( 'NONE', *, *, #96370, .F. ) ;
#87494=STYLED_ITEM ( 'NONE', ( #96425 ), #29969 ) ;
#87515=ORIENTED_EDGE ( 'NONE', *, *, #29726, .T. ) ;
#87520=CARTESIAN_POINT ( 'NONE',  ( -11.50618969897588428, 45.40753567543399782, 14.44225189481708682 ) ) ;
#87555=CARTESIAN_POINT ( 'NONE',  ( 28.32728760970740112, 34.16880792299276948, -9.119155454780885961 ) ) ;
#87569=PRESENTATION_STYLE_ASSIGNMENT (( #71361 ) ) ;
#87576=CARTESIAN_POINT ( 'NONE',  ( -37.88732364326676816, 27.49841400577992445, -13.42516778733551241 ) ) ;
#87598=DIRECTION ( 'NONE',  ( 0.000000000000000000, 0.000000000000000000, 1.000000000000000000 ) ) ;
#87602=CARTESIAN_POINT ( 'NONE',  ( 38.32908635939623565, 27.37244634754295092, 13.21054841214205311 ) ) ;
#87662=CARTESIAN_POINT ( 'NONE',  ( 25.92903732128599970, 37.10984168163323460, 9.238478874643890393 ) ) ;
#87671=CARTESIAN_POINT ( 'NONE',  ( 23.21751746555144180, 27.38103382803512176, -33.20617127781698485 ) ) ;
#87701=CARTESIAN_POINT ( 'NONE',  ( 30.23149608710470915, 7.786108077162794849, 41.98074016422795296 ) ) ;
#87741=CARTESIAN_POINT ( 'NONE',  ( -0.3345420830801542067, 25.18327404291766669, -40.70732875437715137 ) ) ;
#87749=MECHANICAL_DESIGN_GEOMETRIC_PRESENTATION_REPRESENTATION('',(#18945),#49850);
#87761=EDGE_CURVE ( 'NONE', #17374, #38799, #21630, .T. ) ;
#87764=CARTESIAN_POINT ( 'NONE',  ( -1.217303283917842371, 53.94016066554750211, -8.674587859239702325 ) ) ;
#87776=VERTEX_POINT ( 'NONE', #95579 ) ;
#87796=CARTESIAN_POINT ( 'NONE',  ( 17.51117938516244976, 36.87948859581990035, 22.05134542098255324 ) ) ;
#87812=AXIS2_PLACEMENT_3D ( 'NONE', #13138, #46067, #96218 ) ;
#87816=CARTESIAN_POINT ( 'NONE',  ( -27.26366621554978309, 36.83106128561345827, 7.556984339686017904 ) ) ;
#87819=EDGE_LOOP ( 'NONE', ( #41499, #97017, #53162, #13642 ) ) ;
#87822=ORIENTED_EDGE ( 'NONE', *, *, #21536, .T. ) ;
#87846=LINE ( 'NONE', #102428, #89735 ) ;
#87849=CARTESIAN_POINT ( 'NONE',  ( -48.48335035450828201, 8.813057796081508855, 16.77177117249955174 ) ) ;
#87902=DIRECTION ( 'NONE',  ( 0.000000000000000000, 1.000000000000000000, 0.000000000000000000 ) ) ;
#87904=CARTESIAN_POINT ( 'NONE',  ( 15.39709502357282922, 46.16515237750017775, -5.602001606816853219 ) ) ;
#87908=DIRECTION ( 'NONE',  ( -0.000000000000000000, 1.000000000000000000, -0.000000000000000000 ) ) ;
#87910=CARTESIAN_POINT ( 'NONE',  ( -17.08493112194819830, 36.32471929476455585, -24.27338705487295201 ) ) ;
#87927=CARTESIAN_POINT ( 'NONE',  ( -5.290067270632216712, 52.08006895350504095, 6.031152949374556371 ) ) ;
#87939=CARTESIAN_POINT ( 'NONE',  ( -0.8340752422583500580, 12.93528688290565043, 49.56574184153335239 ) ) ;
#87950=CARTESIAN_POINT ( 'NONE',  ( 22.80797863425486938, 28.18718824344973584, 30.77216081686022875 ) ) ;
#87998=LINE ( 'NONE', #38917, #3527 ) ;
#88019=DIRECTION ( 'NONE',  ( 0.000000000000000000, 0.000000000000000000, 1.000000000000000000 ) ) ;
#88036=( GEOMETRIC_REPRESENTATION_CONTEXT ( 3 ) GLOBAL_UNCERTAINTY_ASSIGNED_CONTEXT ( ( #26820 ) ) GLOBAL_UNIT_ASSIGNED_CONTEXT ( ( #90012, #88432, #39360 ) ) REPRESENTATION_CONTEXT ( 'NONE', 'WORKASPACE' ) );
#88038=COLOUR_RGB ( '', 0.08235294, 0.09019608, 0.10196078) ;
#88049=CARTESIAN_POINT ( 'NONE',  ( -10.92969676275529700, 45.30189166192088379, 15.24269870591663079 ) ) ;
#88054=DIRECTION ( 'NONE',  ( 0.000000000000000000, 1.000000000000000000, 0.000000000000000000 ) ) ;
#88077=CARTESIAN_POINT ( 'NONE',  ( 16.34245632501163925, 37.19060558336133226, 21.87293403489666588 ) ) ;
#88079=CARTESIAN_POINT ( 'NONE',  ( 5.581309233574441675E-23, 43.17555810750860701, -18.75000000000000355 ) ) ;
#88105=SURFACE_STYLE_FILL_AREA ( #21802 ) ;
#88111=CARTESIAN_POINT ( 'NONE',  ( 10.45113867624397841, 45.35217484112028075, 15.40779740156150091 ) ) ;
#88126=DIRECTION ( 'NONE',  ( 0.000000000000000000, 0.000000000000000000, 1.000000000000000000 ) ) ;
#88127=B_SPLINE_CURVE_WITH_KNOTS ( 'NONE', 3,
 ( #64064, #9909, #74107, #67102, #55911, #99987, #31179, #66562, #90845, #42819, #88852, #39254, #91384, #75714, #16963, #91902, #72129, #49839, #26157, #82746, #33160, #1808, #34767, #41221, #8847, #50362, #41752, #42279, #25618, #67640 ),
 .UNSPECIFIED., .F., .F.,
 ( 4, 2, 2, 2, 2, 2, 2, 2, 2, 2, 2, 2, 2, 2, 4 ),
 ( 0.008220542767890477720, 0.008453091251724709904, 0.008685639735558942087, 0.009150736703227401250, 0.009615833670895858679, 0.01008093063856431784, 0.01101112457390123443, 0.01194131850923815102, 0.01287151244457507282, 0.01380170637991199462, 0.01426680334758045204, 0.01473190031524891121, 0.01519699728291737037, 0.01542954576675160082, 0.01566209425058583127 ),
 .UNSPECIFIED. ) ;
#88138=EDGE_CURVE ( 'NONE', #12068, #5362, #96517, .T. ) ;
#88140=VERTEX_POINT ( 'NONE', #105130 ) ;
#88141=B_SPLINE_CURVE_WITH_KNOTS ( 'NONE', 3,
 ( #50141, #91163, #91681, #486, #76009, #1573, #33455, #49068, #26448, #34002, #58234, #66872, #81963, #57688, #25377, #73883 ),
 .UNSPECIFIED., .F., .F.,
 ( 4, 2, 2, 2, 2, 2, 2, 4 ),
 ( 0.007045997238651392942, 0.007550033810006847451, 0.008054070381362302827, 0.008558106952717758203, 0.009062143524073211845, 0.009566180095428667221, 0.01007021666678412086, 0.01107828980949503161 ),
 .UNSPECIFIED. ) ;
#88147=CARTESIAN_POINT ( 'NONE',  ( -5.934039023508266730, 53.39575557745317980, 8.365659210409152280 ) ) ;
#88171=CARTESIAN_POINT ( 'NONE',  ( 0.000000000000000000, 29.08768991669519721, 0.000000000000000000 ) ) ;
#88177=CARTESIAN_POINT ( 'NONE',  ( -23.05214773880026513, 26.02499767950420306, 30.70617127781060418 ) ) ;
#88186=ADVANCED_FACE ( 'NONE', ( #63628 ), #6412, .F. ) ;
#88188=FILL_AREA_STYLE_COLOUR ( '', #92079 ) ;
#88190=ORIENTED_EDGE ( 'NONE', *, *, #88739, .F. ) ;
#88198=UNCERTAINTY_MEASURE_WITH_UNIT (LENGTH_MEASURE( 1.000000000000000082E-05 ), #21090, 'distance_accuracy_value', 'NONE');
#88206=CARTESIAN_POINT ( 'NONE',  ( 0.6191880370026833225, 18.48281550088974257, -49.41023453029059453 ) ) ;
#88208=DIRECTION ( 'NONE',  ( 0.000000000000000000, 0.000000000000000000, 1.000000000000000000 ) ) ;
#88217=VERTEX_POINT ( 'NONE', #59246 ) ;
#88218=ORIENTED_EDGE ( 'NONE', *, *, #9154, .F. ) ;
#88220=DIRECTION ( 'NONE',  ( -0.000000000000000000, 1.000000000000000000, -0.000000000000000000 ) ) ;
#88224=PRESENTATION_STYLE_ASSIGNMENT (( #22453 ) ) ;
#88235=CARTESIAN_POINT ( 'NONE',  ( 0.000000000000000000, 55.00000000000000000, 0.000000000000000000 ) ) ;
#88244=CARTESIAN_POINT ( 'NONE',  ( 47.55484174479031623, 16.07433637411964611, 16.76829442854542052 ) ) ;
#88253=SURFACE_STYLE_FILL_AREA ( #55325 ) ;
#88260=COLOUR_RGB ( '', 0.31764706, 0.68627451, 0.89019608) ;
#88265=CARTESIAN_POINT ( 'NONE',  ( 48.02835407290504577, 16.78162100668611956, -14.35535821593549954 ) ) ;
#88268=CARTESIAN_POINT ( 'NONE',  ( 9.147872746976656089, 44.02395455486185227, 13.63474389503118012 ) ) ;
#88301=( NAMED_UNIT ( * ) PLANE_ANGLE_UNIT ( ) SI_UNIT ( $, .RADIAN. ) );
#88316=CYLINDRICAL_SURFACE ( 'NONE', #90776, 22.55262289886175964 ) ;
#88322=CARTESIAN_POINT ( 'NONE',  ( -8.559508646656370345, 51.83514083332403999, 1.531152949374564365 ) ) ;
#88327=CARTESIAN_POINT ( 'NONE',  ( 0.7797239981822461363, 8.371946713100552273, -51.48153055130863009 ) ) ;
#88344=ORIENTED_EDGE ( 'NONE', *, *, #24802, .T. ) ;
#88388=CARTESIAN_POINT ( 'NONE',  ( -30.59734358679111565, 7.793378852367141896, 41.71107540015031390 ) ) ;
#88389=CARTESIAN_POINT ( 'NONE',  ( 28.79546424415136485, 15.38851513919406777, 41.74402054108266924 ) ) ;
#88397=CARTESIAN_POINT ( 'NONE',  ( -27.85247631086664200, 36.60167368073183525, -7.792110844177867257 ) ) ;
#88418=VERTEX_POINT ( 'NONE', #80605 ) ;
#88420=CARTESIAN_POINT ( 'NONE',  ( -7.622868062079398932, 54.26469983982431700, -1.949254839742071033 ) ) ;
#88428=ORIENTED_EDGE ( 'NONE', *, *, #28365, .T. ) ;
#88430=VECTOR ( 'NONE', #95653, 1000.000000000000000 ) ;
#88432=( NAMED_UNIT ( * ) PLANE_ANGLE_UNIT ( ) SI_UNIT ( $, .RADIAN. ) );
#88434=ADVANCED_FACE ( 'NONE', ( #24015 ), #56314, .F. ) ;
#88459=EDGE_CURVE ( 'NONE', #91423, #91282, #34433, .T. ) ;
#88461=UNCERTAINTY_MEASURE_WITH_UNIT (LENGTH_MEASURE( 1.000000000000000082E-05 ), #31891, 'distance_accuracy_value', 'NONE');
#88465=CARTESIAN_POINT ( 'NONE',  ( -1.250037285469578707, 34.50112784842972502, 28.81831915451376602 ) ) ;
#88474=EDGE_LOOP ( 'NONE', ( #27901, #43987 ) ) ;
#88480=FILL_AREA_STYLE ('',( #105702 ) ) ;
#88487=( GEOMETRIC_REPRESENTATION_CONTEXT ( 3 ) GLOBAL_UNCERTAINTY_ASSIGNED_CONTEXT ( ( #4971 ) ) GLOBAL_UNIT_ASSIGNED_CONTEXT ( ( #58294, #75540, #1635 ) ) REPRESENTATION_CONTEXT ( 'NONE', 'WORKASPACE' ) );
#88493=ORIENTED_EDGE ( 'NONE', *, *, #102147, .T. ) ;
#88512=CARTESIAN_POINT ( 'NONE',  ( 26.35354840416186661, 34.76403232285502298, -9.818490863206431385 ) ) ;
#88513=LINE ( 'NONE', #89567, #74439 ) ;
#88515=CARTESIAN_POINT ( 'NONE',  ( -29.68315524077004497, 8.302504244945346557, -42.10535821593474282 ) ) ;
#88516=B_SPLINE_CURVE_WITH_KNOTS ( 'NONE', 3,
 ( #52614, #3009, #35961, #36492, #45088, #77967, #63401, #41087, #98773, #33024, #40551, #55264, #46655, #4617, #79553, #16271, #13745, #24925 ),
 .UNSPECIFIED., .F., .F.,
 ( 4, 2, 2, 2, 2, 2, 2, 2, 4 ),
 ( 0.007125446813973603487, 0.007629686116325599433, 0.008133925418677596247, 0.008638164721029592194, 0.009142404023381588141, 0.009646643325733585822, 0.01015088262808558003, 0.01065512193043757772, 0.01115936123278957366 ),
 .UNSPECIFIED. ) ;
#88520=CARTESIAN_POINT ( 'NONE',  ( 38.81963054373370881, 25.17304704673439986, 12.35078328273734805 ) ) ;
#88529=CARTESIAN_POINT ( 'NONE',  ( 23.99554787606954420, 25.16759095613464225, 32.93816323708791316 ) ) ;
#88541=PRESENTATION_STYLE_ASSIGNMENT (( #71803 ) ) ;
#88560=CARTESIAN_POINT ( 'NONE',  ( 23.21751746555303342, 25.25267828308493989, 33.20617127781017075 ) ) ;
#88600=CARTESIAN_POINT ( 'NONE',  ( 15.64272365568285217, 37.16721670561516078, 22.45732330511662056 ) ) ;
#88604=CARTESIAN_POINT ( 'NONE',  ( -49.27896781154974803, 13.08675713149239250, -15.56311823694480445 ) ) ;
#88619=FACE_OUTER_BOUND ( 'NONE', #10456, .T. ) ;
#88630=CARTESIAN_POINT ( 'NONE',  ( -0.9524572379025817437, 13.93511301620387499, -51.31333095019984825 ) ) ;
#88632=CARTESIAN_POINT ( 'NONE',  ( 0.000000000000000000, 0.000000000000000000, 0.000000000000000000 ) ) ;
#88637=ORIENTED_EDGE ( 'NONE', *, *, #72727, .F. ) ;
#88641=VERTEX_POINT ( 'NONE', #74375 ) ;
#88646=EDGE_CURVE ( 'NONE', #96644, #54873, #98740, .T. ) ;
#88715=CARTESIAN_POINT ( 'NONE',  ( -17.85237544995465342, 45.37579490857304165, -5.050174946722908231 ) ) ;
#88721=CARTESIAN_POINT ( 'NONE',  ( 24.20637929534462884, 27.76268499971478221, -31.17501708768082125 ) ) ;
#88726=CARTESIAN_POINT ( 'NONE',  ( 1.097170575850833218, 51.92387531005979895, 8.380158856765602238 ) ) ;
#88727=CYLINDRICAL_SURFACE ( 'NONE', #56007, 1.250000000000001110 ) ;
#88734=CARTESIAN_POINT ( 'NONE',  ( 23.05265313601412203, 25.28706265245096318, -33.20617127781077471 ) ) ;
#88737=CARTESIAN_POINT ( 'NONE',  ( 46.77767549600488906, 13.52659353100008843, -15.64517449361694723 ) ) ;
#88738=VERTEX_POINT ( 'NONE', #42545 ) ;
#88739=EDGE_CURVE ( 'NONE', #69676, #89428, #17793, .T. ) ;
#88741=EDGE_LOOP ( 'NONE', ( #40056, #79808 ) ) ;
#88743=CARTESIAN_POINT ( 'NONE',  ( 1.221913359428326018, 53.71105537643708061, 9.309427401043976147 ) ) ;
#88750=CARTESIAN_POINT ( 'NONE',  ( -9.500616112259193002, 44.08938505136232777, 13.17116827006698543 ) ) ;
#88752=EDGE_CURVE ( 'NONE', #40774, #25026, #265, .T. ) ;
#88768=CARTESIAN_POINT ( 'NONE',  ( 46.81266956378438948, 18.41561415511120714, 15.90959751601103633 ) ) ;
#88775=AXIS2_PLACEMENT_3D ( 'NONE', #60979, #75545, #10277 ) ;
#88794=PRESENTATION_STYLE_ASSIGNMENT (( #82686 ) ) ;
#88801=EDGE_CURVE ( 'NONE', #20102, #79761, #98555, .T. ) ;
#88810=CARTESIAN_POINT ( 'NONE',  ( -3.381870600466846067E-15, 46.21383923812598482, -16.24999999999995026 ) ) ;
#88831=PRESENTATION_STYLE_ASSIGNMENT (( #104476 ) ) ;
#88837=CARTESIAN_POINT ( 'NONE',  ( 0.7840884375884051849, 25.26123080618498307, -40.48700950034228896 ) ) ;
#88842=EDGE_CURVE ( 'NONE', #40774, #46319, #92366, .T. ) ;
#88844=CARTESIAN_POINT ( 'NONE',  ( -0.7767374935270013880, 34.98060154996775140, -27.51719054460002312 ) ) ;
#88852=CARTESIAN_POINT ( 'NONE',  ( -0.9888037323473499729, 17.70116029579951800, 49.73220125274776393 ) ) ;
#88860=CARTESIAN_POINT ( 'NONE',  ( 8.559508646656350805, 53.96349637827587031, -1.531152949374623651 ) ) ;
#88897=SURFACE_SIDE_STYLE ('',( #15529 ) ) ;
#88907=( NAMED_UNIT ( * ) SI_UNIT ( $, .STERADIAN. ) SOLID_ANGLE_UNIT ( ) );
#88922=CARTESIAN_POINT ( 'NONE',  ( -28.08564602980796820, 36.49793394831486637, -8.015104271803140890 ) ) ;
#88925=VECTOR ( 'NONE', #25468, 1000.000000000000227 ) ;
#88938=CARTESIAN_POINT ( 'NONE',  ( 11.38823185635503599, 43.21649034732992334, -14.75371867866905795 ) ) ;
#88951=AXIS2_PLACEMENT_3D ( 'NONE', #700, #92404, #33670 ) ;
#88971=ORIENTED_EDGE ( 'NONE', *, *, #18459, .T. ) ;
#88979=CARTESIAN_POINT ( 'NONE',  ( 48.15279758643736585, 14.66099993221041231, 16.85535821593428096 ) ) ;
#88986=CARTESIAN_POINT ( 'NONE',  ( -0.3344844736945739583, 35.06558596096873970, 27.29265241697899569 ) ) ;
#88993=( GEOMETRIC_REPRESENTATION_CONTEXT ( 3 ) GLOBAL_UNCERTAINTY_ASSIGNED_CONTEXT ( ( #29981 ) ) GLOBAL_UNIT_ASSIGNED_CONTEXT ( ( #67456, #69057, #28089 ) ) REPRESENTATION_CONTEXT ( 'NONE', 'WORKASPACE' ) );
#89008=CARTESIAN_POINT ( 'NONE',  ( 22.59351686035008910, 27.55929540978658920, 33.04221228726185444 ) ) ;
#89013=( LENGTH_UNIT ( ) NAMED_UNIT ( * ) SI_UNIT ( .MILLI., .METRE. ) );
#89031=CARTESIAN_POINT ( 'NONE',  ( 36.95466138685372925, 27.83244934716666208, 13.30748428295481922 ) ) ;
#89035=CARTESIAN_POINT ( 'NONE',  ( 26.02782056099105645, 34.92022792041685619, -9.461560381890144811 ) ) ;
#89041=CARTESIAN_POINT ( 'NONE',  ( -10.28624191511830155, -1.200000000000000030E-05, -12.90779740156156841 ) ) ;
#89049=CARTESIAN_POINT ( 'NONE',  ( -29.09632818934742104, 14.54213905807120000, -41.96777332363188151 ) ) ;
#89050=PRESENTATION_STYLE_ASSIGNMENT (( #97647 ) ) ;
#89057=CARTESIAN_POINT ( 'NONE',  ( 23.38321737095555619, 25.22051755256121197, 33.19792244304780837 ) ) ;
#89096=EDGE_LOOP ( 'NONE', ( #49312, #20861 ) ) ;
#89145=EDGE_LOOP ( 'NONE', ( #26429, #70094 ) ) ;
#89150=CARTESIAN_POINT ( 'NONE',  ( -22.59351686034986528, 27.55929540978658920, -33.04221228726202497 ) ) ;
#89161=ORIENTED_EDGE ( 'NONE', *, *, #90395, .F. ) ;
#89170=B_SPLINE_CURVE_WITH_KNOTS ( 'NONE', 3,
 ( #65518, #57937, #40698, #49852, #73586, #98405, #57403, #90318, #33699, #41764, #733, #66574, #102126, #75727, #76784, #28282, #20204, #69775, #102667, #61156 ),
 .UNSPECIFIED., .F., .F.,
 ( 4, 2, 2, 2, 2, 2, 2, 2, 2, 4 ),
 ( 0.007119059105098832045, 0.007623191790411414787, 0.008127324475723998395, 0.008379390818380289332, 0.008631457161036580270, 0.009135589846349162144, 0.009639722531661744018, 0.01014385521697432589, 0.01064798790228690777, 0.01115212058759948964 ),
 .UNSPECIFIED. ) ;
#89176=CARTESIAN_POINT ( 'NONE',  ( 48.55172137731254622, 13.85052760073793543, -16.74335408647284495 ) ) ;
#89235=VECTOR ( 'NONE', #104374, 1000.000000000000000 ) ;
#89240=SURFACE_SIDE_STYLE ('',( #71441 ) ) ;
#89242=CARTESIAN_POINT ( 'NONE',  ( -16.12471489245807987, 36.55922634087986012, 24.15021214291690299 ) ) ;
#89245=( NAMED_UNIT ( * ) SI_UNIT ( $, .STERADIAN. ) SOLID_ANGLE_UNIT ( ) );
#89253=CARTESIAN_POINT ( 'NONE',  ( 23.54757723015212179, 27.32420764371300237, -33.16469143611140424 ) ) ;
#89259=CARTESIAN_POINT ( 'NONE',  ( 4.651477914329386962E-14, 52.17923068443710832, 7.749999999999496403 ) ) ;
#89268=CARTESIAN_POINT ( 'NONE',  ( 21.99079640667137880, 25.96820120819537436, -31.66518509989418106 ) ) ;
#89289=CARTESIAN_POINT ( 'NONE',  ( -9.273762745476021863, 44.06279479628684470, 13.41996917811760781 ) ) ;
#89326=CARTESIAN_POINT ( 'NONE',  ( -1.250427155780938104, 25.55909391395953278, -39.65635458840486649 ) ) ;
#89338=ORIENTED_EDGE ( 'NONE', *, *, #19278, .F. ) ;
#89340=CARTESIAN_POINT ( 'NONE',  ( 29.68315524077033629, 13.47185074185905584, 42.10535821593451544 ) ) ;
#89361=DIRECTION ( 'NONE',  ( -0.000000000000000000, 1.000000000000000000, -0.000000000000000000 ) ) ;
#89379=CARTESIAN_POINT ( 'NONE',  ( 1.010662029212957780, 25.34442020277418450, -40.25335562281891555 ) ) ;
#89384=CARTESIAN_POINT ( 'NONE',  ( 0.3347578696900010420, 53.41133083292604766, -10.20729091610875905 ) ) ;
#89428=VERTEX_POINT ( 'NONE', #84106 ) ;
#89433=UNCERTAINTY_MEASURE_WITH_UNIT (LENGTH_MEASURE( 1.000000000000000082E-05 ), #709, 'distance_accuracy_value', 'NONE');
#89449=CARTESIAN_POINT ( 'NONE',  ( 29.27130674176784808, 18.74791880384170284, 39.67321021315746066 ) ) ;
#89452=EDGE_CURVE ( 'NONE', #101117, #81828, #68980, .T. ) ;
#89453=DIRECTION ( 'NONE',  ( -0.000000000000000000, 1.000000000000000000, 0.000000000000000000 ) ) ;
#89458=CARTESIAN_POINT ( 'NONE',  ( -27.26370785122089302, 36.83104668818905481, -7.556984339686001917 ) ) ;
#89464=EDGE_LOOP ( 'NONE', ( #60117, #88637, #10711, #16116 ) ) ;
#89472=VECTOR ( 'NONE', #43988, 1000.000000000000000 ) ;
#89483=CARTESIAN_POINT ( 'NONE',  ( -17.86532138382085932, 45.30096510830348677, 5.720552158557736355 ) ) ;
#89486=ORIENTED_EDGE ( 'NONE', *, *, #2529, .T. ) ;
#89499=CARTESIAN_POINT ( 'NONE',  ( -1.219798531186343959, 25.50106792483703089, 39.81686016623014979 ) ) ;
#89500=CARTESIAN_POINT ( 'NONE',  ( 1.249971410579568287, 27.80243479384745342, -39.34029123867090050 ) ) ;
#89511=CARTESIAN_POINT ( 'NONE',  ( -16.91747028431907296, 34.95463172523481177, -21.80698433968594685 ) ) ;
#89520=CARTESIAN_POINT ( 'NONE',  ( -28.43338544108043919, 12.59781646960431623, 40.78060993930063205 ) ) ;
#89530=CARTESIAN_POINT ( 'NONE',  ( 9.635740931621784355, 51.40895863168635316, 2.124525052985154261 ) ) ;
#89535=CARTESIAN_POINT ( 'NONE',  ( 28.21386086657646075, 34.30365941694820719, -8.223977910641220745 ) ) ;
#89554=CARTESIAN_POINT ( 'NONE',  ( 0.000000000000000000, 43.19193163660326462, 0.000000000000000000 ) ) ;
#89558=CARTESIAN_POINT ( 'NONE',  ( -37.56673239365863282, -1.200000000000000030E-05, -13.45617127781024891 ) ) ;
#89567=CARTESIAN_POINT ( 'NONE',  ( -16.64348903516517098, -1.200000000000000030E-05, 4.157797401561652784 ) ) ;
#89569=CARTESIAN_POINT ( 'NONE',  ( -28.43345358724999983, 12.59863739772598024, -40.78014218160733861 ) ) ;
#89577=CARTESIAN_POINT ( 'NONE',  ( 0.8397591720178106955, 25.95816433063382789, 38.57052554651150444 ) ) ;
#89584=CARTESIAN_POINT ( 'NONE',  ( -28.72970484482200604, 18.79180695567417203, -40.04448862869271153 ) ) ;
#89593=ORIENTED_EDGE ( 'NONE', *, *, #29950, .F. ) ;
#89601=CARTESIAN_POINT ( 'NONE',  ( 4.651477914329386962E-14, 52.17923068443710832, 7.749999999999496403 ) ) ;
#89603=CARTESIAN_POINT ( 'NONE',  ( 29.27137781856704990, 18.74786498819648983, -39.67318581983496983 ) ) ;
#89616=( NAMED_UNIT ( * ) SI_UNIT ( $, .STERADIAN. ) SOLID_ANGLE_UNIT ( ) );
#89654=CARTESIAN_POINT ( 'NONE',  ( 16.75187969033571989, -1.200000000000000030E-05, 23.05698433968582961 ) ) ;
#89666=DIRECTION ( 'NONE',  ( 0.000000000000000000, 1.000000000000000000, -0.000000000000000000 ) ) ;
#89667=CARTESIAN_POINT ( 'NONE',  ( -38.75664172650044748, 25.16721717615375908, 12.59822445845297700 ) ) ;
#89671=AXIS2_PLACEMENT_3D ( 'NONE', #83919, #60734, #12151 ) ;
#89675=CARTESIAN_POINT ( 'NONE',  ( -48.02835407290534420, 16.78162100668604495, -14.35535821593460248 ) ) ;
#89684=CARTESIAN_POINT ( 'NONE',  ( -22.65274949039500285, 28.20149500596347281, -30.83785112677304951 ) ) ;
#89702=ADVANCED_BREP_SHAPE_REPRESENTATION ( '', ( #16251, #10728 ), #105516 ) ;
#89704=VECTOR ( 'NONE', #103970, 1000.000000000000227 ) ;
#89710=CARTESIAN_POINT ( 'NONE',  ( 0.8402286030463997912, 34.96037729579965969, -27.57089172558451295 ) ) ;
#89715=CARTESIAN_POINT ( 'NONE',  ( 0.6421110334426624044, 51.32541146260925302, -10.07566082288705367 ) ) ;
#89719=CARTESIAN_POINT ( 'NONE',  ( 49.03380706566427705, 8.971284072415114608, 14.85953237006425276 ) ) ;
#89721=CARTESIAN_POINT ( 'NONE',  ( 10.69660278669753417, 43.19295133451930724, 15.34151949443403140 ) ) ;
#89730=VECTOR ( 'NONE', #89453, 1000.000000000000000 ) ;
#89735=VECTOR ( 'NONE', #4797, 1000.000000000000000 ) ;
#89744=ORIENTED_EDGE ( 'NONE', *, *, #73268, .F. ) ;
#89754=VECTOR ( 'NONE', #97973, 1000.000000000000000 ) ;
#89766=CARTESIAN_POINT ( 'NONE',  ( 28.35193698574008181, 34.21473308898948318, 8.617696936426447962 ) ) ;
#89771=CARTESIAN_POINT ( 'NONE',  ( 15.56705434506301522, 43.91951069372706939, 6.063903585636011506 ) ) ;
#89781=CARTESIAN_POINT ( 'NONE',  ( -23.97876356160471900, 25.74925960686173809, 30.95194294911825850 ) ) ;
#89791=CARTESIAN_POINT ( 'NONE',  ( 1.250573470519673158, 45.68617730187271775, 17.65550772099327759 ) ) ;
#89803=CARTESIAN_POINT ( 'NONE',  ( 46.97259151695090651, 12.59255281441344110, -16.28847157548977265 ) ) ;
#89806=ORIENTED_EDGE ( 'NONE', *, *, #90298, .T. ) ;
#89807=CARTESIAN_POINT ( 'NONE',  ( 0.3382013191121669982, 53.40883116819954068, 10.21491085553634726 ) ) ;
#89814=( NAMED_UNIT ( * ) SI_UNIT ( $, .STERADIAN. ) SOLID_ANGLE_UNIT ( ) );
#89816=CARTESIAN_POINT ( 'NONE',  ( 30.75880901179687044, 7.960713337733333894, 41.50491223544427299 ) ) ;
#89819=FACE_OUTER_BOUND ( 'NONE', #83438, .T. ) ;
#89823=ORIENTED_EDGE ( 'NONE', *, *, #35152, .F. ) ;
#89850=CARTESIAN_POINT ( 'NONE',  ( -0.08409598735685096249, 26.07813853931758175, -38.24999999999999289 ) ) ;
#89851=CARTESIAN_POINT ( 'NONE',  ( 16.64348903516512834, -1.200000000000000030E-05, -6.657797401561770911 ) ) ;
#89856=CARTESIAN_POINT ( 'NONE',  ( 1.100705560355868640, 45.52331009687405583, -18.11393409840396274 ) ) ;
#89858=AXIS2_PLACEMENT_3D ( 'NONE', #88632, #33080, #72958 ) ;
#89868=VERTEX_POINT ( 'NONE', #42998 ) ;
#89871=CARTESIAN_POINT ( 'NONE',  ( 16.75187969033571989, 34.25544727262119693, 24.30698433968583316 ) ) ;
#89901=CARTESIAN_POINT ( 'NONE',  ( 0.6441586697988379573, 54.23817744608182778, -7.915922717621211468 ) ) ;
#89914=VERTEX_POINT ( 'NONE', #26854 ) ;
#89916=CARTESIAN_POINT ( 'NONE',  ( 46.96405579082752979, 13.62080378033664196, 14.94667195310829122 ) ) ;
#89927=CARTESIAN_POINT ( 'NONE',  ( 23.21751746555303342, 25.98869614573808207, 30.70617127781016720 ) ) ;
#89949=CARTESIAN_POINT ( 'NONE',  ( 7.465530826735402137, 54.30101273655428429, -2.153335479310952039 ) ) ;
#89967=CARTESIAN_POINT ( 'NONE',  ( 28.49094055106857581, 13.12977990610423085, 40.46781900651338049 ) ) ;
#89978=CARTESIAN_POINT ( 'NONE',  ( -16.32395179134260843, 43.58768466397686581, -6.626586996422831888 ) ) ;
#89985=FILL_AREA_STYLE_COLOUR ( '', #48654 ) ;
#90007=ORIENTED_EDGE ( 'NONE', *, *, #44725, .F. ) ;
#90012=( LENGTH_UNIT ( ) NAMED_UNIT ( * ) SI_UNIT ( .MILLI., .METRE. ) );
#90020=CARTESIAN_POINT ( 'NONE',  ( -0.4143833371980254476, 26.05270874984543639, 38.31770394904153676 ) ) ;
#90029=CARTESIAN_POINT ( 'NONE',  ( -0.3333649190976236132, 51.28285977629721515, 10.20765125107239690 ) ) ;
#90031=CARTESIAN_POINT ( 'NONE',  ( -17.73896008590444140, 43.18065877884676951, 6.032786456716696222 ) ) ;
#90033=CARTESIAN_POINT ( 'NONE',  ( 8.559508646656350805, -1.200000000000000030E-05, -1.531152949374623873 ) ) ;
#90034=CARTESIAN_POINT ( 'NONE',  ( -5.623207912502805605, 51.29174090390986152, -8.497605637484657137 ) ) ;
#90039=CARTESIAN_POINT ( 'NONE',  ( -29.59437054465040262, 13.24940423479644735, 39.60535821593506256 ) ) ;
#90040=EDGE_CURVE ( 'NONE', #92392, #32665, #27862, .T. ) ;
#90059=CARTESIAN_POINT ( 'NONE',  ( -16.80223567637828452, 43.70004508566929502, -4.157797401561437844 ) ) ;
#90083=EDGE_LOOP ( 'NONE', ( #54737, #94631, #2556, #82368, #5876, #63196, #6906 ) ) ;
#90091=CARTESIAN_POINT ( 'NONE',  ( 26.12342974137753870, 34.87054449434884162, -9.597107001362633838 ) ) ;
#90098=CARTESIAN_POINT ( 'NONE',  ( 37.56673239365870387, 25.75719283951018923, 10.95617127780998956 ) ) ;
#90108=CARTESIAN_POINT ( 'NONE',  ( 24.32698811271407635, 25.20814661221487896, 32.55533594236108286 ) ) ;
#90115=EDGE_LOOP ( 'NONE', ( #88218, #101736, #62966, #10139 ) ) ;
#90135=( NAMED_UNIT ( * ) SI_UNIT ( $, .STERADIAN. ) SOLID_ANGLE_UNIT ( ) );
#90153=ORIENTED_EDGE ( 'NONE', *, *, #4277, .T. ) ;
#90160=ORIENTED_EDGE ( 'NONE', *, *, #21161, .F. ) ;
#90167=CARTESIAN_POINT ( 'NONE',  ( 17.86591196048134478, 43.17255793597502134, -5.719226232856852832 ) ) ;
#90173=CARTESIAN_POINT ( 'NONE',  ( -24.46939029779962027, 27.46660112286069833, 31.99934855281016155 ) ) ;
#90189=CARTESIAN_POINT ( 'NONE',  ( 15.53259594841288127, 37.09623604092399773, 22.76975648258493123 ) ) ;
#90199=DIRECTION ( 'NONE',  ( 0.000000000000000000, 1.000000000000000000, -0.000000000000000000 ) ) ;
#90214=ORIENTED_EDGE ( 'NONE', *, *, #54374, .T. ) ;
#90224=SURFACE_STYLE_FILL_AREA ( #65422 ) ;
#90249=EDGE_CURVE ( 'NONE', #95728, #16669, #31098, .T. ) ;
#90271=COLOUR_RGB ( '', 0.31764706, 0.68627451, 0.89019608) ;
#90286=EDGE_LOOP ( 'NONE', ( #28612, #77191, #3799, #7993 ) ) ;
#90298=EDGE_CURVE ( 'NONE', #65026, #59863, #62473, .T. ) ;
#90310=CARTESIAN_POINT ( 'NONE',  ( 1.009208733680683423, 51.97703478562248591, 8.244597349404022779 ) ) ;
#90315=CARTESIAN_POINT ( 'NONE',  ( 0.07724506424403219940, 12.91535575337014308, -51.75000000000000000 ) ) ;
#90318=CARTESIAN_POINT ( 'NONE',  ( -11.38830949524098912, 45.34487012134832895, -14.75357462089496252 ) ) ;
#90322=CARTESIAN_POINT ( 'NONE',  ( 47.29368197624711456, 13.12573487771098613, -14.58950938768722771 ) ) ;
#90328=CARTESIAN_POINT ( 'NONE',  ( 1.002517492551115330, 54.10386726457789308, 8.249092293095747763 ) ) ;
#90330=CARTESIAN_POINT ( 'NONE',  ( -36.80474084615011776, 28.12598060908854336, 11.20119898579589801 ) ) ;
#90343=EDGE_CURVE ( 'NONE', #46768, #46516, #92067, .T. ) ;
#90351=B_SPLINE_CURVE_WITH_KNOTS ( 'NONE', 3,
 ( #80090, #30519, #95763, #13760, #63416, #22437, #88206, #9374, #49304, #9920, #67111, #16423, #1817, #42288, #82753, #17509, #18040, #41230, #42827, #91394, #26164, #83809, #75723, #8855, #98916, #99454, #1276, #99996, #90315, #25627 ),
 .UNSPECIFIED., .F., .F.,
 ( 4, 2, 2, 2, 2, 2, 2, 2, 2, 2, 2, 2, 2, 2, 4 ),
 ( 0.006610199206806503976, 0.006841026956352766995, 0.007071854705899030015, 0.007533510204991551718, 0.007995165704084072553, 0.008456821203176593388, 0.009380132201361635058, 0.01030344319954667673, 0.01122675419773171146, 0.01215006519591674272, 0.01261172069500925835, 0.01307337619410177225, 0.01353503169319428615, 0.01376585944274054743, 0.01399668719228680698 ),
 .UNSPECIFIED. ) ;
#90356=CARTESIAN_POINT ( 'NONE',  ( 5.453780363133834186, 52.04077698858505130, -6.031152949374485317 ) ) ;
#90365=FILL_AREA_STYLE_COLOUR ( '', #2226 ) ;
#90376=CARTESIAN_POINT ( 'NONE',  ( -9.646908473743026846, 53.40519435939982174, 3.403286223225750362 ) ) ;
#90380=CARTESIAN_POINT ( 'NONE',  ( -0.6412850917382576510, 43.23485188436026050, 18.57615738839334085 ) ) ;
#90388=CARTESIAN_POINT ( 'NONE',  ( 5.974456367264334036E-20, 45.30391365246044444, -18.75000000000000355 ) ) ;
#90395=EDGE_CURVE ( 'NONE', #34804, #32781, #104987, .T. ) ;
#90414=( NAMED_UNIT ( * ) PLANE_ANGLE_UNIT ( ) SI_UNIT ( $, .RADIAN. ) );
#90425=CARTESIAN_POINT ( 'NONE',  ( 9.523267564284003228, 45.61198619316643743, 15.16070064068354739 ) ) ;
#90439=FILL_AREA_STYLE_COLOUR ( '', #18589 ) ;
#90447=ORIENTED_EDGE ( 'NONE', *, *, #42902, .T. ) ;
#90449=CARTESIAN_POINT ( 'NONE',  ( 47.18533784750991344, 13.30762177597463847, 14.68117529621389750 ) ) ;
#90452=LINE ( 'NONE', #16564, #3245 ) ;
#90456=ORIENTED_EDGE ( 'NONE', *, *, #36004, .T. ) ;
#90459=CARTESIAN_POINT ( 'NONE',  ( 23.21751746555303342, 25.25267828308493989, 33.20617127781017075 ) ) ;
#90470=COLOUR_RGB ( '', 0.66274510, 0.83137255, 0.94901961) ;
#90476=AXIS2_PLACEMENT_3D ( 'NONE', #100304, #17814, #58805 ) ;
#90490=SURFACE_STYLE_USAGE ( .BOTH. , #88897 ) ;
#90498=CARTESIAN_POINT ( 'NONE',  ( 29.27049653814518848, 13.57913911089070780, 39.67351191892522877 ) ) ;
#90507=CARTESIAN_POINT ( 'NONE',  ( -28.77727207546517363, 18.82954237789026308, 39.99083609194100575 ) ) ;
#90510=CARTESIAN_POINT ( 'NONE',  ( -22.20476351154805172, 26.05629838265183906, 31.21875911480587718 ) ) ;
#90525=CARTESIAN_POINT ( 'NONE',  ( -27.10511071441183262, 34.47735702144344572, 10.05698433968616001 ) ) ;
#90526=( GEOMETRIC_REPRESENTATION_CONTEXT ( 3 ) GLOBAL_UNCERTAINTY_ASSIGNED_CONTEXT ( ( #21116 ) ) GLOBAL_UNIT_ASSIGNED_CONTEXT ( ( #29470, #28400, #38088 ) ) REPRESENTATION_CONTEXT ( 'NONE', 'WORKASPACE' ) );
#90527=CARTESIAN_POINT ( 'NONE',  ( 10.28624191511809371, 43.99263840937192782, -12.90779740156171407 ) ) ;
#90546=CARTESIAN_POINT ( 'NONE',  ( 15.51806636169577658, 46.21009754484516208, 4.857304170327764403 ) ) ;
#90554=CARTESIAN_POINT ( 'NONE',  ( -0.3342441623883664614, 25.18324729327973444, 40.70740451072503419 ) ) ;
#90555=CARTESIAN_POINT ( 'NONE',  ( 0.7781286854980117296, 27.39149973645235647, -40.48175932167306001 ) ) ;
#90566=CARTESIAN_POINT ( 'NONE',  ( -17.26387333831402060, 43.28639006945349621, 6.496095472997780007 ) ) ;
#90581=VERTEX_POINT ( 'NONE', #76423 ) ;
#90585=CARTESIAN_POINT ( 'NONE',  ( 36.59027416739721872, 27.99615698493870397, -12.99074957500551086 ) ) ;
#90588=VERTEX_POINT ( 'NONE', #93155 ) ;
#90589=CARTESIAN_POINT ( 'NONE',  ( 28.35825693584814644, 34.17671750055550461, -8.950286295360427857 ) ) ;
#90598=EDGE_CURVE ( 'NONE', #44553, #58472, #57277, .T. ) ;
#90630=SURFACE_SIDE_STYLE ('',( #23800 ) ) ;
#90632=CARTESIAN_POINT ( 'NONE',  ( -28.43946827300288049, 12.73388556380908376, -40.70676336658363681 ) ) ;
#90641=VECTOR ( 'NONE', #25177, 1000.000000000000000 ) ;
#90643=CARTESIAN_POINT ( 'NONE',  ( 23.54609889741162121, 25.19605094436382231, 33.16507022216291034 ) ) ;
#90652=CARTESIAN_POINT ( 'NONE',  ( -4.961791431619821502, 52.14601839267029249, 6.072164406264656478 ) ) ;
#90659=CARTESIAN_POINT ( 'NONE',  ( 28.94969860575612230, 18.87958371857671835, -39.84024749387450015 ) ) ;
#90682=CARTESIAN_POINT ( 'NONE',  ( -1.009236793202067828, 54.10523466797827297, 8.245009025653098789 ) ) ;
#90683=CYLINDRICAL_SURFACE ( 'NONE', #98504, 35.82893434829263413 ) ;
#90709=CARTESIAN_POINT ( 'NONE',  ( -6.533875647324832059, 53.62318002580641974, -7.075595340869824668 ) ) ;
#90713=CARTESIAN_POINT ( 'NONE',  ( -23.29983671023154912, 28.09898118347551588, 30.70617127781060063 ) ) ;
#90725=CARTESIAN_POINT ( 'NONE',  ( -48.55396075288191327, 8.676907163023333425, -16.74236275264532381 ) ) ;
#90728=CARTESIAN_POINT ( 'NONE',  ( -38.66383876797932828, 25.31560946603492113, 11.52610263331877505 ) ) ;
#90730=CARTESIAN_POINT ( 'NONE',  ( 17.89487417552031445, 45.31800925772327560, 5.467316602108490464 ) ) ;
#90743=CARTESIAN_POINT ( 'NONE',  ( -23.05189055320584046, 27.41800202946304310, -33.19783182242394304 ) ) ;
#90758=CARTESIAN_POINT ( 'NONE',  ( -0.8430352374540970306, 13.67053680931865678, -51.42626865055270713 ) ) ;
#90776=AXIS2_PLACEMENT_3D ( 'NONE', #47302, #97436, #83263 ) ;
#90781=CARTESIAN_POINT ( 'NONE',  ( 48.02835407290544367, 9.771516447483593382, 16.85535821593427386 ) ) ;
#90791=FACE_OUTER_BOUND ( 'NONE', #12874, .T. ) ;
#90828=CARTESIAN_POINT ( 'NONE',  ( 0.000000000000000000, 24.35682532067546902, 0.000000000000000000 ) ) ;
#90833=CARTESIAN_POINT ( 'NONE',  ( 15.55735228453472274, 44.07604505559044838, 4.783429685249553920 ) ) ;
#90845=CARTESIAN_POINT ( 'NONE',  ( -0.8340869376443533767, 18.10461962298600724, 49.56574745738932819 ) ) ;
#90859=CARTESIAN_POINT ( 'NONE',  ( -9.204171687489189679, 45.78377104600745895, 14.80353108812683871 ) ) ;
#90877=CARTESIAN_POINT ( 'NONE',  ( 30.77294675439390659, 10.36444884528815180, 40.23167857000779435 ) ) ;
#90881=CARTESIAN_POINT ( 'NONE',  ( 9.169403562584983902, 51.60716162735785417, -1.678691385831598604 ) ) ;
#90885=FACE_BOUND ( 'NONE', #88474, .T. ) ;
#90899=CARTESIAN_POINT ( 'NONE',  ( -16.64348903516517098, 43.75610143575153899, 4.157797401561652784 ) ) ;
#90915=ADVANCED_FACE ( 'NONE', ( #98961 ), #97917, .F. ) ;
#90916=CARTESIAN_POINT ( 'NONE',  ( 38.31446012149793745, 25.47195784124091844, -11.19161216425135308 ) ) ;
#90920=CARTESIAN_POINT ( 'NONE',  ( -8.881211395233728823, 53.58339314524378239, 3.999935137841994504 ) ) ;
#90924=CARTESIAN_POINT ( 'NONE',  ( -27.10511071441192144, 34.47735702144345282, -10.05698433968589178 ) ) ;
#90941=CARTESIAN_POINT ( 'NONE',  ( 8.455951367436818379E-15, 13.70447791526914294, 49.24999999999998579 ) ) ;
#90944=CARTESIAN_POINT ( 'NONE',  ( 16.42488309403321978, 34.33240771944122116, 24.27441078751466108 ) ) ;
#90994=CARTESIAN_POINT ( 'NONE',  ( 46.79842100651300996, 13.68672532571792821, 15.36912611011920582 ) ) ;
#91014=CARTESIAN_POINT ( 'NONE',  ( 7.681258945454893382E-14, -1.200000000000000030E-05, 39.50000000000000000 ) ) ;
#91043=( GEOMETRIC_REPRESENTATION_CONTEXT ( 3 ) GLOBAL_UNCERTAINTY_ASSIGNED_CONTEXT ( ( #35425 ) ) GLOBAL_UNIT_ASSIGNED_CONTEXT ( ( #73187, #81809, #101217 ) ) REPRESENTATION_CONTEXT ( 'NONE', 'WORKASPACE' ) );
#91055=CARTESIAN_POINT ( 'NONE',  ( 22.45459161911025348, 27.61281158839761574, -32.95901622140775089 ) ) ;
#91059=EDGE_CURVE ( 'NONE', #34601, #5811, #5079, .T. ) ;
#91060=DIRECTION ( 'NONE',  ( 0.000000000000000000, 0.000000000000000000, 1.000000000000000000 ) ) ;
#91063=CARTESIAN_POINT ( 'NONE',  ( -22.25750210340301649, 26.06517743502978846, 31.15121832242501299 ) ) ;
#91065=B_SPLINE_CURVE_WITH_KNOTS ( 'NONE', 3,
 ( #83035, #1558, #35047, #19415, #52249, #85159, #100798, #26958, #25359, #92712, #99744, #17782, #9126, #68455, #34523, #74918, #59840, #1002 ),
 .UNSPECIFIED., .F., .F.,
 ( 4, 2, 2, 2, 2, 2, 2, 2, 4 ),
 ( 0.007258363042094923348, 0.007762330413277810856, 0.008266297784460696629, 0.008770265155643584137, 0.009274232526826471645, 0.009778199898009359153, 0.01028216726919224666, 0.01078613464037513243, 0.01129010201155801994 ),
 .UNSPECIFIED. ) ;
#91074=LINE ( 'NONE', #82430, #17439 ) ;
#91078=ORIENTED_EDGE ( 'NONE', *, *, #65697, .T. ) ;
#91079=CARTESIAN_POINT ( 'NONE',  ( 4.142849616820252293E-15, 27.68727484027578356, 33.82893434829263413 ) ) ;
#91080=EDGE_CURVE ( 'NONE', #5811, #84521, #93062, .T. ) ;
#91086=STYLED_ITEM ( 'NONE', ( #88794 ), #40131 ) ;
#91089=CARTESIAN_POINT ( 'NONE',  ( -16.64348903516517098, 45.60392139269950462, 6.657797401561654560 ) ) ;
#91095=CARTESIAN_POINT ( 'NONE',  ( 15.65186372275026017, 46.18633577147563329, 4.642160826816592589 ) ) ;
#91098=SURFACE_SIDE_STYLE ('',( #2589 ) ) ;
#91116=AXIS2_PLACEMENT_3D ( 'NONE', #8836, #41741, #705 ) ;
#91119=CARTESIAN_POINT ( 'NONE',  ( -16.96405139844710064, 43.37130063886583997, 6.627052614058375646 ) ) ;
#91163=CARTESIAN_POINT ( 'NONE',  ( -37.72544201219972848, 25.42175550654698313, -13.45617127781035016 ) ) ;
#91169=STYLED_ITEM ( 'NONE', ( #35305 ), #102736 ) ;
#91179=FACE_OUTER_BOUND ( 'NONE', #103160, .T. ) ;
#91189=EDGE_CURVE ( 'NONE', #17567, #41746, #20250, .T. ) ;
#91191=PRESENTATION_STYLE_ASSIGNMENT (( #58266 ) ) ;
#91204=CARTESIAN_POINT ( 'NONE',  ( -4.044114467841184890, 52.00960197897231296, 7.152013030799439619 ) ) ;
#91211=CARTESIAN_POINT ( 'NONE',  ( 28.45521705596386397, 17.07436234393351171, -41.11936415921402954 ) ) ;
#91279=EDGE_CURVE ( 'NONE', #22572, #54691, #102308, .T. ) ;
#91280=SURFACE_STYLE_FILL_AREA ( #18461 ) ;
#91282=VERTEX_POINT ( 'NONE', #80009 ) ;
#91297=FILL_AREA_STYLE ('',( #50797 ) ) ;
#91300=CARTESIAN_POINT ( 'NONE',  ( -0.5272038479004254041, 18.60450536692893664, -49.36031152383475273 ) ) ;
#91315=CARTESIAN_POINT ( 'NONE',  ( 0.000000000000000000, 38.19193163660327173, 0.000000000000000000 ) ) ;
#91321=CARTESIAN_POINT ( 'NONE',  ( 1.012463078293192487, 43.34708279331648839, 18.25106663962358411 ) ) ;
#91329=FILL_AREA_STYLE ('',( #34169 ) ) ;
#91334=FACE_BOUND ( 'NONE', #54211, .T. ) ;
#91335=FILL_AREA_STYLE ('',( #42763 ) ) ;
#91347=ADVANCED_FACE ( 'NONE', ( #63857 ), #96747, .F. ) ;
#91350=CARTESIAN_POINT ( 'NONE',  ( -15.57484877165060944, 43.91708715447281008, 6.061292577738371712 ) ) ;
#91355=CARTESIAN_POINT ( 'NONE',  ( -22.00868112945024535, 27.89883671455867287, 32.31191507115328676 ) ) ;
#91374=FACE_OUTER_BOUND ( 'NONE', #49432, .T. ) ;
#91384=CARTESIAN_POINT ( 'NONE',  ( -1.159861628855096694, 17.01140986925715026, 50.01797968613450251 ) ) ;
#91394=CARTESIAN_POINT ( 'NONE',  ( 0.9986626498655565287, 14.07191026904348874, -51.25503100627838649 ) ) ;
#91400=CARTESIAN_POINT ( 'NONE',  ( -47.07350275986928523, 18.64911821952795279, -14.79681583022523128 ) ) ;
#91404=CARTESIAN_POINT ( 'NONE',  ( 0.000000000000000000, 45.89575828009193259, -11.27631144943088337 ) ) ;
#91423=VERTEX_POINT ( 'NONE', #51889 ) ;
#91459=CARTESIAN_POINT ( 'NONE',  ( -0.1690119616668960822, 43.17849121649364719, 18.74136049120801673 ) ) ;
#91460=SURFACE_STYLE_USAGE ( .BOTH. , #25145 ) ;
#91463=CARTESIAN_POINT ( 'NONE',  ( 0.7832924031922618990, 46.11172308909048922, -16.51234007558469230 ) ) ;
#91475=CARTESIAN_POINT ( 'NONE',  ( 26.12439441013744101, 34.87005242119162318, 9.598401274034952024 ) ) ;
#91477=CARTESIAN_POINT ( 'NONE',  ( 15.64300095959876202, 35.03905011530154212, 22.45650292849707341 ) ) ;
#91488=SURFACE_SIDE_STYLE ('',( #25174 ) ) ;
#91496=EDGE_CURVE ( 'NONE', #95805, #88641, #79194, .T. ) ;
#91515=CARTESIAN_POINT ( 'NONE',  ( 7.312892434773027972, 54.25556936841643818, 2.973951097466557059 ) ) ;
#91526=CARTESIAN_POINT ( 'NONE',  ( 23.84269658596081243, 25.80551286858905868, -30.86189937676715545 ) ) ;
#91531=EDGE_CURVE ( 'NONE', #68832, #87776, #65504, .T. ) ;
#91535=CARTESIAN_POINT ( 'NONE',  ( -47.24099558602559057, 11.75653836616713299, -16.58383527959137638 ) ) ;
#91541=FACE_OUTER_BOUND ( 'NONE', #71152, .T. ) ;
#91565=DIRECTION ( 'NONE',  ( 0.000000000000000000, 0.000000000000000000, 1.000000000000000000 ) ) ;
#91576=CARTESIAN_POINT ( 'NONE',  ( -16.75187969033532553, -1.200000000000000030E-05, 23.05698433968612093 ) ) ;
#91580=CARTESIAN_POINT ( 'NONE',  ( 23.21751746555220564, 28.11705169068991950, -30.70617127781077116 ) ) ;
#91586=CARTESIAN_POINT ( 'NONE',  ( -29.59455828143376266, 18.41848238274119609, 39.60535821593508388 ) ) ;
#91592=ORIENTED_EDGE ( 'NONE', *, *, #76989, .F. ) ;
#91602=ADVANCED_FACE ( 'NONE', ( #29789, #93968, #69170, #54007, #95551 ), #75809, .F. ) ;
#91612=CARTESIAN_POINT ( 'NONE',  ( -8.559508646656370345, 53.68473964988125857, -4.031152949374577688 ) ) ;
#91615=CARTESIAN_POINT ( 'NONE',  ( -17.84510959215117509, 45.37789619860912893, 5.053583809357591328 ) ) ;
#91616=ORIENTED_EDGE ( 'NONE', *, *, #3822, .F. ) ;
#91622=CARTESIAN_POINT ( 'NONE',  ( 15.43372845131084858, 46.13227632078331197, 5.762758105581649026 ) ) ;
#91633=FILL_AREA_STYLE_COLOUR ( '', #103337 ) ;
#91641=CARTESIAN_POINT ( 'NONE',  ( -17.51143763087804572, 34.75099232332586041, -22.05163403062407923 ) ) ;
#91653=VERTEX_POINT ( 'NONE', #44896 ) ;
#91656=CARTESIAN_POINT ( 'NONE',  ( 9.685714585015881894, 51.27227691868331760, 3.330047012961471431 ) ) ;
#91667=CARTESIAN_POINT ( 'NONE',  ( -17.77056504783044844, 43.17862847894689793, -5.954854177184050634 ) ) ;
#91681=CARTESIAN_POINT ( 'NONE',  ( -37.88755491168825529, 25.36998983636258131, -13.42507852288176728 ) ) ;
#91716=VECTOR ( 'NONE', #15022, 1000.000000000000000 ) ;
#91717=CARTESIAN_POINT ( 'NONE',  ( 4.206664005177994881, 53.86290224764378820, 7.924430552076916712 ) ) ;
#91722=AXIS2_PLACEMENT_3D ( 'NONE', #80617, #64979, #6738 ) ;
#91724=EDGE_CURVE ( 'NONE', #60190, #44416, #87998, .T. ) ;
#91728=CARTESIAN_POINT ( 'NONE',  ( 30.93381850223209639, 8.838939540955992769, -40.91347331214265637 ) ) ;
#91749=AXIS2_PLACEMENT_3D ( 'NONE', #84239, #10333, #2774 ) ;
#91759=ORIENTED_EDGE ( 'NONE', *, *, #5809, .T. ) ;
#91786=EDGE_CURVE ( 'NONE', #56342, #27639, #79882, .T. ) ;
#91797=CARTESIAN_POINT ( 'NONE',  ( 17.85737165039480701, 45.30383319674706399, 5.717692534355065526 ) ) ;
#91800=COLOUR_RGB ( '', 0.72549020, 0.75294118, 0.79215686) ;
#91801=( NAMED_UNIT ( * ) PLANE_ANGLE_UNIT ( ) SI_UNIT ( $, .RADIAN. ) );
#91805=EDGE_LOOP ( 'NONE', ( #51702, #11651 ) ) ;
#91806=CARTESIAN_POINT ( 'NONE',  ( 26.78640155871314832, 36.71834478141271774, -10.02603228771729427 ) ) ;
#91814=EDGE_CURVE ( 'NONE', #39760, #79581, #73369, .T. ) ;
#91815=SURFACE_STYLE_FILL_AREA ( #60004 ) ;
#91821=ORIENTED_EDGE ( 'NONE', *, *, #9154, .T. ) ;
#91835=CARTESIAN_POINT ( 'NONE',  ( 8.559508646656398767, 51.83514083332404709, 1.531152949374243510 ) ) ;
#91838=EDGE_LOOP ( 'NONE', ( #28571, #64987, #37474, #36621 ) ) ;
#91847=SURFACE_STYLE_FILL_AREA ( #59495 ) ;
#91858=ADVANCED_FACE ( 'NONE', ( #71784 ), #15152, .F. ) ;
#91866=CARTESIAN_POINT ( 'NONE',  ( -16.64348903516517098, 43.75610143575153899, 4.157797401561652784 ) ) ;
#91870=CARTESIAN_POINT ( 'NONE',  ( -22.43826451848009995, 28.20713089197012735, 30.97515248374616448 ) ) ;
#91872=CYLINDRICAL_SURFACE ( 'NONE', #44584, 1.250000000000001110 ) ;
#91890=FILL_AREA_STYLE ('',( #59002 ) ) ;
#91902=CARTESIAN_POINT ( 'NONE',  ( -1.250906133227802419, 15.60029824371900276, 50.60801902191838053 ) ) ;
#91913=CARTESIAN_POINT ( 'NONE',  ( -10.28624191511820207, 45.38549880562041494, 15.40779740156164124 ) ) ;
#91920=LINE ( 'NONE', #92435, #12579 ) ;
#91933=CARTESIAN_POINT ( 'NONE',  ( 9.324240130834043683, 51.33788018723820556, -3.783820555081815140 ) ) ;
#91950=CARTESIAN_POINT ( 'NONE',  ( -36.35334569080745126, 28.20664209161598635, -11.89422708507966497 ) ) ;
#91964=CARTESIAN_POINT ( 'NONE',  ( 1.167959526168962814, 9.592220699621755386, 50.96201451364633783 ) ) ;
#91968=EDGE_LOOP ( 'NONE', ( #73483, #10272, #47997, #40967 ) ) ;
#91972=CARTESIAN_POINT ( 'NONE',  ( 10.28624191511840458, -1.200000000000000030E-05, 15.40779740156149202 ) ) ;
#91981=CYLINDRICAL_SURFACE ( 'NONE', #29186, 1.250000000000001110 ) ;
#91987=ORIENTED_EDGE ( 'NONE', *, *, #85967, .T. ) ;
#92052=CARTESIAN_POINT ( 'NONE',  ( -37.02112216959907443, 25.93502769547995257, -11.07860630295547999 ) ) ;
#92066=ADVANCED_FACE ( 'NONE', ( #49639 ), #35089, .F. ) ;
#92067=B_SPLINE_CURVE_WITH_KNOTS ( 'NONE', 3,
 ( #70199, #20651, #100967, #44337, #92872, #37341, #36288, #68631, #43794, #85880, #103106, #11950, #21167, #29256, #61060, #53994, #10876, #84795 ),
 .UNSPECIFIED., .F., .F.,
 ( 4, 2, 2, 2, 2, 2, 2, 2, 4 ),
 ( 0.003784215161170911314, 0.004287519624513744590, 0.004790824087856576999, 0.005042476319527991468, 0.005294128551199405938, 0.005797433014542233143, 0.006300737477885061215, 0.006804041941227888420, 0.007810650867913536757 ),
 .UNSPECIFIED. ) ;
#92079=COLOUR_RGB ( '', 0.09019608, 0.27058824, 0.51372549) ;
#92085=LINE ( 'NONE', #66215, #40052 ) ;
#92086=CARTESIAN_POINT ( 'NONE',  ( 15.90780724146583580, 35.07994696358735354, -22.13120237605230045 ) ) ;
#92090=CARTESIAN_POINT ( 'NONE',  ( 22.37422507490784795, 28.20471669103548606, -31.02961587878864336 ) ) ;
#92095=CARTESIAN_POINT ( 'NONE',  ( -29.35793203618277047, 13.99620286145419179, 42.06478814971824676 ) ) ;
#92155=CARTESIAN_POINT ( 'NONE',  ( -6.400715382019204647, 51.30587535467638816, -7.878101082919672926 ) ) ;
#92161=CARTESIAN_POINT ( 'NONE',  ( -0.1682998283258651528, 37.21016666119768246, 27.25000000000001421 ) ) ;
#92163=ORIENTED_EDGE ( 'NONE', *, *, #79519, .F. ) ;
#92176=CARTESIAN_POINT ( 'NONE',  ( -24.20451479021888730, 25.63535626674006451, -31.17289312728862782 ) ) ;
#92203=MECHANICAL_DESIGN_GEOMETRIC_PRESENTATION_REPRESENTATION('',(#9518),#50848);
#92210=FACE_OUTER_BOUND ( 'NONE', #4120, .T. ) ;
#92216=CARTESIAN_POINT ( 'NONE',  ( -8.559508646656370345, -1.200000000000000030E-05, 1.531152949374564365 ) ) ;
#92221=CARTESIAN_POINT ( 'NONE',  ( 5.523799489093670250E-15, 23.58303312036771615, 45.10524579772351217 ) ) ;
#92225=CARTESIAN_POINT ( 'NONE',  ( 27.71645771920791645, 36.65781692560624805, 7.705275282087030497 ) ) ;
#92240=ORIENTED_EDGE ( 'NONE', *, *, #44725, .T. ) ;
#92253=CARTESIAN_POINT ( 'NONE',  ( -0.1694193870205596697, 54.30391592751540486, 7.758667673557112288 ) ) ;
#92257=EDGE_CURVE ( 'NONE', #35979, #54576, #40796, .T. ) ;
#92274=CARTESIAN_POINT ( 'NONE',  ( 36.94571008616465235, 25.95814344041297517, -11.10931082871520026 ) ) ;
#92276=CARTESIAN_POINT ( 'NONE',  ( -1.218835986930302706, 36.86216219021419960, -28.17983935174571641 ) ) ;
#92290=CARTESIAN_POINT ( 'NONE',  ( -0.8415904055670518913, 45.41420510540432787, 18.42786602808935470 ) ) ;
#92314=ORIENTED_EDGE ( 'NONE', *, *, #77802, .T. ) ;
#92322=ADVANCED_FACE ( 'NONE', ( #828, #33797, #102231, #26790, #19774 ), #10514, .F. ) ;
#92324=B_SPLINE_CURVE_WITH_KNOTS ( 'NONE', 3,
 ( #390, #59217, #18236, #92095, #40896, #99658, #65708, #25272, #17695, #74314, #82417, #81332, #82949, #73780, #66225, #106681, #24213, #40358, #17168, #33897, #90507, #65167, #66770, #81859, #32828, #9044, #33357, #98062, #91586, #1477 ),
 .UNSPECIFIED., .F., .F.,
 ( 4, 2, 2, 2, 2, 2, 2, 2, 2, 2, 2, 2, 2, 2, 4 ),
 ( 0.0006904739626665865699, 0.001153765004792748619, 0.001617056046918910776, 0.002543638131171222297, 0.003470220215423534468, 0.004396802299675845772, 0.005323384383928157944, 0.005786675426054318366, 0.006249966468180478789, 0.006713257510306639211, 0.006944903031369712050, 0.007176548552432786623, 0.007408194073495859462, 0.007639839594558934036, 0.008103130636685088387 ),
 .UNSPECIFIED. ) ;
#92325=CARTESIAN_POINT ( 'NONE',  ( 30.82780881727078182, 15.25261229662383933, -40.33825946679404240 ) ) ;
#92349=VECTOR ( 'NONE', #79072, 1000.000000000000114 ) ;
#92350=ORIENTED_EDGE ( 'NONE', *, *, #68390, .T. ) ;
#92351=CARTESIAN_POINT ( 'NONE',  ( 1.250539423207229994, 43.55815149200913083, 17.65460189445720474 ) ) ;
#92364=PRESENTATION_STYLE_ASSIGNMENT (( #9848 ) ) ;
#92366=CIRCLE ( 'NONE', #66508, 46.61112130868859538 ) ;
#92369=CIRCLE ( 'NONE', #80279, 13.27631144943088515 ) ;
#92372=CARTESIAN_POINT ( 'NONE',  ( 9.176927881262047393, 44.04115577556814287, -13.55866590325632970 ) ) ;
#92375=CYLINDRICAL_SURFACE ( 'NONE', #50424, 1.250000000000001110 ) ;
#92392=VERTEX_POINT ( 'NONE', #95216 ) ;
#92404=DIRECTION ( 'NONE',  ( 0.000000000000000000, 1.000000000000000000, -0.000000000000000000 ) ) ;
#92405=CARTESIAN_POINT ( 'NONE',  ( 47.01788285976068238, 17.61616053603655629, -16.34433538609931347 ) ) ;
#92406=CARTESIAN_POINT ( 'NONE',  ( -11.12940285222375891, 43.17715607477184392, 15.08446948163250845 ) ) ;
#92421=CARTESIAN_POINT ( 'NONE',  ( -26.48777125522224551, 34.95844695497470411, -7.716963249296902028 ) ) ;
#92435=CARTESIAN_POINT ( 'NONE',  ( 0.000000000000000000, 55.00000000000000000, 0.000000000000000000 ) ) ;
#92447=CARTESIAN_POINT ( 'NONE',  ( -17.31689591039211251, 34.17651138339384431, 24.17515860248506598 ) ) ;
#92452=CARTESIAN_POINT ( 'NONE',  ( -29.68315524076956891, -1.200000000000000030E-05, 39.60535821593508388 ) ) ;
#92474=CARTESIAN_POINT ( 'NONE',  ( 5.455839282392823009, 51.31686971843895861, -8.522937042329454371 ) ) ;
#92479=EDGE_CURVE ( 'NONE', #104058, #89914, #66193, .T. ) ;
#92480=( NAMED_UNIT ( * ) SI_UNIT ( $, .STERADIAN. ) SOLID_ANGLE_UNIT ( ) );
#92489=CARTESIAN_POINT ( 'NONE',  ( 1.115771448223378925, 9.312113948361041338, 51.08078732034569924 ) ) ;
#92503=PRESENTATION_STYLE_ASSIGNMENT (( #26757 ) ) ;
#92513=CARTESIAN_POINT ( 'NONE',  ( -7.797782256654760324, 54.21795136539236637, 1.776235144415082567 ) ) ;
#92539=DIRECTION ( 'NONE',  ( 0.000000000000000000, 0.000000000000000000, -1.000000000000000000 ) ) ;
#92544=EDGE_CURVE ( 'NONE', #46516, #46768, #8301, .T. ) ;
#92549=DIRECTION ( 'NONE',  ( 0.000000000000000000, 0.000000000000000000, 1.000000000000000000 ) ) ;
#92561=CARTESIAN_POINT ( 'NONE',  ( 7.370192266679785220, 54.30878245688016648, 2.387241612175243333 ) ) ;
#92578=EDGE_LOOP ( 'NONE', ( #89823, #100003 ) ) ;
#92579=CARTESIAN_POINT ( 'NONE',  ( -47.55322331356164511, 10.90908589463665734, -16.76771630193830376 ) ) ;
#92582=CARTESIAN_POINT ( 'NONE',  ( -37.56673239365863282, 25.75719283951018568, -10.95617127781023648 ) ) ;
#92596=CARTESIAN_POINT ( 'NONE',  ( 28.61418328824293766, 13.49088233573899487, -40.19504096224954992 ) ) ;
#92639=ORIENTED_EDGE ( 'NONE', *, *, #91531, .F. ) ;
#92668=CARTESIAN_POINT ( 'NONE',  ( 16.64348903516523848, 45.88445698070336221, 4.157797401561420081 ) ) ;
#92671=DIRECTION ( 'NONE',  ( 0.000000000000000000, 0.000000000000000000, 1.000000000000000000 ) ) ;
#92681=PRESENTATION_STYLE_ASSIGNMENT (( #43599 ) ) ;
#92687=DIRECTION ( 'NONE',  ( 0.000000000000000000, 0.000000000000000000, -1.000000000000000000 ) ) ;
#92712=CARTESIAN_POINT ( 'NONE',  ( -1.249368327036161963, 45.80196013925338860, -17.33667219389016978 ) ) ;
#92720=VERTEX_POINT ( 'NONE', #61126 ) ;
#92724=EDGE_LOOP ( 'NONE', ( #16575, #58278, #52705, #70668 ) ) ;
#92725=CARTESIAN_POINT ( 'NONE',  ( -4.297323614437654093, 53.80478256577427487, 8.057193928358454826 ) ) ;
#92732=ADVANCED_FACE ( 'NONE', ( #43865, #69228, #53027, #28256, #36359 ), #96608, .T. ) ;
#92737=EDGE_LOOP ( 'NONE', ( #5370, #39961 ) ) ;
#92741=CARTESIAN_POINT ( 'NONE',  ( 10.28624191511773844, 43.25714326066793092, -15.40779740156427202 ) ) ;
#92748=EDGE_CURVE ( 'NONE', #96544, #74990, #84862, .T. ) ;
#92761=ORIENTED_EDGE ( 'NONE', *, *, #20083, .T. ) ;
#92768=EDGE_CURVE ( 'NONE', #45425, #347, #19827, .T. ) ;
#92808=LINE ( 'NONE', #52342, #65915 ) ;
#92812=CARTESIAN_POINT ( 'NONE',  ( -6.518108746679445176, 51.36497237057859166, 7.568279843509460925 ) ) ;
#92815=VERTEX_POINT ( 'NONE', #29318 ) ;
#92821=CARTESIAN_POINT ( 'NONE',  ( -1.220317183347022771, 36.63139401606524359, -28.81440893545308768 ) ) ;
#92824=DIRECTION ( 'NONE',  ( -0.000000000000000000, 1.000000000000000000, -0.000000000000000000 ) ) ;
#92833=ORIENTED_EDGE ( 'NONE', *, *, #106174, .T. ) ;
#92835=CARTESIAN_POINT ( 'NONE',  ( 0.000000000000000000, 0.000000000000000000, 0.000000000000000000 ) ) ;
#92837=CARTESIAN_POINT ( 'NONE',  ( -48.90253429252444306, 9.379793601652298918, -14.70143532337769088 ) ) ;
#92842=LINE ( 'NONE', #60510, #20796 ) ;
#92859=CARTESIAN_POINT ( 'NONE',  ( 30.90663305326217980, 14.69720259819713171, -40.57123681776414514 ) ) ;
#92861=DIRECTION ( 'NONE',  ( 0.000000000000000000, 0.000000000000000000, 1.000000000000000000 ) ) ;
#92869=CARTESIAN_POINT ( 'NONE',  ( 38.54613318107097797, 27.49665781920858265, -11.41323020553166856 ) ) ;
#92872=CARTESIAN_POINT ( 'NONE',  ( 17.40520516324947309, 43.24891479535327932, 6.413032873378024412 ) ) ;
#92897=CARTESIAN_POINT ( 'NONE',  ( -7.576492623273555438, 51.95166532205756482, -3.569847711208139707 ) ) ;
#92901=CARTESIAN_POINT ( 'NONE',  ( -1.115712391155330829, 9.312447554110960368, -51.08064749475159516 ) ) ;
#92903=CARTESIAN_POINT ( 'NONE',  ( 36.35697729507720766, 25.99969806902772262, 12.56106323611688502 ) ) ;
#92914=ADVANCED_FACE ( 'NONE', ( #71846 ), #70801, .T. ) ;
#92931=ORIENTED_EDGE ( 'NONE', *, *, #82009, .F. ) ;
#92936=CARTESIAN_POINT ( 'NONE',  ( 7.806021097029844036, 51.84152802710514862, -3.791216216185762988 ) ) ;
#92941=EDGE_LOOP ( 'NONE', ( #1286, #6955 ) ) ;
#92947=CARTESIAN_POINT ( 'NONE',  ( -11.39536947849075688, 43.21380559344856920, 14.75801218667085912 ) ) ;
#92956=( NAMED_UNIT ( * ) PLANE_ANGLE_UNIT ( ) SI_UNIT ( $, .RADIAN. ) );
#92958=VECTOR ( 'NONE', #55192, 1000.000000000000114 ) ;
#92970=B_SPLINE_CURVE_WITH_KNOTS ( 'NONE', 3,
 ( #3374, #10382, #77796, #3907, #36839, #101537, #11438, #52435, #77261, #19068, #51909, #92901, #1754, #100996, #76183, #43299, #50834, #84822, #10902, #34711, #43821, #75652, #2282, #26623, #36317, #93456, #69706, #2824 ),
 .UNSPECIFIED., .F., .F.,
 ( 4, 2, 2, 2, 2, 2, 2, 2, 2, 2, 2, 2, 2, 4 ),
 ( 0.01419955293336414015, 0.01443026280088062670, 0.01466097266839711498, 0.01512239240343009848, 0.01558381213846308198, 0.01604523187349606722, 0.01696807134356204116, 0.01789091081362801858, 0.01881375028369399252, 0.01973658975375996993, 0.02019800948879296038, 0.02065942922382595082, 0.02112084895885894473, 0.02158226869389193517 ),
 .UNSPECIFIED. ) ;
#92977=DIRECTION ( 'NONE',  ( 0.000000000000000000, 0.000000000000000000, 1.000000000000000000 ) ) ;
#92982=B_SPLINE_CURVE_WITH_KNOTS ( 'NONE', 3,
 ( #52074, #37004, #84989, #28380, #87125, #2459, #13202, #68822, #20844, #93619, #53159, #45606, #61255, #94141, #35950, #12673, #60211, #43996, #20311, #4607 ),
 .UNSPECIFIED., .F., .F.,
 ( 4, 2, 2, 2, 2, 2, 2, 2, 2, 4 ),
 ( 0.007651485924207266677, 0.008155685132977938748, 0.008659884341748609951, 0.009164083550519281154, 0.009668282759289954092, 0.01017248196806062877, 0.01067668117683130344, 0.01092878078121663904, 0.01118088038560197638, 0.01168507959437264758 ),
 .UNSPECIFIED. ) ;
#92991=CARTESIAN_POINT ( 'NONE',  ( 16.64348903516512834, 45.88445698070336931, -4.157797401561768247 ) ) ;
#93015=CARTESIAN_POINT ( 'NONE',  ( -29.68315524077005207, 13.47185074185902209, -42.10535821593474282 ) ) ;
#93016=EDGE_CURVE ( 'NONE', #20894, #34743, #85292, .T. ) ;
#93017=CARTESIAN_POINT ( 'NONE',  ( 48.69302668856813909, 13.59112006857157162, -16.66703530934498900 ) ) ;
#93031=CARTESIAN_POINT ( 'NONE',  ( 1.248957290998449210, 10.99524951701871878, 50.37123180686704416 ) ) ;
#93037=CARTESIAN_POINT ( 'NONE',  ( 38.17883673876440298, 25.52816737538899261, -11.10479361635789175 ) ) ;
#93044=LINE ( 'NONE', #86039, #73577 ) ;
#93047=FILL_AREA_STYLE ('',( #18658 ) ) ;
#93062=CIRCLE ( 'NONE', #67204, 33.82893434829264123 ) ;
#93066=CARTESIAN_POINT ( 'NONE',  ( 9.365057959178315627, 53.65588038361938317, -1.821971454984222083 ) ) ;
#93071=CARTESIAN_POINT ( 'NONE',  ( 5.749654562269868196E-15, 24.35682532067546902, 46.94949242731048145 ) ) ;
#93087=FILL_AREA_STYLE_COLOUR ( '', #44566 ) ;
#93102=CARTESIAN_POINT ( 'NONE',  ( 37.56673239365841255, -1.200000000000000030E-05, -10.95617127781092037 ) ) ;
#93138=CARTESIAN_POINT ( 'NONE',  ( 17.71915776462823189, 45.45154592806376570, -4.750161495150260649 ) ) ;
#93150=( GEOMETRIC_REPRESENTATION_CONTEXT ( 3 ) GLOBAL_UNCERTAINTY_ASSIGNED_CONTEXT ( ( #40961 ) ) GLOBAL_UNIT_ASSIGNED_CONTEXT ( ( #24862, #41553, #43678 ) ) REPRESENTATION_CONTEXT ( 'NONE', 'WORKASPACE' ) );
#93155=CARTESIAN_POINT ( 'NONE',  ( 3.006829104376305816E-15, 43.19193163660326462, 24.55262289886175964 ) ) ;
#93159=SURFACE_STYLE_USAGE ( .BOTH. , #27411 ) ;
#93160=CARTESIAN_POINT ( 'NONE',  ( -8.559508646656389885, -1.200000000000000030E-05, -2.781152949374503081 ) ) ;
#93162=SURFACE_SIDE_STYLE ('',( #10108 ) ) ;
#93170=FACE_OUTER_BOUND ( 'NONE', #83149, .T. ) ;
#93177=COLOUR_RGB ( '', 0.40784314, 0.44705882, 0.49803922) ;
#93185=CARTESIAN_POINT ( 'NONE',  ( 1.005921156701460539, 36.47725511815836796, -29.24640024088538581 ) ) ;
#93186=VERTEX_POINT ( 'NONE', #40419 ) ;
#93200=ORIENTED_EDGE ( 'NONE', *, *, #74556, .F. ) ;
#93214=FACE_BOUND ( 'NONE', #79604, .T. ) ;
#93255=CARTESIAN_POINT ( 'NONE',  ( -24.23034962376434365, 25.18874428018206046, -32.69349392899435713 ) ) ;
#93261=EDGE_CURVE ( 'NONE', #11951, #15047, #97058, .T. ) ;
#93263=CARTESIAN_POINT ( 'NONE',  ( 0.4142141812692001213, 37.18443326924929693, 27.31766813022851181 ) ) ;
#93264=CARTESIAN_POINT ( 'NONE',  ( 15.76193534935208262, 36.72733462479577327, -23.83658602074658717 ) ) ;
#93267=ORIENTED_EDGE ( 'NONE', *, *, #53498, .F. ) ;
#93283=CARTESIAN_POINT ( 'NONE',  ( -15.39205472978310141, 46.19766366449148620, 5.347876573122078980 ) ) ;
#93296=EDGE_CURVE ( 'NONE', #31195, #86477, #8044, .T. ) ;
#93319=FILL_AREA_STYLE_COLOUR ( '', #51085 ) ;
#93327=( NAMED_UNIT ( * ) SI_UNIT ( $, .STERADIAN. ) SOLID_ANGLE_UNIT ( ) );
#93331=CONICAL_SURFACE ( 'NONE', #74145, 11.96035173608223090, 1.221730476396025722 ) ;
#93343=DIRECTION ( 'NONE',  ( 0.000000000000000000, 0.000000000000000000, 1.000000000000000000 ) ) ;
#93347=CARTESIAN_POINT ( 'NONE',  ( 23.38389609179547435, 28.08052868592283957, 30.70617127781017075 ) ) ;
#93360=CARTESIAN_POINT ( 'NONE',  ( -6.529218958540401907, 51.53898023814725349, 6.916366082103534652 ) ) ;
#93367=CARTESIAN_POINT ( 'NONE',  ( -0.08443874956765938522, 37.21016666119768246, -27.25000000000001066 ) ) ;
#93368=CARTESIAN_POINT ( 'NONE',  ( 2.848917157793759055E-13, 44.08548369317517768, 16.24999999999732836 ) ) ;
#93374=EDGE_CURVE ( 'NONE', #103131, #30746, #94270, .T. ) ;
#93375=UNCERTAINTY_MEASURE_WITH_UNIT (LENGTH_MEASURE( 1.000000000000000082E-05 ), #93969, 'distance_accuracy_value', 'NONE');
#93382=CARTESIAN_POINT ( 'NONE',  ( -1.220105902931785113, 45.62896107045330041, 17.81534086607498324 ) ) ;
#93383=COLOUR_RGB ( '', 0.66274510, 0.83137255, 0.94901961) ;
#93389=CARTESIAN_POINT ( 'NONE',  ( 23.21751746555220564, -1.200000000000000030E-05, -30.70617127781077116 ) ) ;
#93419=CARTESIAN_POINT ( 'NONE',  ( -46.79638705082423655, 18.85256363620330333, 15.38003188690398204 ) ) ;
#93422=AXIS2_PLACEMENT_3D ( 'NONE', #11139, #3072, #91565 ) ;
#93424=CARTESIAN_POINT ( 'NONE',  ( 0.9433768135827877988, 17.83653422148033485, 49.67628854547170647 ) ) ;
#93434=DIRECTION ( 'NONE',  ( 0.000000000000000000, -0.3420201433256733758, -0.9396926207859066515 ) ) ;
#93442=ORIENTED_EDGE ( 'NONE', *, *, #99094, .T. ) ;
#93456=CARTESIAN_POINT ( 'NONE',  ( -0.3043501477677958422, 13.62703061655916947, -49.28168406113174171 ) ) ;
#93458=CARTESIAN_POINT ( 'NONE',  ( -17.86210361494380905, 36.33998000098822700, 23.65466217301429452 ) ) ;
#93496=( GEOMETRIC_REPRESENTATION_CONTEXT ( 3 ) GLOBAL_UNCERTAINTY_ASSIGNED_CONTEXT ( ( #84479 ) ) GLOBAL_UNIT_ASSIGNED_CONTEXT ( ( #77512, #12225, #37085 ) ) REPRESENTATION_CONTEXT ( 'NONE', 'WORKASPACE' ) );
#93499=CARTESIAN_POINT ( 'NONE',  ( -10.92659744279963441, 43.17638622626457590, 15.23462367102720805 ) ) ;
#93501=CARTESIAN_POINT ( 'NONE',  ( -49.27914886956171614, 13.08292563505592376, 15.56788460764650317 ) ) ;
#93504=DIRECTION ( 'NONE',  ( -0.000000000000000000, 1.000000000000000000, -0.000000000000000000 ) ) ;
#93511=CARTESIAN_POINT ( 'NONE',  ( 4.958567106242401934, 52.14947999179454996, -6.064245278518590965 ) ) ;
#93525=FILL_AREA_STYLE ('',( #12051 ) ) ;
#93526=CARTESIAN_POINT ( 'NONE',  ( -5.290067270632282437, 54.20842449845790867, 6.031152949371105798 ) ) ;
#93529=CARTESIAN_POINT ( 'NONE',  ( -47.44667293595283297, 16.35698112199736443, -16.71846647949800513 ) ) ;
#93534=( NAMED_UNIT ( * ) SI_UNIT ( $, .STERADIAN. ) SOLID_ANGLE_UNIT ( ) );
#93541=CARTESIAN_POINT ( 'NONE',  ( -17.08484820656748226, 34.19635467231778136, 24.27347930919938435 ) ) ;
#93548=CARTESIAN_POINT ( 'NONE',  ( 6.388342523666968198, 51.65549266189224653, 6.605009197188880243 ) ) ;
#93556=EDGE_LOOP ( 'NONE', ( #52862, #16445, #55721, #103472, #517, #105433, #83040, #38345 ) ) ;
#93559=CARTESIAN_POINT ( 'NONE',  ( -36.95430024838550764, 27.83259845835024393, -13.30727799284015411 ) ) ;
#93570=ORIENTED_EDGE ( 'NONE', *, *, #11769, .F. ) ;
#93588=LINE ( 'NONE', #60184, #95276 ) ;
#93600=CARTESIAN_POINT ( 'NONE',  ( 0.8395943188471228780, 28.08659877555713180, 38.57031298532696439 ) ) ;
#93618=UNCERTAINTY_MEASURE_WITH_UNIT (LENGTH_MEASURE( 1.000000000000000082E-05 ), #68278, 'distance_accuracy_value', 'NONE');
#93619=CARTESIAN_POINT ( 'NONE',  ( 4.036442205379928261, 54.13912236062702732, -7.152865674426393205 ) ) ;
#93622=EDGE_LOOP ( 'NONE', ( #97335, #17648, #23382, #97722 ) ) ;
#93640=DIRECTION ( 'NONE',  ( 0.000000000000000000, 1.000000000000000000, -0.000000000000000000 ) ) ;
#93652=VECTOR ( 'NONE', #27441, 1000.000000000000000 ) ;
#93663=CARTESIAN_POINT ( 'NONE',  ( -16.95986460590401634, 43.64169184087446496, -4.188100785892593159 ) ) ;
#93677=CARTESIAN_POINT ( 'NONE',  ( 29.49710045460141927, 13.37160745013287944, -39.61402429467862873 ) ) ;
#93681=CARTESIAN_POINT ( 'NONE',  ( -9.761721577538938988, 51.33878080989101278, 2.429002427542664488 ) ) ;
#93721=DIRECTION ( 'NONE',  ( -0.000000000000000000, 1.000000000000000000, -0.000000000000000000 ) ) ;
#93736=VERTEX_POINT ( 'NONE', #24548 ) ;
#93753=CARTESIAN_POINT ( 'NONE',  ( -7.577668482282922113, 51.95108853748999422, 3.571063677695252458 ) ) ;
#93755=EDGE_LOOP ( 'NONE', ( #14503, #174, #64070, #85763 ) ) ;
#93760=EDGE_CURVE ( 'NONE', #90581, #58522, #9420, .T. ) ;
#93765=B_SPLINE_CURVE_WITH_KNOTS ( 'NONE', 3,
 ( #47801, #87232, #6821, #14369, #39741, #13314, #72622, #105524, #55365, #62955, #87764, #105002, #12785, #31144, #104456, #31664, #47278, #95852, #64032, #72094 ),
 .UNSPECIFIED., .F., .F.,
 ( 4, 2, 2, 2, 2, 2, 2, 2, 2, 4 ),
 ( 0.007215398811948415224, 0.007719408675872659574, 0.008223418539796903057, 0.008727428403721147407, 0.009231438267645391757, 0.009735448131569637842, 0.01023945799549388046, 0.01049146292745600090, 0.01074346785941812134, 0.01124747772334235701 ),
 .UNSPECIFIED. ) ;
#93775=ORIENTED_EDGE ( 'NONE', *, *, #65031, .F. ) ;
#93792=CARTESIAN_POINT ( 'NONE',  ( -24.31942756636476943, 25.21064302835431548, -32.55221473460276371 ) ) ;
#93796=EDGE_LOOP ( 'NONE', ( #2794, #50893, #86045, #47976 ) ) ;
#93797=CARTESIAN_POINT ( 'NONE',  ( 0.5678959950308366533, 37.15953799686300130, 27.38331912478550478 ) ) ;
#93807=DIRECTION ( 'NONE',  ( -0.000000000000000000, 1.000000000000000000, -0.000000000000000000 ) ) ;
#93811=CARTESIAN_POINT ( 'NONE',  ( -15.39709502357286652, 46.16515237750015643, 5.602001606816734203 ) ) ;
#93812=ORIENTED_EDGE ( 'NONE', *, *, #52412, .T. ) ;
#93843=CARTESIAN_POINT ( 'NONE',  ( 28.34337590820723918, 36.34601651445377968, 8.617044493960250406 ) ) ;
#93846=CARTESIAN_POINT ( 'NONE',  ( 27.10511071441204578, 34.75829513984540142, 7.556984339685363317 ) ) ;
#93858=DIRECTION ( 'NONE',  ( 0.000000000000000000, 0.000000000000000000, 1.000000000000000000 ) ) ;
#93874=CARTESIAN_POINT ( 'NONE',  ( 23.54393690455825094, 28.03570273098069876, 30.73873073986555937 ) ) ;
#93875=DIRECTION ( 'NONE',  ( 0.000000000000000000, 1.000000000000000000, -0.000000000000000000 ) ) ;
#93891=CARTESIAN_POINT ( 'NONE',  ( 36.81615681129832041, 25.76252507750780296, -13.21838005021004747 ) ) ;
#93896=DIRECTION ( 'NONE',  ( -0.000000000000000000, 1.000000000000000000, -0.000000000000000000 ) ) ;
#93900=CARTESIAN_POINT ( 'NONE',  ( -9.295212903232194179, 43.59689220704109403, -14.93628917660103994 ) ) ;
#93912=CYLINDRICAL_SURFACE ( 'NONE', #35366, 33.82893434829263413 ) ;
#93928=ORIENTED_EDGE ( 'NONE', *, *, #101510, .T. ) ;
#93949=CARTESIAN_POINT ( 'NONE',  ( -46.78576055570702863, 18.82161635153803658, 15.45372055756467944 ) ) ;
#93953=CARTESIAN_POINT ( 'NONE',  ( -29.49619080111420999, 13.37262004692842865, -39.61417171781349111 ) ) ;
#93954=CARTESIAN_POINT ( 'NONE',  ( 0.07779196254430825741, 12.91535575337009867, 51.75000000000002842 ) ) ;
#93962=DIRECTION ( 'NONE',  ( 0.000000000000000000, 1.000000000000000000, 0.000000000000000000 ) ) ;
#93968=FACE_BOUND ( 'NONE', #37040, .T. ) ;
#93969=( LENGTH_UNIT ( ) NAMED_UNIT ( * ) SI_UNIT ( .MILLI., .METRE. ) );
#93975=VERTEX_POINT ( 'NONE', #7651 ) ;
#93978=( NAMED_UNIT ( * ) SI_UNIT ( $, .STERADIAN. ) SOLID_ANGLE_UNIT ( ) );
#93986=CARTESIAN_POINT ( 'NONE',  ( -9.443351513663847285, 46.21199249391292341, -13.23092383815009754 ) ) ;
#93989=COLOUR_RGB ( '', 0.40784314, 0.44705882, 0.49803922) ;
#94017=CARTESIAN_POINT ( 'NONE',  ( -11.30498485061268354, 43.19237185749400254, 14.90159096885996703 ) ) ;
#94020=CIRCLE ( 'NONE', #95714, 24.55262289886175964 ) ;
#94058=CARTESIAN_POINT ( 'NONE',  ( -16.75187969033532553, 34.25544727262118982, 24.30698433968612449 ) ) ;
#94063=CARTESIAN_POINT ( 'NONE',  ( 48.87659302348946966, 8.116727071898608870, -16.52478270335645405 ) ) ;
#94079=EDGE_CURVE ( 'NONE', #23687, #84521, #99866, .T. ) ;
#94080=CARTESIAN_POINT ( 'NONE',  ( 6.076047337594906672, 51.26610334597046403, -8.267531848790646620 ) ) ;
#94112=CARTESIAN_POINT ( 'NONE',  ( -27.10511071441183262, 34.47735702144344572, 10.05698433968616001 ) ) ;
#94122=CARTESIAN_POINT ( 'NONE',  ( -30.77294675439362592, 10.36444884528812871, -40.23167857000805014 ) ) ;
#94141=CARTESIAN_POINT ( 'NONE',  ( 4.446365519863139326, 54.30554020026675488, -6.355018452323170308 ) ) ;
#94202=LINE ( 'NONE', #12204, #82020 ) ;
#94205=CARTESIAN_POINT ( 'NONE',  ( 29.27148335582070615, 13.57837266936924081, -39.67318301868883168 ) ) ;
#94214=CARTESIAN_POINT ( 'NONE',  ( 16.75187969033515145, 34.99134772383131775, -21.80698433968624528 ) ) ;
#94226=ORIENTED_EDGE ( 'NONE', *, *, #18018, .T. ) ;
#94237=CARTESIAN_POINT ( 'NONE',  ( 9.204625048146249711, 43.65511487171167460, 14.80422153561283771 ) ) ;
#94255=CARTESIAN_POINT ( 'NONE',  ( -1.219521042794267762, 27.62924000314889739, 39.81737217016015506 ) ) ;
#94256=CARTESIAN_POINT ( 'NONE',  ( 1.219931503106709281, 36.63069750044676454, -28.81634217350109495 ) ) ;
#94268=CARTESIAN_POINT ( 'NONE',  ( -47.90408546931278266, 11.89605000366066889, 14.35535821593516737 ) ) ;
#94270=B_SPLINE_CURVE_WITH_KNOTS ( 'NONE', 3,
 ( #98644, #88979, #47963, #57648, #99174, #6446, #6981, #39899, #72773, #105679, #64702, #44153, #43088, #34503, #2072, #85136, #59814, #978, #68434, #35024, #58748, #25891, #1536, #101846, #51154, #101327, #74894, #11227, #10172, #33961 ),
 .UNSPECIFIED., .F., .F.,
 ( 4, 2, 2, 2, 2, 2, 2, 2, 2, 2, 2, 2, 2, 2, 4 ),
 ( 0.01188303771272031933, 0.01280230725828193292, 0.01326194203106274318, 0.01372157680384355344, 0.01418121157662436196, 0.01441102896301475929, 0.01464084634940515488, 0.01487066373579555220, 0.01510048112218594432, 0.01556011589496672856, 0.01601975066774751280, 0.01647938544052829704, 0.01739865498608986205, 0.01831792453165143053, 0.01923719407721299207 ),
 .UNSPECIFIED. ) ;
#94289=AXIS2_PLACEMENT_3D ( 'NONE', #10302, #27073, #1671 ) ;
#94296=CARTESIAN_POINT ( 'NONE',  ( 18.00631980831534307, 36.44533851663729251, 23.17937010874015158 ) ) ;
#94301=STYLED_ITEM ( 'NONE', ( #71239 ), #67118 ) ;
#94335=ORIENTED_EDGE ( 'NONE', *, *, #82081, .T. ) ;
#94338=B_SPLINE_CURVE_WITH_KNOTS ( 'NONE', 3,
 ( #99338, #11794, #29116, #60387, #37185, #93264, #70047, #44726, #3732, #85171, #102418, #94876, #19426, #102952, #61985, #25517, #21016, #53856, #41657, #74545 ),
 .UNSPECIFIED., .F., .F.,
 ( 4, 2, 2, 2, 2, 2, 2, 2, 2, 4 ),
 ( 0.0009441224788332248452, 0.001448919914566970018, 0.001953717350300715298, 0.002458514786034460362, 0.002963312221768203258, 0.003468109657501946153, 0.003972907093235689482, 0.004225305811102560496, 0.004477704528969431511, 0.004982501964703167467 ),
 .UNSPECIFIED. ) ;
#94349=CONICAL_SURFACE ( 'NONE', #8164, 2747.477419454587107, 1.221730476396026610 ) ;
#94353=CARTESIAN_POINT ( 'NONE',  ( -48.90200833301644678, 9.381371963275082493, 14.70088518568426927 ) ) ;
#94360=CARTESIAN_POINT ( 'NONE',  ( -29.87373162892149026, 8.058069557479628386, 42.09632259471302973 ) ) ;
#94375=ORIENTED_EDGE ( 'NONE', *, *, #79970, .T. ) ;
#94389=EDGE_LOOP ( 'NONE', ( #27494, #7736, #37335, #14439 ) ) ;
#94402=DIRECTION ( 'NONE',  ( -0.000000000000000000, 1.000000000000000000, -0.000000000000000000 ) ) ;
#94419=CARTESIAN_POINT ( 'NONE',  ( 24.44497366060289067, 27.40106161504759896, 32.24452914909036849 ) ) ;
#94425=MECHANICAL_DESIGN_GEOMETRIC_PRESENTATION_REPRESENTATION('',(#73110),#65065);
#94448=UNCERTAINTY_MEASURE_WITH_UNIT (LENGTH_MEASURE( 1.000000000000000082E-05 ), #6802, 'distance_accuracy_value', 'NONE');
#94453=CARTESIAN_POINT ( 'NONE',  ( -1.099991320666667161, 45.96958673343657864, 16.88535858699162517 ) ) ;
#94459=CARTESIAN_POINT ( 'NONE',  ( -48.26727629737658987, 11.05468605157632744, -14.37283805632304912 ) ) ;
#94484=SURFACE_SIDE_STYLE ('',( #11399 ) ) ;
#94491=CARTESIAN_POINT ( 'NONE',  ( 16.91579475168075319, 34.95500323700078837, 21.80698433968581185 ) ) ;
#94493=DIRECTION ( 'NONE',  ( -0.000000000000000000, 1.000000000000000000, -0.000000000000000000 ) ) ;
#94494=CARTESIAN_POINT ( 'NONE',  ( -29.68315524077005207, 13.12249633091091816, -39.60535821593474282 ) ) ;
#94495=CARTESIAN_POINT ( 'NONE',  ( 1.160519905071935698, 17.00675097771450339, 50.01991939293108658 ) ) ;
#94496=DIRECTION ( 'NONE',  ( -0.000000000000000000, 1.000000000000000000, -0.000000000000000000 ) ) ;
#94527=CARTESIAN_POINT ( 'NONE',  ( -16.83431405849851359, 36.36677671467317197, 24.30698433968613870 ) ) ;
#94532=CARTESIAN_POINT ( 'NONE',  ( 5.855955192086414129, 53.40184725084972683, -8.398893590963069755 ) ) ;
#94539=CARTESIAN_POINT ( 'NONE',  ( -9.523267564283898423, 45.61198619316642322, -15.16070064068362200 ) ) ;
#94562=VERTEX_POINT ( 'NONE', #40191 ) ;
#94577=SURFACE_STYLE_USAGE ( .BOTH. , #19653 ) ;
#94582=CARTESIAN_POINT ( 'NONE',  ( 4.071647195599044089, 52.05561507541640509, -6.990456272512426850 ) ) ;
#94612=CARTESIAN_POINT ( 'NONE',  ( -17.99173077915196828, 34.45868671117904114, 22.69654071649677718 ) ) ;
#94631=ORIENTED_EDGE ( 'NONE', *, *, #66217, .T. ) ;
#94642=B_SPLINE_CURVE_WITH_KNOTS ( 'NONE', 3,
 ( #10294, #101446, #60481, #43206, #71704, #79812, #38841, #46394, #70141, #78225, #22674, #86869, #5914, #103045, #104619, #45347, #79284, #103563, #55512, #29201, #53431, #6441, #53936, #38328, #80327, #30768, #62076, #54989, #104084, #71189 ),
 .UNSPECIFIED., .F., .F.,
 ( 4, 2, 2, 2, 2, 2, 2, 2, 2, 2, 2, 2, 2, 2, 4 ),
 ( 0.01423689679755360885, 0.01470129771271631511, 0.01493349817029766477, 0.01516569862787901443, 0.01539789908546036236, 0.01563009954304171029, 0.01586230000062305995, 0.01609450045820440961, 0.01655890137336709506, 0.01702330228852978050, 0.01795210411885515486, 0.01888090594918052922, 0.01980970777950590705, 0.02073850960983128142, 0.02166731144015665578 ),
 .UNSPECIFIED. ) ;
#94644=CARTESIAN_POINT ( 'NONE',  ( 4.080274524171334072, 51.84966241523257224, 7.633405385586866210 ) ) ;
#94653=ADVANCED_FACE ( 'NONE', ( #78264 ), #84769, .F. ) ;
#94670=ORIENTED_EDGE ( 'NONE', *, *, #47989, .F. ) ;
#94720=CARTESIAN_POINT ( 'NONE',  ( 9.757377548409222196E-14, 52.17923068443732149, -7.749999999998994582 ) ) ;
#94749=B_SPLINE_CURVE_WITH_KNOTS ( 'NONE', 3,
 ( #50070, #9073, #16108, #49536, #82444, #17722, #6952, #48993, #81894, #50582, #8545, #33383, #25303, #97542, #105646, #31786, #73813, #17196, #48469, #82978, #40386, #106707, #106165, #32325, #99143, #41977, #94268, #11190 ),
 .UNSPECIFIED., .F., .F.,
 ( 4, 2, 2, 2, 2, 2, 2, 2, 2, 2, 2, 2, 2, 4 ),
 ( 0.002626378601955878331, 0.003560090090687870537, 0.004493801579419862309, 0.005427513068151854081, 0.006361224556883846720, 0.006828080301249843040, 0.007061508173432842067, 0.007294936045615841094, 0.007528363917798841856, 0.007761791789981840883, 0.008228647534347842407, 0.008695503278713843931, 0.009162359023079845455, 0.01009607051181185544 ),
 .UNSPECIFIED. ) ;
#94753=CARTESIAN_POINT ( 'NONE',  ( 29.09616027395232507, 9.373446874598327483, -41.96755440745717181 ) ) ;
#94831=CARTESIAN_POINT ( 'NONE',  ( -7.433075656983189283, 52.17533548997528214, 2.232706251697821997 ) ) ;
#94834=VECTOR ( 'NONE', #103717, 1000.000000000000000 ) ;
#94838=FILL_AREA_STYLE ('',( #104491 ) ) ;
#94845=PLANE ( 'NONE',  #49613 ) ;
#94848=CARTESIAN_POINT ( 'NONE',  ( 3.636386562469240082E-15, 36.30024107553216339, 29.75000000000000355 ) ) ;
#94876=CARTESIAN_POINT ( 'NONE',  ( 15.64282023038906111, 37.16738321503569153, -22.45670599646780374 ) ) ;
#94878=CARTESIAN_POINT ( 'NONE',  ( -26.34322927111401214, 37.12867781788141031, 7.801957073146333244 ) ) ;
#94896=CARTESIAN_POINT ( 'NONE',  ( -30.93163070004102266, 9.246556120444287430, 40.70059110212513076 ) ) ;
#94910=CARTESIAN_POINT ( 'NONE',  ( -15.64685761340797754, 44.06059264762727423, -4.635351185647528460 ) ) ;
#94934=CYLINDRICAL_SURFACE ( 'NONE', #69544, 1.250000000000001110 ) ;
#94942=ORIENTED_EDGE ( 'NONE', *, *, #18018, .F. ) ;
#94955=CARTESIAN_POINT ( 'NONE',  ( -16.75187969033554936, -1.200000000000000030E-05, -23.05698433968595751 ) ) ;
#94962=ORIENTED_EDGE ( 'NONE', *, *, #47450, .F. ) ;
#94984=CARTESIAN_POINT ( 'NONE',  ( -0.9887052094731583196, 12.53211684992026420, 49.73207603363582763 ) ) ;
#94993=CARTESIAN_POINT ( 'NONE',  ( 10.36819426459840265, 43.97404897798725187, 12.90779740156146005 ) ) ;
#95015=B_SPLINE_CURVE_WITH_KNOTS ( 'NONE', 3,
 ( #20260, #9980, #86029, #35359, #44493, #77381, #12101, #76839, #19191, #84413, #83869, #92489, #91964, #10509, #42883, #93031, #26743, #27817, #4025, #36952, #69821, #101122, #11030, #34832, #101658, #27283, #60164, #35902 ),
 .UNSPECIFIED., .F., .F.,
 ( 4, 2, 2, 2, 2, 2, 2, 2, 2, 2, 2, 2, 2, 4 ),
 ( 0.0005213801848541129184, 0.0007543876772704475415, 0.0009873951696867831404, 0.001453410154519451519, 0.001919425139352119464, 0.002385440124184787843, 0.003317470093850121132, 0.004249500063515453986, 0.005181530033180787274, 0.006113560002846121430, 0.007045589972511453851, 0.007511604957344118760, 0.007744612449760451649, 0.007977619942176784537 ),
 .UNSPECIFIED. ) ;
#95024=CARTESIAN_POINT ( 'NONE',  ( -47.50459250088627527, 17.89957706894783840, 14.46754909258801725 ) ) ;
#95044=EDGE_CURVE ( 'NONE', #86521, #94562, #78569, .T. ) ;
#95054=VERTEX_POINT ( 'NONE', #4788 ) ;
#95061=FACE_OUTER_BOUND ( 'NONE', #6947, .T. ) ;
#95062=CARTESIAN_POINT ( 'NONE',  ( 17.83157035608863694, 34.57710935724472279, -22.40747207865632618 ) ) ;
#95115=DIRECTION ( 'NONE',  ( -0.000000000000000000, 1.000000000000000000, -0.000000000000000000 ) ) ;
#95122=DIRECTION ( 'NONE',  ( -0.000000000000000000, 1.000000000000000000, -0.000000000000000000 ) ) ;
#95131=SURFACE_SIDE_STYLE ('',( #54621 ) ) ;
#95155=CARTESIAN_POINT ( 'NONE',  ( 48.80564935040053598, 14.82671221252832972, -14.61894534951930069 ) ) ;
#95162=CARTESIAN_POINT ( 'NONE',  ( 4.524745413718507692, 51.56500811734601797, 8.282296607710694758 ) ) ;
#95164=CARTESIAN_POINT ( 'NONE',  ( 38.54676549570872623, 27.49636554353505247, 11.41392474695979864 ) ) ;
#95176=CARTESIAN_POINT ( 'NONE',  ( -25.91608795999933434, 37.21123558588128333, -8.412246229538014930 ) ) ;
#95203=ADVANCED_FACE ( 'NONE', ( #890 ), #33867, .F. ) ;
#95216=CARTESIAN_POINT ( 'NONE',  ( -8.559508646656370345, 51.83514083332403999, 1.531152949374564365 ) ) ;
#95224=CARTESIAN_POINT ( 'NONE',  ( -17.26510143360928140, 45.41334515577719344, -6.504361445978008582 ) ) ;
#95226=CARTESIAN_POINT ( 'NONE',  ( 17.25418300772434321, 43.52740561176951672, -4.305768132160899597 ) ) ;
#95258=( NAMED_UNIT ( * ) SI_UNIT ( $, .STERADIAN. ) SOLID_ANGLE_UNIT ( ) );
#95276=VECTOR ( 'NONE', #50972, 1000.000000000000114 ) ;
#95278=CARTESIAN_POINT ( 'NONE',  ( -8.717348576474769573, 51.77858947231555220, 1.531152949374564143 ) ) ;
#95294=EDGE_CURVE ( 'NONE', #68089, #96995, #16, .T. ) ;
#95300=CARTESIAN_POINT ( 'NONE',  ( 9.077274974099184490, 43.76958732884290271, 14.51298487815000193 ) ) ;
#95314=DIRECTION ( 'NONE',  ( -0.000000000000000000, 1.000000000000000000, -0.000000000000000000 ) ) ;
#95350=CARTESIAN_POINT ( 'NONE',  ( 1.159632968975068845, 11.84294440633027001, -50.01761517489052267 ) ) ;
#95352=CYLINDRICAL_SURFACE ( 'NONE', #24160, 1.250000000000000222 ) ;
#95365=ORIENTED_EDGE ( 'NONE', *, *, #101410, .F. ) ;
#95383=ADVANCED_FACE ( 'NONE', ( #29889 ), #62774, .F. ) ;
#95399=CARTESIAN_POINT ( 'NONE',  ( -38.56652002779529909, 27.31830886215414012, 12.97473753426408472 ) ) ;
#95400=CARTESIAN_POINT ( 'NONE',  ( -5.290067270632268226, 54.20842449845686417, -6.031152949374520844 ) ) ;
#95406=CARTESIAN_POINT ( 'NONE',  ( -30.42742517972270377, 7.740625494265014339, 41.86256052107386694 ) ) ;
#95408=( GEOMETRIC_REPRESENTATION_CONTEXT ( 3 ) GLOBAL_UNCERTAINTY_ASSIGNED_CONTEXT ( ( #78313 ) ) GLOBAL_UNIT_ASSIGNED_CONTEXT ( ( #35137, #26004, #34081 ) ) REPRESENTATION_CONTEXT ( 'NONE', 'WORKASPACE' ) );
#95420=ADVANCED_FACE ( 'NONE', ( #42729 ), #83703, .F. ) ;
#95426=VECTOR ( 'NONE', #42997, 1000.000000000000000 ) ;
#95435=FACE_BOUND ( 'NONE', #2896, .T. ) ;
#95438=ORIENTED_EDGE ( 'NONE', *, *, #29544, .T. ) ;
#95462=CARTESIAN_POINT ( 'NONE',  ( -16.75187969033554936, 37.11970326878314097, -21.80698433968595751 ) ) ;
#95468=ORIENTED_EDGE ( 'NONE', *, *, #2378, .F. ) ;
#95472=CARTESIAN_POINT ( 'NONE',  ( -1.218060163800027018, 51.81072258316640244, 8.677483100841660857 ) ) ;
#95481=CARTESIAN_POINT ( 'NONE',  ( -9.882987946621028641, 43.35715013040534416, -15.34374875303372576 ) ) ;
#95491=CARTESIAN_POINT ( 'NONE',  ( -0.1549862348970068859, 7.763683557544238667, 51.74239981364938501 ) ) ;
#95509=CARTESIAN_POINT ( 'NONE',  ( -16.58692244248932468, 34.28951775970666915, 24.30698433968612804 ) ) ;
#95521=PRESENTATION_STYLE_ASSIGNMENT (( #12460 ) ) ;
#95524=CARTESIAN_POINT ( 'NONE',  ( 30.10126468112042986, 13.03072330106368781, -42.03538192853125111 ) ) ;
#95551=FACE_OUTER_BOUND ( 'NONE', #97458, .T. ) ;
#95552=AXIS2_PLACEMENT_3D ( 'NONE', #59259, #18829, #92671 ) ;
#95567=ORIENTED_EDGE ( 'NONE', *, *, #86341, .T. ) ;
#95579=CARTESIAN_POINT ( 'NONE',  ( 3.006829104376306210E-15, 38.19193163660327173, -24.55262289886175964 ) ) ;
#95591=DIRECTION ( 'NONE',  ( 0.000000000000000000, 0.000000000000000000, 1.000000000000000000 ) ) ;
#95603=CARTESIAN_POINT ( 'NONE',  ( -11.53061943269021050, 45.53913102596384022, 13.95708208482078483 ) ) ;
#95605=CARTESIAN_POINT ( 'NONE',  ( 10.45288716919446692, 45.35420570811798058, -15.39944944803840698 ) ) ;
#95620=CARTESIAN_POINT ( 'NONE',  ( -9.560175649466449599, 53.41719017493603872, -3.548455548004890936 ) ) ;
#95627=EDGE_CURVE ( 'NONE', #1638, #23889, #84512, .T. ) ;
#95634=AXIS2_PLACEMENT_3D ( 'NONE', #30950, #31995, #13654 ) ;
#95635=MECHANICAL_DESIGN_GEOMETRIC_PRESENTATION_REPRESENTATION('',(#74965),#14686);
#95652=DIRECTION ( 'NONE',  ( 0.000000000000000000, 0.000000000000000000, 1.000000000000000000 ) ) ;
#95653=DIRECTION ( 'NONE',  ( 0.000000000000000000, -0.9221233147934838614, -0.3868961001538753219 ) ) ;
#95663=FILL_AREA_STYLE_COLOUR ( '', #31634 ) ;
#95667=AXIS2_PLACEMENT_3D ( 'NONE', #645, #51888, #10367 ) ;
#95674=CARTESIAN_POINT ( 'NONE',  ( 0.000000000000000000, 27.68727484027578356, -33.82893434829263413 ) ) ;
#95683=CARTESIAN_POINT ( 'NONE',  ( 37.88764991246872427, 27.49831504271226734, 13.42506037026353738 ) ) ;
#95714=AXIS2_PLACEMENT_3D ( 'NONE', #64890, #97252, #48158 ) ;
#95716=B_SPLINE_CURVE_WITH_KNOTS ( 'NONE', 3,
 ( #22940, #63398, #104903, #105423, #21886, #23471, #71991, #39648, #31041, #15344, #63921, #56307, #96809, #40150, #81133, #6180, #55777, #31563 ),
 .UNSPECIFIED., .F., .F.,
 ( 4, 2, 2, 2, 2, 2, 2, 2, 4 ),
 ( 0.002442598131820562096, 0.002946487642774274582, 0.003198432398251129308, 0.003450377153727984467, 0.004458156175635422450, 0.004962045686589144043, 0.005465935197542866504, 0.005969824708496588965, 0.006473714219450311426 ),
 .UNSPECIFIED. ) ;
#95728=VERTEX_POINT ( 'NONE', #25388 ) ;
#95735=ORIENTED_EDGE ( 'NONE', *, *, #119, .T. ) ;
#95740=ORIENTED_EDGE ( 'NONE', *, *, #102003, .F. ) ;
#95747=CARTESIAN_POINT ( 'NONE',  ( 17.58429050390567383, 43.20947028070973772, -6.235027717422475746 ) ) ;
#95752=CARTESIAN_POINT ( 'NONE',  ( 24.32770621568436198, 27.33676458719045854, -32.55389746325929679 ) ) ;
#95753=ORIENTED_EDGE ( 'NONE', *, *, #91531, .T. ) ;
#95761=CARTESIAN_POINT ( 'NONE',  ( -0.08502184264844901695, 51.26930509877139031, -10.25000000000000000 ) ) ;
#95763=CARTESIAN_POINT ( 'NONE',  ( 0.1551999952495689006, 18.85523120475384573, -49.25760693525473499 ) ) ;
#95765=B_SPLINE_CURVE_WITH_KNOTS ( 'NONE', 3,
 ( #26520, #57755, #92253, #75552, #50722, #17869, #18408, #90682, #58858, #58306, #33522, #83634, #75003, #1647, #34608, #9209, #43194, #2180, #51263, #84187, #1098, #10282 ),
 .UNSPECIFIED., .F., .F.,
 ( 4, 2, 2, 2, 2, 2, 2, 2, 2, 2, 4 ),
 ( 0.007303875631389625950, 0.007555818938590126363, 0.007807762245790625909, 0.008311648860191622398, 0.008815535474592619755, 0.009319422088993615377, 0.009823308703394612734, 0.01032719531779561009, 0.01083108193219660571, 0.01108302523939710613, 0.01133496854659760480 ),
 .UNSPECIFIED. ) ;
#95789=CYLINDRICAL_SURFACE ( 'NONE', #36447, 1.250000000000001110 ) ;
#95800=LINE ( 'NONE', #103870, #84067 ) ;
#95802=CARTESIAN_POINT ( 'NONE',  ( 16.64348903516512834, 45.60392139269950462, -6.657797401561770911 ) ) ;
#95805=VERTEX_POINT ( 'NONE', #40469 ) ;
#95822=CARTESIAN_POINT ( 'NONE',  ( 16.58627947206455744, 35.02806585639755355, -21.80698433968624173 ) ) ;
#95828=CARTESIAN_POINT ( 'NONE',  ( 9.523181975977013991, 43.48366182708068095, 15.16065324379447077 ) ) ;
#95835=MECHANICAL_DESIGN_GEOMETRIC_PRESENTATION_REPRESENTATION('',(#13126),#50999);
#95845=VERTEX_POINT ( 'NONE', #92741 ) ;
#95852=CARTESIAN_POINT ( 'NONE',  ( -0.3374940846666292793, 54.29275678046128206, -7.784862885205691363 ) ) ;
#95863=EDGE_CURVE ( 'NONE', #54301, #98888, #57543, .T. ) ;
#95873=FILL_AREA_STYLE_COLOUR ( '', #65184 ) ;
#95888=CARTESIAN_POINT ( 'NONE',  ( 17.99621717127815046, 36.54019273113857480, 22.85642881224868006 ) ) ;
#95889=CONICAL_SURFACE ( 'NONE', #40822, 46.94949242731048145, 0.3972631705159501148 ) ;
#95905=ADVANCED_FACE ( 'NONE', ( #10743 ), #43135, .F. ) ;
#95942=CARTESIAN_POINT ( 'NONE',  ( -38.54883366569859504, 27.49541921524758337, 11.41610407978632402 ) ) ;
#95958=CARTESIAN_POINT ( 'NONE',  ( -15.88903491159068082, 43.99850675625265950, -4.407766777241893585 ) ) ;
#95959=ORIENTED_EDGE ( 'NONE', *, *, #51762, .F. ) ;
#95971=ORIENTED_EDGE ( 'NONE', *, *, #12962, .F. ) ;
#95973=VERTEX_POINT ( 'NONE', #95400 ) ;
#95994=FILL_AREA_STYLE ('',( #7478 ) ) ;
#96023=CARTESIAN_POINT ( 'NONE',  ( -9.076720569991527654, 43.77011807854803749, -14.51161200666307849 ) ) ;
#96040=CARTESIAN_POINT ( 'NONE',  ( 10.61022379808845351, 43.90722765790382454, 12.94778756132729391 ) ) ;
#96048=CARTESIAN_POINT ( 'NONE',  ( -16.42296553627748423, 35.05188915981860731, 21.84814778194889939 ) ) ;
#96061=CARTESIAN_POINT ( 'NONE',  ( 30.87964800539008081, 13.48323453669522465, -41.23000148635505013 ) ) ;
#96071=CARTESIAN_POINT ( 'NONE',  ( 26.48443586042315445, 34.96036863989223775, -7.709928564565299069 ) ) ;
#96072=PRESENTATION_STYLE_ASSIGNMENT (( #70198 ) ) ;
#96107=CYLINDRICAL_SURFACE ( 'NONE', #102869, 1.250000000000001110 ) ;
#96114=ORIENTED_EDGE ( 'NONE', *, *, #37418, .F. ) ;
#96116=SURFACE_SIDE_STYLE ('',( #102613 ) ) ;
#96121=DIRECTION ( 'NONE',  ( 0.000000000000000000, 0.000000000000000000, 1.000000000000000000 ) ) ;
#96133=CARTESIAN_POINT ( 'NONE',  ( -16.75187969033554936, 36.38380281757302015, -24.30698433968596106 ) ) ;
#96141=DIRECTION ( 'NONE',  ( -0.000000000000000000, 1.000000000000000000, -0.000000000000000000 ) ) ;
#96156=CARTESIAN_POINT ( 'NONE',  ( -9.655545083697493425, 53.40239499979105631, -3.405056376145797703 ) ) ;
#96171=CARTESIAN_POINT ( 'NONE',  ( 16.58646281676601575, 37.15392203743714816, 21.81520449073893531 ) ) ;
#96174=CARTESIAN_POINT ( 'NONE',  ( 0.7842477567516482617, 43.26537946031525195, -18.48697474366874616 ) ) ;
#96186=VERTEX_POINT ( 'NONE', #66084 ) ;
#96199=VECTOR ( 'NONE', #2624, 1000.000000000000227 ) ;
#96218=DIRECTION ( 'NONE',  ( 0.000000000000000000, 0.000000000000000000, 1.000000000000000000 ) ) ;
#96231=CARTESIAN_POINT ( 'NONE',  ( 11.53817350584529144, 43.34042535094782522, 14.20050555370484169 ) ) ;
#96286=CARTESIAN_POINT ( 'NONE',  ( -16.41900535493362412, 37.18348077072296576, 21.84048156162998922 ) ) ;
#96295=CARTESIAN_POINT ( 'NONE',  ( 17.81883034442599012, 43.26653065284484256, -4.974467122015703069 ) ) ;
#96300=CARTESIAN_POINT ( 'NONE',  ( -23.55017320447252871, 25.19299454758883527, 33.17279571835358354 ) ) ;
#96312=CARTESIAN_POINT ( 'NONE',  ( 22.59032126178805200, 25.42946310086070483, -33.04941538723348060 ) ) ;
#96323=CARTESIAN_POINT ( 'NONE',  ( -36.47142920048730019, 28.20086854896861084, 11.58052048957462965 ) ) ;
#96347=CARTESIAN_POINT ( 'NONE',  ( 46.83658167332238520, 18.87978240383752748, 15.22028160905541228 ) ) ;
#96353=STYLED_ITEM ( 'NONE', ( #64444 ), #31924 ) ;
#96368=CARTESIAN_POINT ( 'NONE',  ( -1.007187577324624161, 25.34754566897618133, -40.24471185633667147 ) ) ;
#96370=EDGE_CURVE ( 'NONE', #95728, #56342, #29873, .T. ) ;
#96398=PRESENTATION_STYLE_ASSIGNMENT (( #30610 ) ) ;
#96415=CARTESIAN_POINT ( 'NONE',  ( 1.249985938038163935, 25.55829499317779607, -39.65856465433250122 ) ) ;
#96419=CARTESIAN_POINT ( 'NONE',  ( -7.350717716529898027, 52.09114849985863316, 3.138633237920497088 ) ) ;
#96422=CARTESIAN_POINT ( 'NONE',  ( -1.101843165701975602, 34.39665841235530053, -29.11167040375564952 ) ) ;
#96424=CARTESIAN_POINT ( 'NONE',  ( 0.8429065489285075818, 8.500928503492241717, -51.42638058623190744 ) ) ;
#96425=PRESENTATION_STYLE_ASSIGNMENT (( #63527 ) ) ;
#96435=CARTESIAN_POINT ( 'NONE',  ( -1.093036222098963561, 36.52507611590718284, 29.11179518116718512 ) ) ;
#96440=CARTESIAN_POINT ( 'NONE',  ( -27.10511071441182906, 36.60571256639526894, 10.05698433968618488 ) ) ;
#96443=ORIENTED_EDGE ( 'NONE', *, *, #83243, .T. ) ;
#96445=AXIS2_PLACEMENT_3D ( 'NONE', #66968, #34628, #68569 ) ;
#96517=LINE ( 'NONE', #80837, #69833 ) ;
#96518=LINE ( 'NONE', #55485, #47781 ) ;
#96521=ORIENTED_EDGE ( 'NONE', *, *, #86571, .F. ) ;
#96532=CARTESIAN_POINT ( 'NONE',  ( -1.100033992246165715, 25.39386148385951358, 40.11500734754208963 ) ) ;
#96533=CARTESIAN_POINT ( 'NONE',  ( 0.3379642130336351080, 27.30892935218310313, -40.71492746916538863 ) ) ;
#96544=VERTEX_POINT ( 'NONE', #30169 ) ;
#96555=CARTESIAN_POINT ( 'NONE',  ( -0.5680898101815228252, 34.21849481828488848, 29.61659561779407568 ) ) ;
#96578=CARTESIAN_POINT ( 'NONE',  ( -15.51141066637804400, 34.77717015103064568, 23.41592087525514643 ) ) ;
#96581=EDGE_CURVE ( 'NONE', #74647, #67680, #92324, .T. ) ;
#96587=DIRECTION ( 'NONE',  ( 0.000000000000000000, 0.000000000000000000, 1.000000000000000000 ) ) ;
#96605=CARTESIAN_POINT ( 'NONE',  ( 26.49069557787568385, 34.70594681385026092, -9.907218389797451508 ) ) ;
#96608=CONICAL_SURFACE ( 'NONE', #50089, 23.23666318551310539, 1.221730476396026388 ) ;
#96615=CARTESIAN_POINT ( 'NONE',  ( -28.79546424415106998, 15.38851513919402869, -41.74402054108289661 ) ) ;
#96616=FILL_AREA_STYLE_COLOUR ( '', #1805 ) ;
#96636=CARTESIAN_POINT ( 'NONE',  ( 6.400292240292954737, 53.43402837650388904, -7.879178544242287252 ) ) ;
#96637=CARTESIAN_POINT ( 'NONE',  ( 17.95946743641316345, 34.46552302443144100, -22.69735960963333454 ) ) ;
#96644=VERTEX_POINT ( 'NONE', #57584 ) ;
#96647=AXIS2_PLACEMENT_3D ( 'NONE', #1491, #40907, #930 ) ;
#96665=CARTESIAN_POINT ( 'NONE',  ( -10.91152070480441871, 45.93327767897820735, 13.06343554040036459 ) ) ;
#96667=CARTESIAN_POINT ( 'NONE',  ( 11.53061943269010392, 45.53913102596383311, -13.95708208482086121 ) ) ;
#96677=CARTESIAN_POINT ( 'NONE',  ( -48.02835407290516656, -1.200000000000000030E-05, 15.60535821593516737 ) ) ;
#96698=CARTESIAN_POINT ( 'NONE',  ( -48.91605700228340936, 13.22299455560985315, -16.49079035033054197 ) ) ;
#96720=ORIENTED_EDGE ( 'NONE', *, *, #35342, .F. ) ;
#96730=CARTESIAN_POINT ( 'NONE',  ( -1.167655683674313938, 14.75960163002330994, -50.96284648200735745 ) ) ;
#96732=DIRECTION ( 'NONE',  ( 1.150791560227848544E-16, -0.3420201433256727652, 0.9396926207859068736 ) ) ;
#96747=CYLINDRICAL_SURFACE ( 'NONE', #20759, 1.250000000000001110 ) ;
#96751=CARTESIAN_POINT ( 'NONE',  ( 37.56673239365873940, 27.88554838446218653, 10.95617127780822564 ) ) ;
#96753=CARTESIAN_POINT ( 'NONE',  ( 11.39584891955474433, 43.21406130090534958, 14.75674298142433827 ) ) ;
#96761=ORIENTED_EDGE ( 'NONE', *, *, #21027, .T. ) ;
#96772=DIRECTION ( 'NONE',  ( 0.000000000000000000, 0.000000000000000000, 1.000000000000000000 ) ) ;
#96782=B_SPLINE_CURVE_WITH_KNOTS ( 'NONE', 3,
 ( #78398, #3993, #53072, #69788, #94612, #37454, #35323, #43911, #69271, #3459, #102144, #102682, #59581, #26708, #92447, #93541, #84379, #94058 ),
 .UNSPECIFIED., .F., .F.,
 ( 4, 2, 2, 2, 2, 2, 2, 2, 4 ),
 ( 0.006884628567306551837, 0.007891832553332813263, 0.008899036539359075557, 0.009150837535865643732, 0.009402638532372210173, 0.009906240525385343054, 0.01015804152189190776, 0.01040984251839847420, 0.01091344451141159320 ),
 .UNSPECIFIED. ) ;
#96796=LINE ( 'NONE', #22928, #61316 ) ;
#96803=CARTESIAN_POINT ( 'NONE',  ( -15.76193534935225671, 36.72733462479576616, 23.83658602074646637 ) ) ;
#96809=CARTESIAN_POINT ( 'NONE',  ( 1.009401082359720370, 34.89502620709782121, 27.74504690791027528 ) ) ;
#96817=CARTESIAN_POINT ( 'NONE',  ( -5.208114383187426810, 52.09973805833581650, -6.031152949374310346 ) ) ;
#96823=CARTESIAN_POINT ( 'NONE',  ( -1.220780421567363883, 43.50148743144289654, -17.81286546842412832 ) ) ;
#96835=CARTESIAN_POINT ( 'NONE',  ( -48.02835407290534420, 16.78162100668604495, -14.35535821593460248 ) ) ;
#96865=CARTESIAN_POINT ( 'NONE',  ( 46.77759138928176696, 18.69812886098186411, 15.64253076101912399 ) ) ;
#96878=EDGE_CURVE ( 'NONE', #35979, #59308, #59571, .T. ) ;
#96880=CIRCLE ( 'NONE', #91722, 33.82893434829263413 ) ;
#96882=CARTESIAN_POINT ( 'NONE',  ( -1.249563713075066307, 25.67532180842502854, -39.33688851605202075 ) ) ;
#96915=FACE_OUTER_BOUND ( 'NONE', #59248, .T. ) ;
#96931=CARTESIAN_POINT ( 'NONE',  ( 0.1685780251646490369, 54.30395748168558612, -7.758569535635805536 ) ) ;
#96941=DIRECTION ( 'NONE',  ( 0.000000000000000000, 0.000000000000000000, 1.000000000000000000 ) ) ;
#96960=EDGE_CURVE ( 'NONE', #101, #79036, #91920, .T. ) ;
#96963=EDGE_CURVE ( 'NONE', #73917, #741, #81784, .T. ) ;
#96981=CARTESIAN_POINT ( 'NONE',  ( -27.10511071441182906, 36.60571256639526894, 10.05698433968618488 ) ) ;
#96995=VERTEX_POINT ( 'NONE', #74133 ) ;
#96999=( NAMED_UNIT ( * ) PLANE_ANGLE_UNIT ( ) SI_UNIT ( $, .RADIAN. ) );
#97000=CARTESIAN_POINT ( 'NONE',  ( 28.71549002649010518, 15.67055689680115016, 41.65541077617245946 ) ) ;
#97004=EDGE_CURVE ( 'NONE', #80390, #94562, #7272, .T. ) ;
#97006=CARTESIAN_POINT ( 'NONE',  ( -27.10511071441192144, 36.60571256639527604, -10.05698433968589178 ) ) ;
#97017=ORIENTED_EDGE ( 'NONE', *, *, #102806, .F. ) ;
#97034=ORIENTED_EDGE ( 'NONE', *, *, #30072, .T. ) ;
#97044=AXIS2_PLACEMENT_3D ( 'NONE', #100426, #65414, #1168 ) ;
#97046=CARTESIAN_POINT ( 'NONE',  ( 1.099700806557082355, 27.96998724311644935, -38.88428954940741988 ) ) ;
#97058=LINE ( 'NONE', #8579, #70887 ) ;
#97067=CARTESIAN_POINT ( 'NONE',  ( 3.337162542380456721E-15, 35.08181111624585213, 27.25000000000000000 ) ) ;
#97074=ADVANCED_FACE ( 'NONE', ( #217 ), #22450, .F. ) ;
#97091=SURFACE_SIDE_STYLE ('',( #104653 ) ) ;
#97129=CARTESIAN_POINT ( 'NONE',  ( -29.59387530091278862, 18.41945862786178623, -39.60535821593474992 ) ) ;
#97134=EDGE_CURVE ( 'NONE', #56766, #12068, #106244, .T. ) ;
#97145=CARTESIAN_POINT ( 'NONE',  ( 28.56372199056505323, 18.54333498561200955, -40.29094744152394014 ) ) ;
#97179=CARTESIAN_POINT ( 'NONE',  ( 10.28624191511809371, 45.38549880562041494, -15.40779740156171762 ) ) ;
#97216=ORIENTED_EDGE ( 'NONE', *, *, #95863, .T. ) ;
#97225=CARTESIAN_POINT ( 'NONE',  ( -23.21751746555280249, 27.38103382803677022, -33.20617127781034839 ) ) ;
#97229=FILL_AREA_STYLE_COLOUR ( '', #2303 ) ;
#97232=EDGE_LOOP ( 'NONE', ( #17561, #16321, #4220, #17082 ) ) ;
#97239=CARTESIAN_POINT ( 'NONE',  ( -38.31422226540048115, 27.60041950521512533, -11.19138753273245257 ) ) ;
#97242=CARTESIAN_POINT ( 'NONE',  ( -1.106745437108234142, 17.28904319046834459, -49.90271519190591931 ) ) ;
#97252=DIRECTION ( 'NONE',  ( 0.000000000000000000, 1.000000000000000000, 0.000000000000000000 ) ) ;
#97254=( NAMED_UNIT ( * ) SI_UNIT ( $, .STERADIAN. ) SOLID_ANGLE_UNIT ( ) );
#97277=CARTESIAN_POINT ( 'NONE',  ( -6.488032186737915374, 53.47822873620448547, 7.647501018148323837 ) ) ;
#97286=CARTESIAN_POINT ( 'NONE',  ( 0.000000000000000000, -1.200000000000000030E-05, -7.749999999999999112 ) ) ;
#97301=ORIENTED_EDGE ( 'NONE', *, *, #31070, .T. ) ;
#97305=CARTESIAN_POINT ( 'NONE',  ( 28.09805714684552314, 34.19617451435909317, 9.570894723979119334 ) ) ;
#97310=FACE_OUTER_BOUND ( 'NONE', #43356, .T. ) ;
#97314=CARTESIAN_POINT ( 'NONE',  ( 16.02260224162418112, 43.96096248673147500, 4.310921585563690428 ) ) ;
#97317=( GEOMETRIC_REPRESENTATION_CONTEXT ( 3 ) GLOBAL_UNCERTAINTY_ASSIGNED_CONTEXT ( ( #84743 ) ) GLOBAL_UNIT_ASSIGNED_CONTEXT ( ( #47502, #34018, #25946 ) ) REPRESENTATION_CONTEXT ( 'NONE', 'WORKASPACE' ) );
#97326=CARTESIAN_POINT ( 'NONE',  ( 23.62741386766530383, 27.31466638971096472, -33.14007574073367124 ) ) ;
#97335=ORIENTED_EDGE ( 'NONE', *, *, #25435, .F. ) ;
#97346=CARTESIAN_POINT ( 'NONE',  ( 1.102447643272868261, 53.60738151370213700, 9.611086547314165784 ) ) ;
#97348=CARTESIAN_POINT ( 'NONE',  ( -36.94533202345532885, 28.08661236372360293, 11.10948794531283212 ) ) ;
#97356=CARTESIAN_POINT ( 'NONE',  ( 30.36467006388678769, 11.77175644674778354, 39.80053734054823167 ) ) ;
#97372=CARTESIAN_POINT ( 'NONE',  ( 6.390056616433401615, 51.65448240894459531, -6.607212291912419211 ) ) ;
#97392=FILL_AREA_STYLE_COLOUR ( '', #46027 ) ;
#97411=EDGE_CURVE ( 'NONE', #56430, #57955, #62759, .T. ) ;
#97436=DIRECTION ( 'NONE',  ( 0.000000000000000000, 1.000000000000000000, 0.000000000000000000 ) ) ;
#97437=CARTESIAN_POINT ( 'NONE',  ( 1.219356500951631173, 25.50065391225449574, -39.81801105826245646 ) ) ;
#97441=CARTESIAN_POINT ( 'NONE',  ( 0.7788225383843935257, 53.48454317400725699, -9.981205654210052458 ) ) ;
#97443=CARTESIAN_POINT ( 'NONE',  ( -1.249019603477211415, 34.73419941383219367, -28.17738922607452778 ) ) ;
#97446=ORIENTED_EDGE ( 'NONE', *, *, #19691, .F. ) ;
#97456=ORIENTED_EDGE ( 'NONE', *, *, #77389, .T. ) ;
#97458=EDGE_LOOP ( 'NONE', ( #99816, #62313, #74655, #82893, #42301, #84195, #27440, #26558 ) ) ;
#97467=ORIENTED_EDGE ( 'NONE', *, *, #96878, .T. ) ;
#97469=CARTESIAN_POINT ( 'NONE',  ( 0.000000000000000000, 41.79151656018385097, -22.55262289886175608 ) ) ;
#97470=CARTESIAN_POINT ( 'NONE',  ( 22.20562253605685044, 26.05647078817540674, 31.21756717792845137 ) ) ;
#97471=SURFACE_STYLE_USAGE ( .BOTH. , #99061 ) ;
#97480=CARTESIAN_POINT ( 'NONE',  ( 9.956561055908812463, 45.46170052629870639, -15.37429631330344471 ) ) ;
#97482=CIRCLE ( 'NONE', #27013, 56.32976553137783782 ) ;
#97487=EDGE_LOOP ( 'NONE', ( #59229, #32746, #28979, #20587 ) ) ;
#97516=CARTESIAN_POINT ( 'NONE',  ( -27.42575526752855808, 36.50017221940704815, -10.02597686312969572 ) ) ;
#97542=CARTESIAN_POINT ( 'NONE',  ( -46.78648606410043698, 13.65508681559504112, 15.44775621776469698 ) ) ;
#97553=FILL_AREA_STYLE ('',( #71689 ) ) ;
#97561=CARTESIAN_POINT ( 'NONE',  ( -0.3345794276167288750, 26.06210933331781376, 38.29266687495983490 ) ) ;
#97570=ORIENTED_EDGE ( 'NONE', *, *, #92479, .F. ) ;
#97586=VECTOR ( 'NONE', #13569, 1000.000000000000000 ) ;
#97595=CARTESIAN_POINT ( 'NONE',  ( 28.30697985939074357, 34.24750371692589823, -8.453642661119904034 ) ) ;
#97630=CARTESIAN_POINT ( 'NONE',  ( 36.80384673170812704, 28.12620022927966801, 11.20205233349968843 ) ) ;
#97634=CARTESIAN_POINT ( 'NONE',  ( 26.34381013455766052, 35.00016137052017484, -7.801548275680215916 ) ) ;
#97646=CARTESIAN_POINT ( 'NONE',  ( -29.32938745888669274, 18.70033273455118916, -39.65510828929056686 ) ) ;
#97647=SURFACE_STYLE_USAGE ( .BOTH. , #56660 ) ;
#97652=CARTESIAN_POINT ( 'NONE',  ( 23.21751746555303342, 25.98869614573808207, 30.70617127781016720 ) ) ;
#97661=CONICAL_SURFACE ( 'NONE', #59828, 23.23666318551310539, 1.221730476396026388 ) ;
#97670=CARTESIAN_POINT ( 'NONE',  ( 28.58254312158936727, 16.23466659877848528, -41.45958612840302493 ) ) ;
#97679=FILL_AREA_STYLE ('',( #56137 ) ) ;
#97684=FACE_OUTER_BOUND ( 'NONE', #67853, .T. ) ;
#97704=LINE ( 'NONE', #82600, #88925 ) ;
#97713=CARTESIAN_POINT ( 'NONE',  ( -5.457196206890739809, 53.44502160359606080, -8.522729681404539903 ) ) ;
#97714=CARTESIAN_POINT ( 'NONE',  ( 7.149395896920095848E-21, 27.29656849860388235, -40.75000000000000000 ) ) ;
#97722=ORIENTED_EDGE ( 'NONE', *, *, #20641, .T. ) ;
#97731=CARTESIAN_POINT ( 'NONE',  ( 1.219995453278951203, 43.50041496824643161, -17.81587387532546884 ) ) ;
#97736=COLOUR_RGB ( '', 0.40784314, 0.44705882, 0.49803922) ;
#97749=CARTESIAN_POINT ( 'NONE',  ( -23.13430097919831496, 28.13531915807118367, -30.70617127781035194 ) ) ;
#97753=ORIENTED_EDGE ( 'NONE', *, *, #61910, .F. ) ;
#97754=( GEOMETRIC_REPRESENTATION_CONTEXT ( 3 ) GLOBAL_UNCERTAINTY_ASSIGNED_CONTEXT ( ( #79562 ) ) GLOBAL_UNIT_ASSIGNED_CONTEXT ( ( #51343, #42194, #60534 ) ) REPRESENTATION_CONTEXT ( 'NONE', 'WORKASPACE' ) );
#97761=EDGE_CURVE ( 'NONE', #56223, #10253, #60270, .T. ) ;
#97779=AXIS2_PLACEMENT_3D ( 'NONE', #96677, #31956, #47576 ) ;
#97783=CARTESIAN_POINT ( 'NONE',  ( 0.8424608613547267533, 51.37392267887781117, -9.927074889301541916 ) ) ;
#97787=CARTESIAN_POINT ( 'NONE',  ( 0.000000000000000000, 56.87938524157181774, -0.6840402866513453084 ) ) ;
#97790=CARTESIAN_POINT ( 'NONE',  ( 49.27893332326006259, 7.918143476871231101, 15.56220613712076606 ) ) ;
#97840=AXIS2_PLACEMENT_3D ( 'NONE', #30319, #79375, #33917 ) ;
#97843=DIRECTION ( 'NONE',  ( -0.000000000000000000, -1.000000000000000000, -0.000000000000000000 ) ) ;
#97853=SURFACE_STYLE_USAGE ( .BOTH. , #15880 ) ;
#97857=FILL_AREA_STYLE_COLOUR ( '', #59602 ) ;
#97859=CARTESIAN_POINT ( 'NONE',  ( -23.38275356398436244, 25.95242394571446098, 30.70617127781060418 ) ) ;
#97867=SURFACE_STYLE_USAGE ( .BOTH. , #22433 ) ;
#97884=CARTESIAN_POINT ( 'NONE',  ( 1.126990790682043331, 54.02434422481241683, 8.453431372524891074 ) ) ;
#97898=FACE_BOUND ( 'NONE', #86961, .T. ) ;
#97910=EDGE_CURVE ( 'NONE', #43603, #101117, #61859, .T. ) ;
#97917=CYLINDRICAL_SURFACE ( 'NONE', #15441, 1.250000000000001110 ) ;
#97937=CARTESIAN_POINT ( 'NONE',  ( -1.250245718140553297, 43.55766156206008333, 17.65597227886197373 ) ) ;
#97938=UNCERTAINTY_MEASURE_WITH_UNIT (LENGTH_MEASURE( 1.000000000000000082E-05 ), #4038, 'distance_accuracy_value', 'NONE');
#97957=CARTESIAN_POINT ( 'NONE',  ( 16.58588328558601788, 34.28973238854128880, 24.30698433968584027 ) ) ;
#97973=DIRECTION ( 'NONE',  ( 0.000000000000000000, 1.000000000000000000, 0.000000000000000000 ) ) ;
#97992=CARTESIAN_POINT ( 'NONE',  ( -1.125072770816725631, 34.85036833913648735, -27.86405521226426529 ) ) ;
#98004=CARTESIAN_POINT ( 'NONE',  ( 46.89473120401049044, 12.86731181406132940, 16.16132821689873467 ) ) ;
#98012=ORIENTED_EDGE ( 'NONE', *, *, #101069, .F. ) ;
#98015=STYLED_ITEM ( 'NONE', ( #19326 ), #6315 ) ;
#98050=ORIENTED_EDGE ( 'NONE', *, *, #710, .F. ) ;
#98061=FILL_AREA_STYLE_COLOUR ( '', #56244 ) ;
#98062=CARTESIAN_POINT ( 'NONE',  ( -29.49662366984263073, 18.54149253525968177, 39.61409757040016189 ) ) ;
#98098=DIRECTION ( 'NONE',  ( 0.000000000000000000, 0.000000000000000000, 1.000000000000000000 ) ) ;
#98121=CARTESIAN_POINT ( 'NONE',  ( -17.37648585630541120, 34.80701782457118298, -21.96231721963981443 ) ) ;
#98124=CARTESIAN_POINT ( 'NONE',  ( -37.56673239365863282, 25.75719283951018568, -10.95617127781023648 ) ) ;
#98129=CARTESIAN_POINT ( 'NONE',  ( -28.73053610125101542, 13.62316949804204569, 40.04352587319202428 ) ) ;
#98136=CARTESIAN_POINT ( 'NONE',  ( 36.48035061666895018, 28.19748189396849725, -11.58222015087291012 ) ) ;
#98143=CARTESIAN_POINT ( 'NONE',  ( -36.74627714604517337, 26.01170350572267154, -11.25947311975635223 ) ) ;
#98146=CARTESIAN_POINT ( 'NONE',  ( 22.46054152223527467, 27.61307239794278345, 32.95409374511044831 ) ) ;
#98163=CIRCLE ( 'NONE', #24137, 35.82893434829263413 ) ;
#98173=ORIENTED_EDGE ( 'NONE', *, *, #27739, .T. ) ;
#98181=CARTESIAN_POINT ( 'NONE',  ( -28.98512335478656610, 9.657432045445705882, -41.89946025606985813 ) ) ;
#98183=VECTOR ( 'NONE', #93434, 1000.000000000000227 ) ;
#98199=EDGE_CURVE ( 'NONE', #35444, #68049, #65001, .T. ) ;
#98207=CARTESIAN_POINT ( 'NONE',  ( -7.199040112754230057E-19, 54.30758622938872549, -7.749999999999999112 ) ) ;
#98210=CARTESIAN_POINT ( 'NONE',  ( 28.88608732843768223, 18.87339843927420091, -39.88959139356639838 ) ) ;
#98220=ORIENTED_EDGE ( 'NONE', *, *, #19748, .F. ) ;
#98223=DIRECTION ( 'NONE',  ( 0.000000000000000000, 0.000000000000000000, 1.000000000000000000 ) ) ;
#98245=CARTESIAN_POINT ( 'NONE',  ( -6.390201886731505354, 51.65431772680223332, 6.607700835476884471 ) ) ;
#98256=CARTESIAN_POINT ( 'NONE',  ( 17.71899192986533222, 43.32325553723746481, -4.750071910800272690 ) ) ;
#98257=CARTESIAN_POINT ( 'NONE',  ( -6.518111695417504237, 53.49350304183202809, -7.567621837673542018 ) ) ;
#98267=SURFACE_SIDE_STYLE ('',( #9775 ) ) ;
#98294=CARTESIAN_POINT ( 'NONE',  ( -22.10829536976837417, 28.16405687208418129, -31.35662012625487804 ) ) ;
#98296=MECHANICAL_DESIGN_GEOMETRIC_PRESENTATION_REPRESENTATION('',(#31119),#84533);
#98331=CARTESIAN_POINT ( 'NONE',  ( 49.10020235979921921, 7.817788915495893498, 16.25178062802444146 ) ) ;
#98347=DIRECTION ( 'NONE',  ( 0.000000000000000000, 0.000000000000000000, -1.000000000000000000 ) ) ;
#98383=FACE_OUTER_BOUND ( 'NONE', #46269, .T. ) ;
#98385=CARTESIAN_POINT ( 'NONE',  ( -17.88790647107488496, 45.31130133375064872, -5.552611910813008755 ) ) ;
#98387=B_SPLINE_CURVE_WITH_KNOTS ( 'NONE', 3,
 ( #92668, #75419, #58169, #57620, #8555, #18826, #91095, #26392, #90546, #51670, #84590, #50590, #91622, #10672, #65741, #25867, #82984, #41456, #41987, #74868 ),
 .UNSPECIFIED., .F., .F.,
 ( 4, 2, 2, 2, 2, 2, 2, 2, 2, 4 ),
 ( 0.002921171163060745646, 0.003426533276933593948, 0.003931895390806442250, 0.004184576447742869437, 0.004437257504679297491, 0.004942619618552150998, 0.005447981732425004504, 0.005953343846297858011, 0.006458705960170712385, 0.006964068074043565891 ),
 .UNSPECIFIED. ) ;
#98389=ORIENTED_EDGE ( 'NONE', *, *, #2529, .F. ) ;
#98397=CARTESIAN_POINT ( 'NONE',  ( 1.217738148383409991, 51.81134339436971459, 8.675808517492017202 ) ) ;
#98398=FILL_AREA_STYLE ('',( #65510 ) ) ;
#98405=CARTESIAN_POINT ( 'NONE',  ( -11.24762705481934333, 45.31580660681511574, -14.96115168073767698 ) ) ;
#98408=LINE ( 'NONE', #64984, #89235 ) ;
#98410=CARTESIAN_POINT ( 'NONE',  ( 47.50581258546137065, 12.72782412601330115, -14.46700746232373369 ) ) ;
#98412=CARTESIAN_POINT ( 'NONE',  ( -36.49060748323162073, 28.04595687074818144, 12.86268870334000525 ) ) ;
#98415=CARTESIAN_POINT ( 'NONE',  ( 0.6452690800229740065, 53.45118871115546710, 10.08352034291727684 ) ) ;
#98417=CARTESIAN_POINT ( 'NONE',  ( 16.64348903516512834, -1.200000000000000030E-05, -5.407797401561770023 ) ) ;
#98422=CYLINDRICAL_SURFACE ( 'NONE', #77715, 1.250000000000001110 ) ;
#98424=CARTESIAN_POINT ( 'NONE',  ( -9.067040280756096138, 43.96870084527508027, 13.87029715775338801 ) ) ;
#98430=CARTESIAN_POINT ( 'NONE',  ( 0.000000000000000000, 36.79151656018385097, 0.000000000000000000 ) ) ;
#98445=CARTESIAN_POINT ( 'NONE',  ( -16.64348903516517098, 45.88445698070336221, 4.157797401561652784 ) ) ;
#98456=CARTESIAN_POINT ( 'NONE',  ( -1.220499935668712288, 25.50207722378707587, -39.81406367740636654 ) ) ;
#98464=CARTESIAN_POINT ( 'NONE',  ( 6.544664027967929343, 53.53201714234263164, 7.403362352172786487 ) ) ;
#98479=CARTESIAN_POINT ( 'NONE',  ( 16.41969624815436646, 35.05500855676915961, 21.84035938125508025 ) ) ;
#98488=PRESENTATION_STYLE_ASSIGNMENT (( #48866 ) ) ;
#98491=EDGE_CURVE ( 'NONE', #64333, #11951, #50833, .T. ) ;
#98493=ORIENTED_EDGE ( 'NONE', *, *, #6597, .F. ) ;
#98500=CARTESIAN_POINT ( 'NONE',  ( 9.177191262247363923, 46.16966304056472836, 13.55798985375333565 ) ) ;
#98504=AXIS2_PLACEMENT_3D ( 'NONE', #40530, #82585, #84189 ) ;
#98516=CARTESIAN_POINT ( 'NONE',  ( -0.4145836998305446053, 34.19552549475105963, -29.68225718326698370 ) ) ;
#98531=CARTESIAN_POINT ( 'NONE',  ( 23.21751746555220564, 25.25267828308493634, -33.20617127781077471 ) ) ;
#98551=CARTESIAN_POINT ( 'NONE',  ( -28.32689090366336160, 34.16882244950244996, -9.120241557729505288 ) ) ;
#98555=B_SPLINE_CURVE_WITH_KNOTS ( 'NONE', 3,
 ( #99527, #74716, #56935, #75249, #1350, #34312, #81209, #40237, #73112, #106018, #98464, #40764, #106559, #24618, #8157, #53202, #86121, #19815, #11118, #37587, #36527, #12722 ),
 .UNSPECIFIED., .F., .F.,
 ( 4, 2, 2, 2, 2, 2, 2, 2, 2, 2, 4 ),
 ( 0.003041022514278852139, 0.003544801402695308724, 0.003796690846903537017, 0.004048580291111764443, 0.004552359179528218426, 0.005056138067944675012, 0.005559916956361130730, 0.006063695844777587315, 0.006567474733194043901, 0.006819364177402275663, 0.007071253621610506558 ),
 .UNSPECIFIED. ) ;
#98569=FILL_AREA_STYLE ('',( #55967 ) ) ;
#98584=CARTESIAN_POINT ( 'NONE',  ( 29.49550841906154375, 18.54274624009278583, 39.61427208276940348 ) ) ;
#98585=CARTESIAN_POINT ( 'NONE',  ( 22.43826451847985837, 28.20713089197013446, -30.97515248374633146 ) ) ;
#98590=CARTESIAN_POINT ( 'NONE',  ( -16.64348903516521005, 43.47556584774768140, -6.657797401561535544 ) ) ;
#98592=CARTESIAN_POINT ( 'NONE',  ( -22.07885140346273900, 26.01882032652172327, 31.43383091546978036 ) ) ;
#98599=CARTESIAN_POINT ( 'NONE',  ( -48.02835407290515946, 14.94086294439721030, 16.85535821593516559 ) ) ;
#98606=CARTESIAN_POINT ( 'NONE',  ( -26.49116892277528024, 34.70576323815743081, 9.907392575990456862 ) ) ;
#98616=STYLED_ITEM ( 'NONE', ( #2543 ), #83469 ) ;
#98622=CARTESIAN_POINT ( 'NONE',  ( 8.719144900081944982, 53.90630142508563694, 1.531152949374442462 ) ) ;
#98629=CARTESIAN_POINT ( 'NONE',  ( -30.90153257058555170, 13.61190038887007248, 41.14606609713253249 ) ) ;
#98630=CARTESIAN_POINT ( 'NONE',  ( -0.4139846110599526008, 25.19206125174364175, 40.68244515147750917 ) ) ;
#98631=CARTESIAN_POINT ( 'NONE',  ( 0.8405003012203439150, 27.41029791806389326, -40.42883694400927652 ) ) ;
#98642=CARTESIAN_POINT ( 'NONE',  ( -17.89171299917695279, 43.20822152669683902, 5.300773039380033858 ) ) ;
#98644=CARTESIAN_POINT ( 'NONE',  ( 48.02835407290544367, 14.94086294439726892, 16.85535821593427386 ) ) ;
#98678=CARTESIAN_POINT ( 'NONE',  ( -4.647051454204487619, 54.31004531717275796, 6.195923535874935162 ) ) ;
#98701=CARTESIAN_POINT ( 'NONE',  ( 38.31547885847380286, 25.47151378724775839, 11.19247416203105416 ) ) ;
#98706=CARTESIAN_POINT ( 'NONE',  ( -28.43348347353486005, 17.76907357228462558, -40.77956405912765803 ) ) ;
#98712=CARTESIAN_POINT ( 'NONE',  ( 23.78270938940518420, 25.17287789278546128, 33.07427373539508864 ) ) ;
#98721=CARTESIAN_POINT ( 'NONE',  ( -5.123687866623413356, 51.38063399059588932, 8.522745146031866170 ) ) ;
#98740=B_SPLINE_CURVE_WITH_KNOTS ( 'NONE', 3,
 ( #81396, #24276, #57129, #16146, #40963, #73851, #32895, #101332, #68978, #77047, #11234, #67895, #76509, #3163, #75448, #26419, #34508, #101852, #2617, #84616, #100256, #59819 ),
 .UNSPECIFIED., .F., .F.,
 ( 4, 2, 2, 2, 2, 2, 2, 2, 2, 2, 4 ),
 ( 0.007079440862166612621, 0.007331525063779767253, 0.007583609265392921885, 0.008087777668619232016, 0.008339861870232388383, 0.008591946071845546484, 0.009096114475071866157, 0.009600282878298185829, 0.01010445128152450724, 0.01060861968475082691, 0.01111278808797714832 ),
 .UNSPECIFIED. ) ;
#98773=CARTESIAN_POINT ( 'NONE',  ( -24.47192364801391662, 27.44308780173428985, -32.07880713851005083 ) ) ;
#98794=CARTESIAN_POINT ( 'NONE',  ( -37.72755895515653890, 25.42103013220621577, 13.45617127781066280 ) ) ;
#98799=VECTOR ( 'NONE', #76551, 1000.000000000000000 ) ;
#98808=LINE ( 'NONE', #27105, #33981 ) ;
#98810=CARTESIAN_POINT ( 'NONE',  ( -22.80797863425463490, 28.18718824344973228, -30.77216081686040283 ) ) ;
#98824=CARTESIAN_POINT ( 'NONE',  ( 38.81129420777568839, 27.30432117811967530, -12.34979214484390475 ) ) ;
#98830=ORIENTED_EDGE ( 'NONE', *, *, #105476, .T. ) ;
#98834=CARTESIAN_POINT ( 'NONE',  ( 0.6419170815367052363, 35.01568727531654446, -27.42424321200550352 ) ) ;
#98845=CARTESIAN_POINT ( 'NONE',  ( 0.7854637262267426534, 43.26570879096288280, 18.48601689480677734 ) ) ;
#98888=VERTEX_POINT ( 'NONE', #98445 ) ;
#98900=CARTESIAN_POINT ( 'NONE',  ( 23.21751746555303342, -1.200000000000000030E-05, 31.95617127781017075 ) ) ;
#98901=AXIS2_PLACEMENT_3D ( 'NONE', #89654, #15755, #82620 ) ;
#98902=ORIENTED_EDGE ( 'NONE', *, *, #10751, .T. ) ;
#98910=CARTESIAN_POINT ( 'NONE',  ( -0.4138759434715034158, 44.05905633758010964, -16.31753750977479811 ) ) ;
#98916=CARTESIAN_POINT ( 'NONE',  ( 0.5340534162559666953, 13.17884539425582346, -51.63681601966053591 ) ) ;
#98917=EDGE_LOOP ( 'NONE', ( #70432, #33795 ) ) ;
#98925=CARTESIAN_POINT ( 'NONE',  ( -36.35825146749015602, 28.12716662175846949, 12.56482682837719977 ) ) ;
#98928=CARTESIAN_POINT ( 'NONE',  ( 9.491091496279695579E-16, 54.30758622938872549, 7.749999999999999112 ) ) ;
#98930=CARTESIAN_POINT ( 'NONE',  ( -16.34909811654727818, 34.35725799356371368, -24.24308462023440214 ) ) ;
#98936=ORIENTED_EDGE ( 'NONE', *, *, #6733, .F. ) ;
#98937=CARTESIAN_POINT ( 'NONE',  ( 30.63590201688485593, 10.93049107008198817, 40.03749794393651484 ) ) ;
#98940=CARTESIAN_POINT ( 'NONE',  ( 8.717352708370867731, 51.77858799192747341, -1.531152949374622985 ) ) ;
#98961=FACE_OUTER_BOUND ( 'NONE', #3349, .T. ) ;
#99009=FACE_OUTER_BOUND ( 'NONE', #52268, .T. ) ;
#99022=CARTESIAN_POINT ( 'NONE',  ( 10.20373343965789381, 45.40217293244036512, 15.40779740156149735 ) ) ;
#99033=CARTESIAN_POINT ( 'NONE',  ( 0.6428726534874711351, 53.45391827455260625, -10.07519478865332196 ) ) ;
#99043=EDGE_LOOP ( 'NONE', ( #28207, #25421, #51564, #103869 ) ) ;
#99050=CARTESIAN_POINT ( 'NONE',  ( 23.38273396131690518, 25.95242824884117283, -30.70617127781076405 ) ) ;
#99055=ORIENTED_EDGE ( 'NONE', *, *, #78805, .T. ) ;
#99058=CARTESIAN_POINT ( 'NONE',  ( 22.57676703600024837, 26.08017106655005790, 30.86991111420691425 ) ) ;
#99061=SURFACE_SIDE_STYLE ('',( #16035 ) ) ;
#99067=ORIENTED_EDGE ( 'NONE', *, *, #20641, .F. ) ;
#99078=CARTESIAN_POINT ( 'NONE',  ( -28.35171477237968318, 34.21495322681006712, -8.616345005959455960 ) ) ;
#99093=CARTESIAN_POINT ( 'NONE',  ( 0.1546360390246568628, 18.85543002168095938, 49.25752556588032860 ) ) ;
#99094=EDGE_CURVE ( 'NONE', #45425, #50509, #76829, .T. ) ;
#99099=DIRECTION ( 'NONE',  ( 0.000000000000000000, -0.3420201433256725987, -0.9396926207859068736 ) ) ;
#99103=EDGE_CURVE ( 'NONE', #66879, #79335, #22428, .T. ) ;
#99127=CYLINDRICAL_SURFACE ( 'NONE', #97840, 1.250000000000001110 ) ;
#99130=CARTESIAN_POINT ( 'NONE',  ( 11.29895642217514684, 43.19531110207578450, -14.89530219903277519 ) ) ;
#99143=CARTESIAN_POINT ( 'NONE',  ( -47.57472544752269528, 12.59044387134402321, 14.43844179794134952 ) ) ;
#99152=CARTESIAN_POINT ( 'NONE',  ( 9.317657253014628438, 53.46886534697259918, 3.778385012062984050 ) ) ;
#99159=CARTESIAN_POINT ( 'NONE',  ( -30.80732993440543410, 13.24159032961888549, 41.41050123719129772 ) ) ;
#99167=ORIENTED_EDGE ( 'NONE', *, *, #34551, .F. ) ;
#99174=CARTESIAN_POINT ( 'NONE',  ( 48.55387420720872171, 13.84642135131330853, 16.74239769522738897 ) ) ;
#99185=CARTESIAN_POINT ( 'NONE',  ( 9.169967954764700835, 51.60694363734955914, 1.678936458957752009 ) ) ;
#99218=CARTESIAN_POINT ( 'NONE',  ( 15.54899369231023343, 44.07947967433609904, -4.780801059126263297 ) ) ;
#99243=CARTESIAN_POINT ( 'NONE',  ( 23.85631536739324332, 25.16912815653500246, 33.03393598700190381 ) ) ;
#99246=CARTESIAN_POINT ( 'NONE',  ( 5.290067270632322405, 53.47475093287481940, 8.531152949374478212 ) ) ;
#99265=ORIENTED_EDGE ( 'NONE', *, *, #3930, .T. ) ;
#99266=CARTESIAN_POINT ( 'NONE',  ( 0.000000000000000000, 1.999999999999998224, 0.000000000000000000 ) ) ;
#99278=ADVANCED_FACE ( 'NONE', ( #25544, #26084 ), #100979, .T. ) ;
#99306=CARTESIAN_POINT ( 'NONE',  ( -23.29992259251663711, 27.36384728240174979, 33.20617127781060418 ) ) ;
#99320=CARTESIAN_POINT ( 'NONE',  ( 16.75187969033571989, 36.38380281757302726, 24.30698433968583316 ) ) ;
#99323=CARTESIAN_POINT ( 'NONE',  ( -38.81120307428947314, 25.17591441068872982, 12.35054225871727596 ) ) ;
#99330=EDGE_CURVE ( 'NONE', #653, #25026, #68085, .T. ) ;
#99338=CARTESIAN_POINT ( 'NONE',  ( 16.75187969033441604, 36.38380281757147827, -24.30698433969211791 ) ) ;
#99367=CARTESIAN_POINT ( 'NONE',  ( 7.312797294236363932, 52.12749630495425635, 2.972055287740744234 ) ) ;
#99383=CYLINDRICAL_SURFACE ( 'NONE', #35837, 1.250000000000001110 ) ;
#99386=CARTESIAN_POINT ( 'NONE',  ( 9.034543481159971634, 43.90162183362577508, -14.11077590592769049 ) ) ;
#99392=VECTOR ( 'NONE', #8879, 1000.000000000000227 ) ;
#99424=CARTESIAN_POINT ( 'NONE',  ( 15.39052280876485668, 44.08006356674551540, 5.263393437970842470 ) ) ;
#99430=DIRECTION ( 'NONE',  ( 0.000000000000000000, 0.000000000000000000, 1.000000000000000000 ) ) ;
#99431=PRESENTATION_STYLE_ASSIGNMENT (( #63923 ) ) ;
#99433=ORIENTED_EDGE ( 'NONE', *, *, #95627, .F. ) ;
#99454=CARTESIAN_POINT ( 'NONE',  ( 0.3605712710638133145, 13.03532800917887258, -51.69843826998983616 ) ) ;
#99467=CARTESIAN_POINT ( 'NONE',  ( -15.76179818182182224, 34.59899376685505246, -23.83662882038466080 ) ) ;
#99479=CARTESIAN_POINT ( 'NONE',  ( 5.623226095793158130, 51.29171802761456433, 8.497680151582294172 ) ) ;
#99523=( GEOMETRIC_REPRESENTATION_CONTEXT ( 3 ) GLOBAL_UNCERTAINTY_ASSIGNED_CONTEXT ( ( #72859 ) ) GLOBAL_UNIT_ASSIGNED_CONTEXT ( ( #77263, #102059, #86445 ) ) REPRESENTATION_CONTEXT ( 'NONE', 'WORKASPACE' ) );
#99527=CARTESIAN_POINT ( 'NONE',  ( 5.290067270632322405, 53.47475093287481940, 8.531152949374478212 ) ) ;
#99529=ORIENTED_EDGE ( 'NONE', *, *, #63865, .T. ) ;
#99537=EDGE_CURVE ( 'NONE', #53305, #67639, #32728, .T. ) ;
#99573=CARTESIAN_POINT ( 'NONE',  ( 0.1695342223295464856, 53.40043206617340843, -10.24131878858624844 ) ) ;
#99578=CARTESIAN_POINT ( 'NONE',  ( 7.315107926653602988, 54.29845173462179986, 2.635958794940676864 ) ) ;
#99585=ORIENTED_EDGE ( 'NONE', *, *, #79895, .F. ) ;
#99590=CARTESIAN_POINT ( 'NONE',  ( 46.92822048327062845, 13.65838325462198277, 15.00718171297847015 ) ) ;
#99620=CARTESIAN_POINT ( 'NONE',  ( -28.31435381911579441, 34.24534108781838171, -8.450334191970046760 ) ) ;
#99625=ORIENTED_EDGE ( 'NONE', *, *, #49313, .T. ) ;
#99627=( NAMED_UNIT ( * ) PLANE_ANGLE_UNIT ( ) SI_UNIT ( $, .RADIAN. ) );
#99636=ADVANCED_FACE ( 'NONE', ( #92210 ), #57712, .F. ) ;
#99640=CARTESIAN_POINT ( 'NONE',  ( 18.00376551885534582, 36.46870192104551478, -23.09987717863831946 ) ) ;
#99645=CARTESIAN_POINT ( 'NONE',  ( 15.76058568550410222, 34.59977121747715501, -23.83486895696631436 ) ) ;
#99647=( NAMED_UNIT ( * ) PLANE_ANGLE_UNIT ( ) SI_UNIT ( $, .RADIAN. ) );
#99654=CLOSED_SHELL ( 'NONE', ( #16277, #7853, #37977, #83469, #95420, #6315, #64108, #82778, #45279, #3886, #10508, #92066, #73803, #22488, #66937, #24760, #56276, #97074, #62053, #3855, #64164, #67118, #63566, #91858, #52510, #51627, #50486, #63298, #52434, #84617, #77775, #59141, #40131, #41549, #53370, #210, #12836, #100114, #104728, #19158, #42201, #59058, #7393, #13822, #36367, #75676, #95905, #41346, #15641, #91347, #71773, #91602, #9632, #23020, #37090, #929, #79784, #25103, #35910, #34285, #106130, #60091, #92914, #23511, #51402, #37502, #45084, #60442, #62809, #40392, #8347, #75360, #92732, #36964, #40217, #29030, #99278, #48315, #94653, #51083, #37782, #66323, #82422, #92322, #84437, #2163, #21074, #103796, #71881, #1611, #95203, #51962, #31006, #102736, #57681, #85152, #31924, #23944, #21810, #46117, #13026, #37891, #90915, #99636, #42426, #80013, #49987, #25527, #42019, #41857, #88434, #76497, #37228, #56122, #65896, #9182, #69567, #88186, #70943, #19142, #83685, #58526, #9022, #95383, #50038, #2836, #1263, #48764, #7067, #81287, #87330, #63047, #27291, #17835, #52620, #29969 ) ) ;
#99658=CARTESIAN_POINT ( 'NONE',  ( -29.09597697838586683, 14.54318144277621982, 41.96748357178371691 ) ) ;
#99668=SURFACE_STYLE_USAGE ( .BOTH. , #41961 ) ;
#99676=DIRECTION ( 'NONE',  ( 1.150791560227848297E-16, -0.3420201433256725987, 0.9396926207859068736 ) ) ;
#99688=CARTESIAN_POINT ( 'NONE',  ( -17.62428443205143580, 45.49731502040739883, 4.616218165345990165 ) ) ;
#99695=CARTESIAN_POINT ( 'NONE',  ( 9.307364947981332293, 53.68040549777599324, 1.766710806768802877 ) ) ;
#99697=CARTESIAN_POINT ( 'NONE',  ( 16.32302039041864106, 45.99487210642904955, -4.188696036804095080 ) ) ;
#99698=( NAMED_UNIT ( * ) PLANE_ANGLE_UNIT ( ) SI_UNIT ( $, .RADIAN. ) );
#99699=COLOUR_RGB ( '', 0.31764706, 0.68627451, 0.89019608) ;
#99710=VECTOR ( 'NONE', #59619, 1000.000000000000000 ) ;
#99720=CARTESIAN_POINT ( 'NONE',  ( -17.95923320562059899, 34.46585161348816229, -22.69639360600545430 ) ) ;
#99722=CARTESIAN_POINT ( 'NONE',  ( -6.069123655689745434, 51.26876736100241772, -8.262300084537509193 ) ) ;
#99730=MECHANICAL_DESIGN_GEOMETRIC_PRESENTATION_REPRESENTATION('',(#56600),#67026);
#99735=CARTESIAN_POINT ( 'NONE',  ( 9.499542073392305497, 51.30140843018365615, 3.609232774367274299 ) ) ;
#99738=ORIENTED_EDGE ( 'NONE', *, *, #10199, .F. ) ;
#99743=CARTESIAN_POINT ( 'NONE',  ( -17.62458197301598162, 43.36883309418347920, -4.616457421087988955 ) ) ;
#99744=CARTESIAN_POINT ( 'NONE',  ( -1.218394774668507763, 45.86026819846987479, -17.17834643895785263 ) ) ;
#99754=CARTESIAN_POINT ( 'NONE',  ( 3.636386562469240082E-15, 36.30024107553216339, 29.75000000000000355 ) ) ;
#99765=CARTESIAN_POINT ( 'NONE',  ( 15.66131014786430242, 43.86972238223016518, -6.197328158278672561 ) ) ;
#99779=B_SPLINE_CURVE_WITH_KNOTS ( 'NONE', 3,
 ( #45181, #35509, #61362, #85638, #11711, #53260, #10649, #68388, #101799, #19875, #94255, #69450, #27965, #43043, #18250, #52710, #34978, #60830, #18803, #100204 ),
 .UNSPECIFIED., .F., .F.,
 ( 4, 2, 2, 2, 2, 2, 2, 2, 2, 4 ),
 ( 0.007223778813970589859, 0.007727726098206796727, 0.008231673382443002729, 0.008735620666679209598, 0.009239567950915416467, 0.009743515235151623335, 0.01024746251938783020, 0.01049943616150593451, 0.01075140980362403881, 0.01125535708786024047 ),
 .UNSPECIFIED. ) ;
#99795=CARTESIAN_POINT ( 'NONE',  ( 5.126025408076855250, 54.24534041977454280, 6.039183340882647855 ) ) ;
#99816=ORIENTED_EDGE ( 'NONE', *, *, #6597, .T. ) ;
#99825=CARTESIAN_POINT ( 'NONE',  ( -1.484885661199817548E-13, 25.16821295365152622, -40.75000000000150635 ) ) ;
#99846=CARTESIAN_POINT ( 'NONE',  ( -0.3340761435813103253, 37.19397736156746959, -27.29255811281833033 ) ) ;
#99852=CARTESIAN_POINT ( 'NONE',  ( -9.955499077880663350, 44.05779190055731220, -12.94048145135424299 ) ) ;
#99853=CARTESIAN_POINT ( 'NONE',  ( -23.21751746555168339, 27.38103382803512176, 33.20617127781681432 ) ) ;
#99866=LINE ( 'NONE', #64847, #100289 ) ;
#99869=CARTESIAN_POINT ( 'NONE',  ( -48.69610342378912549, 8.416294429711154379, -16.66514711139025806 ) ) ;
#99885=CARTESIAN_POINT ( 'NONE',  ( 26.03569976539403186, 37.04610443471195680, -9.459197729484262851 ) ) ;
#99912=CARTESIAN_POINT ( 'NONE',  ( 29.68315524076959377, 13.12249633091058243, -39.60535821593525441 ) ) ;
#99917=ORIENTED_EDGE ( 'NONE', *, *, #16465, .F. ) ;
#99930=CARTESIAN_POINT ( 'NONE',  ( -9.554774132531640873, 51.29119502155290178, -3.542050502601651552 ) ) ;
#99932=CARTESIAN_POINT ( 'NONE',  ( 37.56673239365870387, 25.47613764497372557, 13.45617127780999134 ) ) ;
#99940=VECTOR ( 'NONE', #11115, 1000.000000000000000 ) ;
#99945=EDGE_CURVE ( 'NONE', #85904, #65856, #82745, .T. ) ;
#99950=CARTESIAN_POINT ( 'NONE',  ( -15.43483729484961842, 44.00314096588699897, 5.765889254525177421 ) ) ;
#99960=ORIENTED_EDGE ( 'NONE', *, *, #59012, .T. ) ;
#99965=CARTESIAN_POINT ( 'NONE',  ( 7.481431019367137836, 52.00404499236192635, -3.434350709771399224 ) ) ;
#99973=CARTESIAN_POINT ( 'NONE',  ( -48.60160210973805306, 15.38206115941372865, 14.48795722268544672 ) ) ;
#99987=CARTESIAN_POINT ( 'NONE',  ( -0.5285977877722420892, 18.60303940554467772, 49.36091255612689110 ) ) ;
#99996=CARTESIAN_POINT ( 'NONE',  ( 0.1551307017114974263, 12.93301843199755297, -51.74240478515310571 ) ) ;
#100003=ORIENTED_EDGE ( 'NONE', *, *, #34461, .F. ) ;
#100015=SURFACE_STYLE_FILL_AREA ( #42309 ) ;
#100028=( GEOMETRIC_REPRESENTATION_CONTEXT ( 3 ) GLOBAL_UNCERTAINTY_ASSIGNED_CONTEXT ( ( #49481 ) ) GLOBAL_UNIT_ASSIGNED_CONTEXT ( ( #1970, #41907, #41378 ) ) REPRESENTATION_CONTEXT ( 'NONE', 'WORKASPACE' ) );
#100037=CARTESIAN_POINT ( 'NONE',  ( -37.24632233508901891, 27.99432795351219738, -10.98715164801380517 ) ) ;
#100060=LINE ( 'NONE', #89851, #10380 ) ;
#100064=CARTESIAN_POINT ( 'NONE',  ( -10.28624191511820207, -1.200000000000000030E-05, 14.15779740156163946 ) ) ;
#100069=CARTESIAN_POINT ( 'NONE',  ( 30.92841573401205579, 13.86971257847474703, 40.99043602818870369 ) ) ;
#100078=CARTESIAN_POINT ( 'NONE',  ( 0.6452404136000341461, 27.35540082825626484, 40.58352349220777455 ) ) ;
#100079=CARTESIAN_POINT ( 'NONE',  ( -30.36467006388648926, 11.77175644674776223, -39.80053734054845904 ) ) ;
#100086=CARTESIAN_POINT ( 'NONE',  ( 8.559508646656103892, 51.55638410492932167, -4.031152949375861105 ) ) ;
#100114=ADVANCED_FACE ( 'NONE', ( #97310 ), #15868, .F. ) ;
#100116=CARTESIAN_POINT ( 'NONE',  ( -8.880059686752383996, 53.58371679781946995, -4.000342112176812570 ) ) ;
#100117=UNCERTAINTY_MEASURE_WITH_UNIT (LENGTH_MEASURE( 1.000000000000000082E-05 ), #49829, 'distance_accuracy_value', 'NONE');
#100119=CARTESIAN_POINT ( 'NONE',  ( -10.28624191511830155, -1.200000000000000030E-05, -14.15779740156157018 ) ) ;
#100127=ORIENTED_EDGE ( 'NONE', *, *, #91496, .F. ) ;
#100130=CARTESIAN_POINT ( 'NONE',  ( 23.86066917533285192, 25.16615122465923093, -33.04118181549677757 ) ) ;
#100138=EDGE_LOOP ( 'NONE', ( #69882, #62767, #63543, #1360 ) ) ;
#100142=CARTESIAN_POINT ( 'NONE',  ( -36.31983699975081237, 26.03207335590308347, -12.39576754523718272 ) ) ;
#100158=CARTESIAN_POINT ( 'NONE',  ( 17.73948671138767352, 45.30893932440047678, -6.031879864029628280 ) ) ;
#100173=CARTESIAN_POINT ( 'NONE',  ( 17.16184658094818261, 36.31812281971417633, -24.24086490087793067 ) ) ;
#100191=PRESENTATION_STYLE_ASSIGNMENT (( #67310 ) ) ;
#100204=CARTESIAN_POINT ( 'NONE',  ( 4.988960626530190971E-15, 27.29656849860388235, 40.75000000000000000 ) ) ;
#100206=ORIENTED_EDGE ( 'NONE', *, *, #90249, .T. ) ;
#100209=VERTEX_POINT ( 'NONE', #25601 ) ;
#100221=EDGE_LOOP ( 'NONE', ( #27057, #87822, #63769, #23221, #92931, #58058, #22659, #65713 ) ) ;
#100224=CARTESIAN_POINT ( 'NONE',  ( 9.773125458951499311, 53.39756354753611589, 3.092076115194700492 ) ) ;
#100228=FACE_OUTER_BOUND ( 'NONE', #105648, .T. ) ;
#100232=FACE_OUTER_BOUND ( 'NONE', #60559, .T. ) ;
#100256=CARTESIAN_POINT ( 'NONE',  ( -10.45150921522485632, 43.95515046479253130, -12.90779740156153821 ) ) ;
#100263=VECTOR ( 'NONE', #64067, 1000.000000000000000 ) ;
#100282=CARTESIAN_POINT ( 'NONE',  ( 0.7770801399229583240, 37.10885713635266825, 27.51745571163628412 ) ) ;
#100287=CARTESIAN_POINT ( 'NONE',  ( 0.000000000000000000, 2.000000000000000000, 63.00000000000000000 ) ) ;
#100289=VECTOR ( 'NONE', #41636, 1000.000000000000000 ) ;
#100297=ORIENTED_EDGE ( 'NONE', *, *, #77308, .F. ) ;
#100304=CARTESIAN_POINT ( 'NONE',  ( 48.02835407290544367, -1.200000000000000030E-05, 15.60535821593427563 ) ) ;
#100313=( NAMED_UNIT ( * ) SI_UNIT ( $, .STERADIAN. ) SOLID_ANGLE_UNIT ( ) );
#100315=ORIENTED_EDGE ( 'NONE', *, *, #34551, .T. ) ;
#100323=CARTESIAN_POINT ( 'NONE',  ( 4.881448269507570714, 54.28580602658091436, 6.096853558198860767 ) ) ;
#100325=ORIENTED_EDGE ( 'NONE', *, *, #53315, .T. ) ;
#100327=CARTESIAN_POINT ( 'NONE',  ( 28.19909662334077538, 36.30566500375478967, 9.434792300628540573 ) ) ;
#100328=CARTESIAN_POINT ( 'NONE',  ( -5.290067270632216712, 52.08006895350504095, 6.031152949374556371 ) ) ;
#100329=AXIS2_PLACEMENT_3D ( 'NONE', #6476, #103594, #22709 ) ;
#100332=CARTESIAN_POINT ( 'NONE',  ( 30.80770627799282124, 8.073552547385910216, -41.40953488888267486 ) ) ;
#100333=CARTESIAN_POINT ( 'NONE',  ( -23.21751746555244722, -1.200000000000000030E-05, 31.95617127781060773 ) ) ;
#100342=( NAMED_UNIT ( * ) SI_UNIT ( $, .STERADIAN. ) SOLID_ANGLE_UNIT ( ) );
#100346=VERTEX_POINT ( 'NONE', #101575 ) ;
#100370=CARTESIAN_POINT ( 'NONE',  ( -5.623754609091350609, 51.29168761065961490, 8.497413747174256571 ) ) ;
#100377=CARTESIAN_POINT ( 'NONE',  ( -0.1682053726333464228, 36.30024107553215629, -29.75000000000000711 ) ) ;
#100381=LINE ( 'NONE', #10304, #106289 ) ;
#100383=EDGE_CURVE ( 'NONE', #17567, #29960, #85947, .T. ) ;
#100385=PRESENTATION_STYLE_ASSIGNMENT (( #67503 ) ) ;
#100415=CARTESIAN_POINT ( 'NONE',  ( 26.12851586566475248, 36.99786746614248045, -9.591385120608638459 ) ) ;
#100426=CARTESIAN_POINT ( 'NONE',  ( -16.64348903516521005, -1.200000000000000030E-05, -5.407797401561534656 ) ) ;
#100429=SURFACE_SIDE_STYLE ('',( #84790 ) ) ;
#100450=CARTESIAN_POINT ( 'NONE',  ( 7.945231034609332887, 51.78157138488628419, 3.881274660011450717 ) ) ;
#100452=FILL_AREA_STYLE ('',( #44353 ) ) ;
#100468=CARTESIAN_POINT ( 'NONE',  ( 9.108175880970147631, 43.74195033122234122, -14.58320101129880975 ) ) ;
#100472=EDGE_CURVE ( 'NONE', #17653, #59863, #79934, .T. ) ;
#100479=CARTESIAN_POINT ( 'NONE',  ( -16.02226691200762332, 43.96107415247629291, 4.310996538645964549 ) ) ;
#100496=CARTESIAN_POINT ( 'NONE',  ( -1.012387302972281189, 27.47360406062330185, -40.25103504401613463 ) ) ;
#100497=VERTEX_POINT ( 'NONE', #39505 ) ;
#100502=CARTESIAN_POINT ( 'NONE',  ( 48.02835407290504577, -1.200000000000000030E-05, -14.35535821593549954 ) ) ;
#100514=DIRECTION ( 'NONE',  ( -0.000000000000000000, 1.000000000000000000, -0.000000000000000000 ) ) ;
#100516=CARTESIAN_POINT ( 'NONE',  ( -4.152276560052219345, 52.11353348511973849, -6.756903599530849291 ) ) ;
#100521=CARTESIAN_POINT ( 'NONE',  ( -26.02888215231238789, 34.91958502330739833, -9.463828569828224957 ) ) ;
#100531=CARTESIAN_POINT ( 'NONE',  ( -46.78679791479559213, 18.82552674760556144, -15.44534812371305144 ) ) ;
#100535=CARTESIAN_POINT ( 'NONE',  ( -36.95390076149564607, 27.83275904791154431, 13.30708510620654472 ) ) ;
#100539=CARTESIAN_POINT ( 'NONE',  ( -16.75187969033531132, 34.25544727262101219, -24.30698433968676753 ) ) ;
#100546=CARTESIAN_POINT ( 'NONE',  ( -48.02835407290516656, 16.78162100668608048, 14.35535821593516559 ) ) ;
#100548=EDGE_CURVE ( 'NONE', #88217, #88418, #8030, .T. ) ;
#100549=CARTESIAN_POINT ( 'NONE',  ( 9.686686328283677483, 51.27217407866643129, -3.328097068059955976 ) ) ;
#100550=DIRECTION ( 'NONE',  ( 0.000000000000000000, 1.000000000000000000, -0.000000000000000000 ) ) ;
#100564=ORIENTED_EDGE ( 'NONE', *, *, #80510, .F. ) ;
#100565=DIRECTION ( 'NONE',  ( -0.000000000000000000, 1.000000000000000000, -0.000000000000000000 ) ) ;
#100567=CARTESIAN_POINT ( 'NONE',  ( -36.47314689784992225, 28.20057725235767876, -11.57774245207459707 ) ) ;
#100587=CARTESIAN_POINT ( 'NONE',  ( 38.81815223091233946, 25.18283608031790877, -12.26568976353609131 ) ) ;
#100601=CARTESIAN_POINT ( 'NONE',  ( 30.82452621380425484, 13.29951192218422484, 41.36733700123890145 ) ) ;
#100603=SURFACE_STYLE_USAGE ( .BOTH. , #33774 ) ;
#100610=CARTESIAN_POINT ( 'NONE',  ( 0.7771955416098277336, 28.10628302878886586, 38.51754525846273225 ) ) ;
#100631=SURFACE_STYLE_FILL_AREA ( #102234 ) ;
#100634=EDGE_CURVE ( 'NONE', #68832, #90588, #42134, .T. ) ;
#100647=UNCERTAINTY_MEASURE_WITH_UNIT (LENGTH_MEASURE( 1.000000000000000082E-05 ), #64892, 'distance_accuracy_value', 'NONE');
#100655=CARTESIAN_POINT ( 'NONE',  ( -16.11359103326322995, 37.20915759416860880, -21.97891983235047775 ) ) ;
#100660=CARTESIAN_POINT ( 'NONE',  ( 23.97884343762943615, 25.74916088538413561, -30.95222414396502941 ) ) ;
#100671=DIRECTION ( 'NONE',  ( 0.000000000000000000, 0.000000000000000000, -1.000000000000000000 ) ) ;
#100676=ORIENTED_EDGE ( 'NONE', *, *, #33140, .F. ) ;
#100679=CARTESIAN_POINT ( 'NONE',  ( 0.000000000000000000, 47.77514352166374323, -11.96035173608223090 ) ) ;
#100712=CARTESIAN_POINT ( 'NONE',  ( 22.88454736421187263, 28.18015032983889867, -30.73969532942466998 ) ) ;
#100714=EDGE_CURVE ( 'NONE', #18144, #14145, #97482, .T. ) ;
#100716=FACE_BOUND ( 'NONE', #105052, .T. ) ;
#100740=VERTEX_POINT ( 'NONE', #49697 ) ;
#100741=CARTESIAN_POINT ( 'NONE',  ( -7.350202751404733448, 54.21988909062471862, -3.137162962828702106 ) ) ;
#100744=CARTESIAN_POINT ( 'NONE',  ( -16.64348903516521005, -1.200000000000000030E-05, -6.657797401561535544 ) ) ;
#100746=EDGE_LOOP ( 'NONE', ( #24195, #46472, #75608, #43509 ) ) ;
#100784=B_SPLINE_CURVE_WITH_KNOTS ( 'NONE', 3,
 ( #45508, #47062, #71343, #39535, #5034, #14690, #71876, #96698, #103719, #72412, #22835, #21773, #62744, #31458, #104782, #55667, #88604, #86511, #54608, #30388, #54086, #103199, #29345, #53579, #20742, #30930, #47592, #14159, #5552, #38479 ),
 .UNSPECIFIED., .F., .F.,
 ( 4, 2, 2, 2, 2, 2, 2, 2, 2, 2, 2, 2, 2, 2, 4 ),
 ( 0.01188303771272565881, 0.01280230725828810680, 0.01326194203106932298, 0.01372157680385054090, 0.01418121157663175709, 0.01441102896302235911, 0.01464084634941296287, 0.01487066373580356662, 0.01510048112219417038, 0.01556011589497537442, 0.01601975066775657847, 0.01647938544053778251, 0.01739865498610019406, 0.01831792453166260909, 0.01923719407722502064 ),
 .UNSPECIFIED. ) ;
#100798=CARTESIAN_POINT ( 'NONE',  ( -1.102503403746643018, 45.52456777125835430, -18.11035969089068587 ) ) ;
#100821=CARTESIAN_POINT ( 'NONE',  ( -16.02987949830368564, 45.83140534720697445, 6.508315408883771802 ) ) ;
#100828=EDGE_CURVE ( 'NONE', #12068, #56766, #53143, .T. ) ;
#100829=( GEOMETRIC_REPRESENTATION_CONTEXT ( 3 ) GLOBAL_UNCERTAINTY_ASSIGNED_CONTEXT ( ( #50469 ) ) GLOBAL_UNIT_ASSIGNED_CONTEXT ( ( #4783, #14975, #13380 ) ) REPRESENTATION_CONTEXT ( 'NONE', 'WORKASPACE' ) );
#100842=SURFACE_SIDE_STYLE ('',( #25406 ) ) ;
#100845=PRESENTATION_STYLE_ASSIGNMENT (( #75511 ) ) ;
#100863=CARTESIAN_POINT ( 'NONE',  ( 29.86026515094307854, 12.86933730193439196, -39.60535821593534678 ) ) ;
#100870=FILL_AREA_STYLE ('',( #102482 ) ) ;
#100873=FILL_AREA_STYLE ('',( #50710 ) ) ;
#100879=FILL_AREA_STYLE ('',( #101430 ) ) ;
#100888=EDGE_CURVE ( 'NONE', #77549, #62895, #71089, .T. ) ;
#100913=UNCERTAINTY_MEASURE_WITH_UNIT (LENGTH_MEASURE( 1.000000000000000082E-05 ), #40443, 'distance_accuracy_value', 'NONE');
#100921=CARTESIAN_POINT ( 'NONE',  ( 1.944839216437187431E-15, 45.30391365246044444, 18.75000000000001066 ) ) ;
#100947=CARTESIAN_POINT ( 'NONE',  ( 27.10511071441177222, 36.88665068479793518, -7.556984339679249985 ) ) ;
#100954=( NAMED_UNIT ( * ) PLANE_ANGLE_UNIT ( ) SI_UNIT ( $, .RADIAN. ) );
#100962=CARTESIAN_POINT ( 'NONE',  ( -46.90314054034880797, 18.02221697236581832, 16.15497048139663860 ) ) ;
#100967=CARTESIAN_POINT ( 'NONE',  ( 16.96311743595812871, 43.37158770818926001, 6.627271858056736242 ) ) ;
#100979=PLANE ( 'NONE',  #95667 ) ;
#100992=CARTESIAN_POINT ( 'NONE',  ( -7.466998042452497764, 52.17245120308862738, -2.150398540845605666 ) ) ;
#100996=CARTESIAN_POINT ( 'NONE',  ( -1.236033772363036132, 10.15598684385509642, -50.72379936455069327 ) ) ;
#101005=CARTESIAN_POINT ( 'NONE',  ( -4.512569058504254826, 54.30834730652590991, -6.298727642264635662 ) ) ;
#101009=CARTESIAN_POINT ( 'NONE',  ( -9.882762594765820197, 45.48558064014431324, -15.34364832776106979 ) ) ;
#101029=CARTESIAN_POINT ( 'NONE',  ( 8.400757966424366785, 51.89201850070815425, -1.531152949374624317 ) ) ;
#101040=CARTESIAN_POINT ( 'NONE',  ( -48.02835407290515946, 14.94086294439721030, 16.85535821593516559 ) ) ;
#101047=( LENGTH_UNIT ( ) NAMED_UNIT ( * ) SI_UNIT ( .MILLI., .METRE. ) );
#101054=CARTESIAN_POINT ( 'NONE',  ( -23.05169487621096991, 26.02509709072602817, -30.70617127781034128 ) ) ;
#101062=EDGE_LOOP ( 'NONE', ( #43575, #20097 ) ) ;
#101069=EDGE_CURVE ( 'NONE', #36063, #5362, #22341, .T. ) ;
#101070=CARTESIAN_POINT ( 'NONE',  ( -47.55484174478885961, 16.07433637412307803, -16.76829442854521091 ) ) ;
#101077=CARTESIAN_POINT ( 'NONE',  ( -15.64244949893494052, 35.03874255891448541, -22.45790977275887457 ) ) ;
#101091=VECTOR ( 'NONE', #93875, 1000.000000000000000 ) ;
#101108=CARTESIAN_POINT ( 'NONE',  ( 48.98918515124452000, 13.11539385479792941, -16.41516879933306683 ) ) ;
#101117=VERTEX_POINT ( 'NONE', #59153 ) ;
#101122=CARTESIAN_POINT ( 'NONE',  ( 0.6202535915621898432, 13.31182157833917934, 49.41091134881317970 ) ) ;
#101141=CARTESIAN_POINT ( 'NONE',  ( 30.93190593211533823, 14.41219003788192587, 40.70233947780381101 ) ) ;
#101155=CARTESIAN_POINT ( 'NONE',  ( 9.805911699687639427, 53.43740237845030094, -2.589507950532081271 ) ) ;
#101162=STYLED_ITEM ( 'NONE', ( #18480 ), #24760 ) ;
#101169=EDGE_LOOP ( 'NONE', ( #43404, #9608 ) ) ;
#101170=UNCERTAINTY_MEASURE_WITH_UNIT (LENGTH_MEASURE( 1.000000000000000082E-05 ), #4930, 'distance_accuracy_value', 'NONE');
#101190=CARTESIAN_POINT ( 'NONE',  ( -16.64348903516517098, 45.60392139269950462, 6.657797401561654560 ) ) ;
#101192=ORIENTED_EDGE ( 'NONE', *, *, #39626, .F. ) ;
#101217=( NAMED_UNIT ( * ) SI_UNIT ( $, .STERADIAN. ) SOLID_ANGLE_UNIT ( ) );
#101236=CARTESIAN_POINT ( 'NONE',  ( 17.88133836625030426, 45.34897204669927362, -5.215214262617966945 ) ) ;
#101243=DIRECTION ( 'NONE',  ( -0.000000000000000000, 1.000000000000000000, -0.000000000000000000 ) ) ;
#101254=CARTESIAN_POINT ( 'NONE',  ( 17.37779721166321778, 36.93489020264718192, -21.96297318349786210 ) ) ;
#101258=FILL_AREA_STYLE ('',( #20922 ) ) ;
#101260=CYLINDRICAL_SURFACE ( 'NONE', #16611, 1.250000000000001110 ) ;
#101272=DIRECTION ( 'NONE',  ( -0.000000000000000000, 1.000000000000000000, -0.000000000000000000 ) ) ;
#101275=( GEOMETRIC_REPRESENTATION_CONTEXT ( 3 ) GLOBAL_UNCERTAINTY_ASSIGNED_CONTEXT ( ( #61272 ) ) GLOBAL_UNIT_ASSIGNED_CONTEXT ( ( #14401, #80210, #12294 ) ) REPRESENTATION_CONTEXT ( 'NONE', 'WORKASPACE' ) );
#101282=CARTESIAN_POINT ( 'NONE',  ( 0.6421581498681602218, 36.36120089367192065, -29.57562450428436662 ) ) ;
#101288=FILL_AREA_STYLE_COLOUR ( '', #77425 ) ;
#101295=( NAMED_UNIT ( * ) SI_UNIT ( $, .STERADIAN. ) SOLID_ANGLE_UNIT ( ) );
#101298=EDGE_LOOP ( 'NONE', ( #1177, #57600 ) ) ;
#101305=ORIENTED_EDGE ( 'NONE', *, *, #64871, .T. ) ;
#101327=CARTESIAN_POINT ( 'NONE',  ( 48.59987877357390573, 15.38663336896927447, 14.48702310944051419 ) ) ;
#101332=CARTESIAN_POINT ( 'NONE',  ( -11.24782996177939332, 43.18746564262799126, -14.96095123926246373 ) ) ;
#101367=STYLED_ITEM ( 'NONE', ( #69256 ), #2836 ) ;
#101369=AXIS2_PLACEMENT_3D ( 'NONE', #29064, #18832, #53804 ) ;
#101410=EDGE_CURVE ( 'NONE', #88641, #20459, #79065, .T. ) ;
#101421=PRESENTATION_STYLE_ASSIGNMENT (( #3789 ) ) ;
#101427=ORIENTED_EDGE ( 'NONE', *, *, #88739, .T. ) ;
#101428=DIRECTION ( 'NONE',  ( -0.000000000000000000, 1.000000000000000000, 0.000000000000000000 ) ) ;
#101430=FILL_AREA_STYLE_COLOUR ( '', #90470 ) ;
#101431=VERTEX_POINT ( 'NONE', #37590 ) ;
#101437=DIRECTION ( 'NONE',  ( 0.000000000000000000, 1.000000000000000000, 0.000000000000000000 ) ) ;
#101446=CARTESIAN_POINT ( 'NONE',  ( -29.77292113577844646, 13.34857726707550007, -42.10535821593474282 ) ) ;
#101496=B_SPLINE_CURVE_WITH_KNOTS ( 'NONE', 3,
 ( #18436, #18982, #101976, #51828, #44831, #43223, #36234, #77718, #51291, #76105, #10826, #35700, #2206, #61016, #69106, #28137, #11358, #3829, #69630, #102524 ),
 .UNSPECIFIED., .F., .F.,
 ( 4, 2, 2, 2, 2, 2, 2, 2, 2, 4 ),
 ( 0.002921171163060748248, 0.003426533276933608693, 0.003931895390806470006, 0.004184576447742896325, 0.004437257504679322645, 0.004942619618552173549, 0.005447981732425023586, 0.005953343846297873623, 0.006458705960170724528, 0.006964068074043574565 ),
 .UNSPECIFIED. ) ;
#101506=DIRECTION ( 'NONE',  ( 0.000000000000000000, 1.000000000000000000, -0.000000000000000000 ) ) ;
#101510=EDGE_CURVE ( 'NONE', #63888, #29217, #5488, .T. ) ;
#101515=EDGE_CURVE ( 'NONE', #347, #45425, #40249, .T. ) ;
#101523=SURFACE_SIDE_STYLE ('',( #10890 ) ) ;
#101530=EDGE_CURVE ( 'NONE', #66067, #9858, #82235, .T. ) ;
#101532=FACE_BOUND ( 'NONE', #34930, .T. ) ;
#101537=CARTESIAN_POINT ( 'NONE',  ( -0.5361375818286260309, 8.011584859334254460, -51.63592075595909137 ) ) ;
#101548=CARTESIAN_POINT ( 'NONE',  ( -10.28624191511829977, 46.12099395432375104, -12.90779740156156841 ) ) ;
#101553=DIRECTION ( 'NONE',  ( 0.000000000000000000, -0.3420201433256725987, -0.9396926207859068736 ) ) ;
#101575=CARTESIAN_POINT ( 'NONE',  ( 16.75187969033571989, 34.25544727262119693, 24.30698433968583316 ) ) ;
#101576=CARTESIAN_POINT ( 'NONE',  ( 47.14730021652958669, 17.20087926883151752, -16.50246546963092698 ) ) ;
#101578=DIRECTION ( 'NONE',  ( -0.000000000000000000, -1.000000000000000000, -0.000000000000000000 ) ) ;
#101582=( LENGTH_UNIT ( ) NAMED_UNIT ( * ) SI_UNIT ( .MILLI., .METRE. ) );
#101583=( GEOMETRIC_REPRESENTATION_CONTEXT ( 3 ) GLOBAL_UNCERTAINTY_ASSIGNED_CONTEXT ( ( #57036 ) ) GLOBAL_UNIT_ASSIGNED_CONTEXT ( ( #22561, #22014, #39255 ) ) REPRESENTATION_CONTEXT ( 'NONE', 'WORKASPACE' ) );
#101586=UNCERTAINTY_MEASURE_WITH_UNIT (LENGTH_MEASURE( 1.000000000000000082E-05 ), #85448, 'distance_accuracy_value', 'NONE');
#101591=CARTESIAN_POINT ( 'NONE',  ( 4.523357435794008730, 51.56555634218408812, -8.281338046071601511 ) ) ;
#101613=CARTESIAN_POINT ( 'NONE',  ( -46.89590902281747731, 18.03207604453001167, -16.16381118462896183 ) ) ;
#101616=ORIENTED_EDGE ( 'NONE', *, *, #93374, .T. ) ;
#101617=CARTESIAN_POINT ( 'NONE',  ( 37.56673239365870387, 25.75719283951018923, 10.95617127780998956 ) ) ;
#101626=CARTESIAN_POINT ( 'NONE',  ( 9.646320399536545409, 46.21287003049852871, -13.08069908581829388 ) ) ;
#101658=CARTESIAN_POINT ( 'NONE',  ( 0.2960823612032095764, 13.62269841106403589, 49.28347290955902338 ) ) ;
#101681=VERTEX_POINT ( 'NONE', #100546 ) ;
#101710=VECTOR ( 'NONE', #59140, 1000.000000000000000 ) ;
#101725=CARTESIAN_POINT ( 'NONE',  ( -15.51166181318948567, 36.90500793569740523, -23.41746243165360042 ) ) ;
#101736=ORIENTED_EDGE ( 'NONE', *, *, #104014, .F. ) ;
#101751=B_SPLINE_CURVE_WITH_KNOTS ( 'NONE', 3,
 ( #78614, #86221, #71066, #37686, #103438, #71583, #4746, #29589, #62458, #104490, #95350, #30637, #54321, #13877, #87266, #55396, #79685, #13344, #63525, #96424, #88327, #36622, #44688, #77576, #3695, #69487, #102373, #28521 ),
 .UNSPECIFIED., .F., .F.,
 ( 4, 2, 2, 2, 2, 2, 2, 2, 2, 2, 2, 2, 2, 4 ),
 ( 0.006869492556767144154, 0.007098556943535802230, 0.007327621330304460306, 0.007785750103841772123, 0.008702007650916396622, 0.009618265197991021989, 0.01053452274506564736, 0.01145078029214027099, 0.01236703783921489636, 0.01282516661275220730, 0.01328329538628951825, 0.01374142415982682920, 0.01397048854659548381, 0.01419955293336414015 ),
 .UNSPECIFIED. ) ;
#101760=ORIENTED_EDGE ( 'NONE', *, *, #36297, .T. ) ;
#101761=FILL_AREA_STYLE ('',( #36014 ) ) ;
#101772=CARTESIAN_POINT ( 'NONE',  ( 16.75187969033515145, 37.11970326878314808, -21.80698433968624528 ) ) ;
#101775=( LENGTH_UNIT ( ) NAMED_UNIT ( * ) SI_UNIT ( .MILLI., .METRE. ) );
#101799=CARTESIAN_POINT ( 'NONE',  ( -1.249969396200062199, 27.80191114808519615, 39.34173072747167765 ) ) ;
#101810=CARTESIAN_POINT ( 'NONE',  ( 48.02835407290544367, 9.771516447483593382, 16.85535821593427386 ) ) ;
#101828=DIRECTION ( 'NONE',  ( 0.000000000000000000, 0.000000000000000000, -1.000000000000000000 ) ) ;
#101832=CARTESIAN_POINT ( 'NONE',  ( -8.397840381921547248, 51.60961829421124492, 4.031152949374568806 ) ) ;
#101846=CARTESIAN_POINT ( 'NONE',  ( 48.90276556242013584, 14.54846953981844315, 14.70164374843103339 ) ) ;
#101852=CARTESIAN_POINT ( 'NONE',  ( -11.04491272560624182, 43.74903401048490537, -13.15179640090838298 ) ) ;
#101854=CARTESIAN_POINT ( 'NONE',  ( -1.219694214448577840, 36.63054784644727846, 28.81676271875494066 ) ) ;
#101862=EDGE_LOOP ( 'NONE', ( #43726, #70097, #21889, #97216 ) ) ;
#101877=CARTESIAN_POINT ( 'NONE',  ( 1.125013611802090141, 36.97869928123036942, 27.86412292502800980 ) ) ;
#101923=CARTESIAN_POINT ( 'NONE',  ( 27.72595153895140996, 36.41251212665846282, 9.903912806810659220 ) ) ;
#101933=DIRECTION ( 'NONE',  ( 0.000000000000000000, 0.000000000000000000, -1.000000000000000000 ) ) ;
#101934=LINE ( 'NONE', #64029, #36440 ) ;
#101937=FACE_OUTER_BOUND ( 'NONE', #73895, .T. ) ;
#101943=ORIENTED_EDGE ( 'NONE', *, *, #27739, .F. ) ;
#101961=ORIENTED_EDGE ( 'NONE', *, *, #1086, .F. ) ;
#101976=CARTESIAN_POINT ( 'NONE',  ( -16.32527301256094177, 45.99414959098179168, -4.187920679398874135 ) ) ;
#101991=CARTESIAN_POINT ( 'NONE',  ( -28.28142067734527032, 36.39280011943776572, 8.376232292823662107 ) ) ;
#101999=COLOUR_RGB ( '', 0.08235294, 0.09019608, 0.10196078) ;
#102003=EDGE_CURVE ( 'NONE', #58472, #44553, #94338, .T. ) ;
#102015=EDGE_LOOP ( 'NONE', ( #1164, #33560 ) ) ;
#102024=( LENGTH_UNIT ( ) NAMED_UNIT ( * ) SI_UNIT ( .MILLI., .METRE. ) );
#102025=MECHANICAL_DESIGN_GEOMETRIC_PRESENTATION_REPRESENTATION('',(#31383),#62400);
#102046=CARTESIAN_POINT ( 'NONE',  ( 0.000000000000000000, 38.19193163660327173, 24.55262289886175964 ) ) ;
#102059=( NAMED_UNIT ( * ) PLANE_ANGLE_UNIT ( ) SI_UNIT ( $, .RADIAN. ) );
#102060=UNCERTAINTY_MEASURE_WITH_UNIT (LENGTH_MEASURE( 1.000000000000000082E-05 ), #23306, 'distance_accuracy_value', 'NONE');
#102066=SURFACE_STYLE_USAGE ( .BOTH. , #61096 ) ;
#102069=CARTESIAN_POINT ( 'NONE',  ( -9.088913997560085889, 46.11732115646235286, -13.78939345329818877 ) ) ;
#102097=CARTESIAN_POINT ( 'NONE',  ( -11.38818291378892056, 43.57520507334620419, 13.48712730654634662 ) ) ;
#102100=( GEOMETRIC_REPRESENTATION_CONTEXT ( 3 ) GLOBAL_UNCERTAINTY_ASSIGNED_CONTEXT ( ( #6356 ) ) GLOBAL_UNIT_ASSIGNED_CONTEXT ( ( #52707, #102868, #61360 ) ) REPRESENTATION_CONTEXT ( 'NONE', 'WORKASPACE' ) );
#102116=CARTESIAN_POINT ( 'NONE',  ( -25.88429648623745649, 35.08523104449947283, -8.490101697507606460 ) ) ;
#102126=CARTESIAN_POINT ( 'NONE',  ( -11.49350100829453325, 45.59260286365996961, -13.79671030421808098 ) ) ;
#102133=EDGE_CURVE ( 'NONE', #68169, #77582, #79727, .T. ) ;
#102138=SURFACE_SIDE_STYLE ('',( #54101 ) ) ;
#102144=CARTESIAN_POINT ( 'NONE',  ( -17.77115019406404173, 34.18919163712646281, 23.80020659827771112 ) ) ;
#102145=CARTESIAN_POINT ( 'NONE',  ( 9.041225629235734473, 45.95386998337555440, -14.35441598012803510 ) ) ;
#102147=EDGE_CURVE ( 'NONE', #41373, #104078, #92982, .T. ) ;
#102151=FILL_AREA_STYLE_COLOUR ( '', #12844 ) ;
#102165=CARTESIAN_POINT ( 'NONE',  ( -36.35727881789110683, 28.12781631794103276, -12.56218724973182255 ) ) ;
#102166=EDGE_CURVE ( 'NONE', #46319, #40774, #35789, .T. ) ;
#102167=CARTESIAN_POINT ( 'NONE',  ( 49.03498469565151652, 14.13689777146936422, -14.86104782056310114 ) ) ;
#102172=DIRECTION ( 'NONE',  ( 1.150791560227848051E-16, -0.3420201433256733758, 0.9396926207859066515 ) ) ;
#102180=MECHANICAL_DESIGN_GEOMETRIC_PRESENTATION_REPRESENTATION('',(#22989),#16027);
#102206=CARTESIAN_POINT ( 'NONE',  ( -7.461489502270862495, 54.13514019874089200, 3.459350134084382855 ) ) ;
#102218=CARTESIAN_POINT ( 'NONE',  ( 9.166999376131622412, 53.73590836252315484, -1.685805968339065819 ) ) ;
#102229=UNCERTAINTY_MEASURE_WITH_UNIT (LENGTH_MEASURE( 1.000000000000000082E-05 ), #7662, 'distance_accuracy_value', 'NONE');
#102230=DIRECTION ( 'NONE',  ( 0.000000000000000000, 1.000000000000000000, 0.000000000000000000 ) ) ;
#102231=FACE_BOUND ( 'NONE', #8865, .T. ) ;
#102234=FILL_AREA_STYLE ('',( #73145 ) ) ;
#102288=CARTESIAN_POINT ( 'NONE',  ( 29.59213159313616970, 8.427504962981444692, -42.10535821593531125 ) ) ;
#102292=CARTESIAN_POINT ( 'NONE',  ( -9.559820589950547287, 51.28889575324969741, 3.548930410621208953 ) ) ;
#102308=B_SPLINE_CURVE_WITH_KNOTS ( 'NONE', 3,
 ( #65434, #30436, #40096, #81582, #7181, #40617, #80537, #15814, #64384, #48169, #39049, #22354, #64901, #97783, #39583, #89715, #30976, #23950, #24484, #104832 ),
 .UNSPECIFIED., .F., .F.,
 ( 4, 2, 2, 2, 2, 2, 2, 2, 2, 4 ),
 ( 0.003044366697538010598, 0.003296264436757893445, 0.003548162175977776726, 0.004051957654417542853, 0.005059548611297080313, 0.005563344089736851211, 0.006067139568176622977, 0.006319037307396508860, 0.006570935046616394742, 0.007074730525056170845 ),
 .UNSPECIFIED. ) ;
#102330=DIRECTION ( 'NONE',  ( -0.000000000000000000, 1.000000000000000000, -0.000000000000000000 ) ) ;
#102334=( LENGTH_UNIT ( ) NAMED_UNIT ( * ) SI_UNIT ( .MILLI., .METRE. ) );
#102342=B_SPLINE_CURVE_WITH_KNOTS ( 'NONE', 3,
 ( #21958, #4162, #54809, #87741, #13821, #79624, #71529, #63472, #96368, #16488, #31637, #98456, #89326, #96882, #8388, #25139, #57457, #15419, #74708, #49367, #15955, #31120, #81202, #74178, #89850, #24608 ),
 .UNSPECIFIED., .F., .F.,
 ( 4, 2, 2, 2, 2, 2, 2, 2, 2, 2, 2, 2, 4 ),
 ( 0.007354091942747225871, 0.007606081946708171705, 0.007858071950669117539, 0.008362051958591010942, 0.008614041962551966317, 0.008866031966512921692, 0.009370011974434832441, 0.009873991982356743191, 0.01037797199027865394, 0.01062996199423960758, 0.01088195199820056296, 0.01113394200216151660, 0.01138593200612247024 ),
 .UNSPECIFIED. ) ;
#102344=ORIENTED_EDGE ( 'NONE', *, *, #19193, .T. ) ;
#102373=CARTESIAN_POINT ( 'NONE',  ( 0.07719627998383862821, 7.746009256456144243, -51.75000000000014921 ) ) ;
#102389=ORIENTED_EDGE ( 'NONE', *, *, #33349, .T. ) ;
#102418=CARTESIAN_POINT ( 'NONE',  ( 15.52419239919875693, 37.09839268680908475, -22.76866006007180587 ) ) ;
#102428=CARTESIAN_POINT ( 'NONE',  ( -8.559508646656370345, -1.200000000000000030E-05, 4.031152949374564365 ) ) ;
#102432=CARTESIAN_POINT ( 'NONE',  ( 0.000000000000000000, -1.200000000000000030E-05, -17.50000000000000000 ) ) ;
#102462=EDGE_CURVE ( 'NONE', #41320, #88738, #76158, .T. ) ;
#102476=CARTESIAN_POINT ( 'NONE',  ( 0.000000000000000000, 32.68727484027578356, -33.82893434829263413 ) ) ;
#102482=FILL_AREA_STYLE_COLOUR ( '', #102862 ) ;
#102498=CARTESIAN_POINT ( 'NONE',  ( 23.85899507165746414, 27.29461519911105682, 33.04201830783504334 ) ) ;
#102503=EDGE_CURVE ( 'NONE', #100209, #81828, #58493, .T. ) ;
#102523=EDGE_CURVE ( 'NONE', #85798, #50509, #31317, .T. ) ;
#102524=CARTESIAN_POINT ( 'NONE',  ( -16.64348903516496136, 45.60392139269943357, -6.657797401562710604 ) ) ;
#102538=CARTESIAN_POINT ( 'NONE',  ( 2.761899744546835519E-15, 36.79151656018385097, 22.55262289886175964 ) ) ;
#102546=ORIENTED_EDGE ( 'NONE', *, *, #17544, .T. ) ;
#102569=CARTESIAN_POINT ( 'NONE',  ( -48.02835407290516656, 16.78162100668608048, 14.35535821593516559 ) ) ;
#102571=SURFACE_STYLE_FILL_AREA ( #38387 ) ;
#102592=EDGE_CURVE ( 'NONE', #26726, #6732, #89170, .T. ) ;
#102594=ORIENTED_EDGE ( 'NONE', *, *, #75268, .T. ) ;
#102601=CARTESIAN_POINT ( 'NONE',  ( -17.99842623603809244, 36.44670248777274679, 23.18063615129680954 ) ) ;
#102605=CARTESIAN_POINT ( 'NONE',  ( 5.455323569189487465, 53.44305311210484888, -8.531152949374620320 ) ) ;
#102613=SURFACE_STYLE_FILL_AREA ( #69721 ) ;
#102658=CARTESIAN_POINT ( 'NONE',  ( -25.85821479973299120, 35.03516150445064881, -8.996769488741277243 ) ) ;
#102667=CARTESIAN_POINT ( 'NONE',  ( -10.45249458729210090, 46.08328249563463430, -12.90779740156156663 ) ) ;
#102682=CARTESIAN_POINT ( 'NONE',  ( -17.59489243402637371, 34.17351006103357491, 23.98382166917486558 ) ) ;
#102688=CARTESIAN_POINT ( 'NONE',  ( 48.02835407290504577, 9.771516447483525880, -16.85535821593549954 ) ) ;
#102700=B_SPLINE_CURVE_WITH_KNOTS ( 'NONE', 3,
 ( #93846, #38680, #80169, #71546, #30599, #62950, #104450, #39212, #72087, #104994, #31138, #25161, #33245, #59107, #91475, #33779, #17590, #66655, #106570, #32721 ),
 .UNSPECIFIED., .F., .F.,
 ( 4, 2, 2, 2, 2, 2, 2, 2, 2, 4 ),
 ( 0.007841668765295708304, 0.008346380259883516214, 0.008851091754471324125, 0.009103447501765230682, 0.009355803249059137239, 0.009860514743646950353, 0.01036522623823476347, 0.01086993773282257658, 0.01137464922741038970, 0.01187936072199820281 ),
 .UNSPECIFIED. ) ;
#102711=CARTESIAN_POINT ( 'NONE',  ( 4.189287965499270072, 52.12930734542786126, 6.683032746053408246 ) ) ;
#102736=ADVANCED_FACE ( 'NONE', ( #67650 ), #51448, .F. ) ;
#102749=ORIENTED_EDGE ( 'NONE', *, *, #38224, .F. ) ;
#102773=CARTESIAN_POINT ( 'NONE',  ( -16.64348903516496136, 45.60392139269943357, -6.657797401562710604 ) ) ;
#102775=( NAMED_UNIT ( * ) PLANE_ANGLE_UNIT ( ) SI_UNIT ( $, .RADIAN. ) );
#102806=EDGE_CURVE ( 'NONE', #11951, #64333, #20822, .T. ) ;
#102813=CARTESIAN_POINT ( 'NONE',  ( 48.02835407290544367, -1.200000000000000030E-05, 14.35535821593427386 ) ) ;
#102829=CARTESIAN_POINT ( 'NONE',  ( 16.64348903516523848, -1.200000000000000030E-05, 4.157797401561420081 ) ) ;
#102862=COLOUR_RGB ( '', 0.08235294, 0.09019608, 0.10196078) ;
#102868=( NAMED_UNIT ( * ) PLANE_ANGLE_UNIT ( ) SI_UNIT ( $, .RADIAN. ) );
#102869=AXIS2_PLACEMENT_3D ( 'NONE', #54025, #13037, #88019 ) ;
#102872=CARTESIAN_POINT ( 'NONE',  ( 1.219658573673010116, 36.86119053457258588, -28.18247609706499546 ) ) ;
#102881=EDGE_LOOP ( 'NONE', ( #51941, #95740 ) ) ;
#102897=SURFACE_SIDE_STYLE ('',( #61930 ) ) ;
#102900=FACE_BOUND ( 'NONE', #328, .T. ) ;
#102906=CARTESIAN_POINT ( 'NONE',  ( -7.337702322492915208, 52.18298084268283787, 2.467673208560980491 ) ) ;
#102952=CARTESIAN_POINT ( 'NONE',  ( 15.90864490579649626, 37.20836975595025820, -22.13037531087910992 ) ) ;
#102965=CARTESIAN_POINT ( 'NONE',  ( -49.07747248321140887, 8.835459238882952704, 14.91203737403126794 ) ) ;
#102967=CARTESIAN_POINT ( 'NONE',  ( -15.64519568958363749, 46.18931709473498159, 4.637408661950026101 ) ) ;
#102972=CARTESIAN_POINT ( 'NONE',  ( -30.10549840784188902, 7.858493733726967356, 42.03383688247123473 ) ) ;
#103011=FACE_BOUND ( 'NONE', #98917, .T. ) ;
#103012=VECTOR ( 'NONE', #3060, 1000.000000000000000 ) ;
#103033=CARTESIAN_POINT ( 'NONE',  ( 24.20499783611734657, 27.76345924012371924, 31.17339665328782772 ) ) ;
#103045=CARTESIAN_POINT ( 'NONE',  ( -30.80294602723943598, 13.24188206181652383, -41.41355684762699951 ) ) ;
#103064=CARTESIAN_POINT ( 'NONE',  ( -0.6187860399584415028, 13.31391022449570194, 49.41005378291666261 ) ) ;
#103096=CARTESIAN_POINT ( 'NONE',  ( 30.92872287337538850, 13.87446774603010979, -40.98770496732647217 ) ) ;
#103106=CARTESIAN_POINT ( 'NONE',  ( 17.89629221201704823, 43.18024824084014313, 5.552246930289013171 ) ) ;
#103131=VERTEX_POINT ( 'NONE', #40318 ) ;
#103132=CARTESIAN_POINT ( 'NONE',  ( -28.34962641295014052, 34.17951769392475825, 8.951028473884061754 ) ) ;
#103138=CARTESIAN_POINT ( 'NONE',  ( 16.75187969033515145, 37.11970326878314808, -21.80698433968624528 ) ) ;
#103141=CARTESIAN_POINT ( 'NONE',  ( 17.51296689355397262, 34.75029386635176820, -22.05286986923737302 ) ) ;
#103160=EDGE_LOOP ( 'NONE', ( #27447, #11641, #83420, #52272 ) ) ;
#103170=CARTESIAN_POINT ( 'NONE',  ( -11.53815258514799602, 45.46891437459017027, 14.20004885619764146 ) ) ;
#103182=PRESENTATION_STYLE_ASSIGNMENT (( #94577 ) ) ;
#103199=CARTESIAN_POINT ( 'NONE',  ( -49.07537269082070708, 14.00518788141075710, -14.91829442325389721 ) ) ;
#103200=( GEOMETRIC_REPRESENTATION_CONTEXT ( 3 ) GLOBAL_UNCERTAINTY_ASSIGNED_CONTEXT ( ( #100117 ) ) GLOBAL_UNIT_ASSIGNED_CONTEXT ( ( #49829, #56306, #89245 ) ) REPRESENTATION_CONTEXT ( 'NONE', 'WORKASPACE' ) );
#103233=EDGE_LOOP ( 'NONE', ( #66584, #40735, #52222, #57797 ) ) ;
#103243=DIRECTION ( 'NONE',  ( 0.000000000000000000, 1.000000000000000000, 0.000000000000000000 ) ) ;
#103245=CARTESIAN_POINT ( 'NONE',  ( 4.958618710454560485, 52.14943927389753497, 6.064328585294240348 ) ) ;
#103266=CARTESIAN_POINT ( 'NONE',  ( 27.10511071441177222, 36.88665068479793518, -7.556984339679249985 ) ) ;
#103305=CARTESIAN_POINT ( 'NONE',  ( -16.18712010533815615, 37.20509496956294981, 21.93868532144427164 ) ) ;
#103332=DIRECTION ( 'NONE',  ( 0.000000000000000000, 1.000000000000000000, -0.000000000000000000 ) ) ;
#103337=COLOUR_RGB ( '', 0.66274510, 0.83137255, 0.94901961) ;
#103350=CARTESIAN_POINT ( 'NONE',  ( 30.04499556692307394, 7.904673525308155924, 42.05327650403261686 ) ) ;
#103360=CARTESIAN_POINT ( 'NONE',  ( 28.94979900162220687, 13.71034195483037443, -39.84012157007438049 ) ) ;
#103408=CARTESIAN_POINT ( 'NONE',  ( -37.56673239365849781, -1.200000000000000030E-05, 13.45617127781066280 ) ) ;
#103420=COLOUR_RGB ( '', 0.66274510, 0.83137255, 0.94901961) ;
#103423=( NAMED_UNIT ( * ) SI_UNIT ( $, .STERADIAN. ) SOLID_ANGLE_UNIT ( ) );
#103438=CARTESIAN_POINT ( 'NONE',  ( 0.3587072354609493474, 13.57974219347169509, -49.30106301256189028 ) ) ;
#103471=SURFACE_SIDE_STYLE ('',( #23108 ) ) ;
#103472=ORIENTED_EDGE ( 'NONE', *, *, #29149, .F. ) ;
#103477=CARTESIAN_POINT ( 'NONE',  ( -26.49211181453642538, 36.83374520352522552, 9.907801504249466262 ) ) ;
#103489=ORIENTED_EDGE ( 'NONE', *, *, #20547, .F. ) ;
#103492=CARTESIAN_POINT ( 'NONE',  ( -48.02835407290516656, 9.771516447483513446, 16.85535821593516559 ) ) ;
#103494=ORIENTED_EDGE ( 'NONE', *, *, #12691, .T. ) ;
#103499=CARTESIAN_POINT ( 'NONE',  ( -29.68315524076989576, 13.12249633091057177, 39.60535821593503414 ) ) ;
#103527=DIRECTION ( 'NONE',  ( 0.000000000000000000, 0.000000000000000000, -1.000000000000000000 ) ) ;
#103536=DIRECTION ( 'NONE',  ( 0.000000000000000000, -0.3420201433256725987, -0.9396926207859068736 ) ) ;
#103552=CARTESIAN_POINT ( 'NONE',  ( -10.28624191511820207, 43.25714326066858462, 15.40779740156164124 ) ) ;
#103553=CARTESIAN_POINT ( 'NONE',  ( 23.97722388339762389, 27.87827700592711722, 30.95083563548385541 ) ) ;
#103563=CARTESIAN_POINT ( 'NONE',  ( -30.92841573401175381, 13.86971257847473460, -40.99043602818892396 ) ) ;
#103564=ORIENTED_EDGE ( 'NONE', *, *, #9617, .T. ) ;
#103570=CYLINDRICAL_SURFACE ( 'NONE', #37881, 1.250000000000001110 ) ;
#103579=VERTEX_POINT ( 'NONE', #14311 ) ;
#103581=CARTESIAN_POINT ( 'NONE',  ( -0.2951772788882962018, 7.823394093897796608, 51.71673678500803106 ) ) ;
#103594=DIRECTION ( 'NONE',  ( 0.000000000000000000, 1.000000000000000000, 0.000000000000000000 ) ) ;
#103607=DIRECTION ( 'NONE',  ( 0.000000000000000000, 0.000000000000000000, 1.000000000000000000 ) ) ;
#103608=( NAMED_UNIT ( * ) PLANE_ANGLE_UNIT ( ) SI_UNIT ( $, .RADIAN. ) );
#103614=( NAMED_UNIT ( * ) PLANE_ANGLE_UNIT ( ) SI_UNIT ( $, .RADIAN. ) );
#103619=CARTESIAN_POINT ( 'NONE',  ( 37.56673239365873940, 27.88554838446218653, 10.95617127780822564 ) ) ;
#103656=CARTESIAN_POINT ( 'NONE',  ( -17.74039601254163045, 36.76373445370536075, 22.27539783717242727 ) ) ;
#103661=CARTESIAN_POINT ( 'NONE',  ( 17.97939362404986952, 34.27531155324909662, -23.34516625433381520 ) ) ;
#103663=B_SPLINE_CURVE_WITH_KNOTS ( 'NONE', 3,
 ( #53999, #86939, #13009, #8106, #48561, #104687, #55582, #81451, #24856, #71776, #56107, #22745, #88520, #72323, #23263, #57182, #57705, #98701, #40483, #5981, #49086, #90098 ),
 .UNSPECIFIED., .F., .F.,
 ( 4, 2, 2, 2, 2, 2, 2, 2, 2, 2, 4 ),
 ( 0.0002601258248896089241, 0.0007638464171177765079, 0.001015706713231860625, 0.001267567009345944851, 0.001519427305460029076, 0.001771287601574113302, 0.002275008193802294330, 0.002778728786030475358, 0.003282449378258655952, 0.003786169970486836980, 0.004289890562715018008 ),
 .UNSPECIFIED. ) ;
#103666=ORIENTED_EDGE ( 'NONE', *, *, #29989, .T. ) ;
#103693=CARTESIAN_POINT ( 'NONE',  ( 10.28624191511840458, -1.200000000000000030E-05, 12.90779740156148847 ) ) ;
#103706=CARTESIAN_POINT ( 'NONE',  ( -9.169161018550420650, 53.73561361817692728, -1.678544271685364464 ) ) ;
#103717=DIRECTION ( 'NONE',  ( 0.000000000000000000, 1.000000000000000000, -0.000000000000000000 ) ) ;
#103719=CARTESIAN_POINT ( 'NONE',  ( -48.99295625602604787, 13.11026251878874227, -16.41069188771936638 ) ) ;
#103742=VECTOR ( 'NONE', #14345, 1000.000000000000000 ) ;
#103759=CARTESIAN_POINT ( 'NONE',  ( 3.840629472727446691E-14, -1.200000000000000030E-05, 28.50000000000000000 ) ) ;
#103769=CARTESIAN_POINT ( 'NONE',  ( 16.64348903516499334, 45.60392139269944067, 6.657797401562596917 ) ) ;
#103770=ORIENTED_EDGE ( 'NONE', *, *, #36245, .F. ) ;
#103778=CARTESIAN_POINT ( 'NONE',  ( -25.86082360276708414, 37.20200679985001102, -8.660809983426863923 ) ) ;
#103796=ADVANCED_FACE ( 'NONE', ( #89819 ), #95789, .F. ) ;
#103802=AXIS2_PLACEMENT_3D ( 'NONE', #44849, #36256, #20620 ) ;
#103834=CARTESIAN_POINT ( 'NONE',  ( 24.29723907929104598, 27.70462894893681494, -31.30642834101323047 ) ) ;
#103869=ORIENTED_EDGE ( 'NONE', *, *, #26486, .F. ) ;
#103870=CARTESIAN_POINT ( 'NONE',  ( -48.02835407290534420, -1.200000000000000030E-05, -14.35535821593460248 ) ) ;
#103872=VECTOR ( 'NONE', #33771, 1000.000000000000000 ) ;
#103889=EDGE_CURVE ( 'NONE', #3192, #67680, #34800, .T. ) ;
#103897=VECTOR ( 'NONE', #42299, 1000.000000000000227 ) ;
#103902=CARTESIAN_POINT ( 'NONE',  ( 10.11927453338527094, 43.29088567661159459, 15.40779740156148669 ) ) ;
#103906=SURFACE_SIDE_STYLE ('',( #38665 ) ) ;
#103942=EDGE_CURVE ( 'NONE', #31195, #45709, #50162, .T. ) ;
#103956=ORIENTED_EDGE ( 'NONE', *, *, #5200, .F. ) ;
#103959=SURFACE_STYLE_USAGE ( .BOTH. , #105557 ) ;
#103965=( GEOMETRIC_REPRESENTATION_CONTEXT ( 3 ) GLOBAL_UNCERTAINTY_ASSIGNED_CONTEXT ( ( #9511 ) ) GLOBAL_UNIT_ASSIGNED_CONTEXT ( ( #65286, #9157, #31368 ) ) REPRESENTATION_CONTEXT ( 'NONE', 'WORKASPACE' ) );
#103970=DIRECTION ( 'NONE',  ( 0.000000000000000000, -0.3420201433256727652, -0.9396926207859068736 ) ) ;
#103974=ORIENTED_EDGE ( 'NONE', *, *, #75429, .F. ) ;
#103976=COLOUR_RGB ( '', 0.31764706, 0.68627451, 0.89019608) ;
#103996=CARTESIAN_POINT ( 'NONE',  ( -26.10555842523061898, 37.18665756854946380, 8.037934041381376460 ) ) ;
#103997=ORIENTED_EDGE ( 'NONE', *, *, #32973, .F. ) ;
#104005=LINE ( 'NONE', #87316, #10570 ) ;
#104009=CARTESIAN_POINT ( 'NONE',  ( -48.28084718957928345, 9.217476947337136295, 16.83779905917586817 ) ) ;
#104014=EDGE_CURVE ( 'NONE', #96544, #59570, #18098, .T. ) ;
#104017=CARTESIAN_POINT ( 'NONE',  ( 29.49619080111450131, 13.37262004692844464, 39.61417171781327795 ) ) ;
#104058=VERTEX_POINT ( 'NONE', #64912 ) ;
#104060=ORIENTED_EDGE ( 'NONE', *, *, #43111, .T. ) ;
#104066=MECHANICAL_DESIGN_GEOMETRIC_PRESENTATION_REPRESENTATION('',(#30043),#24871);
#104067=CARTESIAN_POINT ( 'NONE',  ( 15.56772955930212099, 46.04746595587301528, -6.065209611211576757 ) ) ;
#104073=CARTESIAN_POINT ( 'NONE',  ( -17.51117938516228634, 36.87948859581990035, -22.05134542098268113 ) ) ;
#104078=VERTEX_POINT ( 'NONE', #2139 ) ;
#104084=CARTESIAN_POINT ( 'NONE',  ( -29.85995211472205213, 18.03913124950666003, -39.60535821593472861 ) ) ;
#104092=LINE ( 'NONE', #30232, #44690 ) ;
#104102=CARTESIAN_POINT ( 'NONE',  ( -0.3586650412126671794, 13.57975806887350245, 49.30105652963410989 ) ) ;
#104117=PRESENTATION_STYLE_ASSIGNMENT (( #23233 ) ) ;
#104134=EDGE_CURVE ( 'NONE', #92392, #38377, #35632, .T. ) ;
#104135=CARTESIAN_POINT ( 'NONE',  ( 30.48723010194639471, 12.91713162683277538, -41.81530375792760879 ) ) ;
#104136=FILL_AREA_STYLE ('',( #45918 ) ) ;
#104145=CARTESIAN_POINT ( 'NONE',  ( 17.95960601129987211, 34.46549755681294158, 22.69733944828496774 ) ) ;
#104160=( NAMED_UNIT ( * ) SI_UNIT ( $, .STERADIAN. ) SOLID_ANGLE_UNIT ( ) );
#104191=FACE_BOUND ( 'NONE', #78222, .T. ) ;
#104203=VERTEX_POINT ( 'NONE', #77654 ) ;
#104212=CARTESIAN_POINT ( 'NONE',  ( 10.92969676275519042, 45.30189166192086958, -15.24269870591670184 ) ) ;
#104213=CARTESIAN_POINT ( 'NONE',  ( 47.29141116144560186, 18.29911311166214105, -14.59113362281996551 ) ) ;
#104240=CARTESIAN_POINT ( 'NONE',  ( 0.000000000000000000, 45.89575828009193259, 11.27631144943088337 ) ) ;
#104249=CARTESIAN_POINT ( 'NONE',  ( -16.75187969033532553, -1.200000000000000030E-05, 24.30698433968612449 ) ) ;
#104267=ORIENTED_EDGE ( 'NONE', *, *, #59396, .F. ) ;
#104270=CARTESIAN_POINT ( 'NONE',  ( -38.80476300150524338, 27.34311131113723903, -12.01468182136296470 ) ) ;
#104292=CARTESIAN_POINT ( 'NONE',  ( 11.06447879995736194, 43.17496316643826759, 15.13962491005383271 ) ) ;
#104340=( LENGTH_UNIT ( ) NAMED_UNIT ( * ) SI_UNIT ( .MILLI., .METRE. ) );
#104350=CARTESIAN_POINT ( 'NONE',  ( 25.85216931545142316, 37.20485424854442158, 8.663044351978108182 ) ) ;
#104351=FACE_OUTER_BOUND ( 'NONE', #48852, .T. ) ;
#104358=CARTESIAN_POINT ( 'NONE',  ( -24.31874290140378747, 25.21043322494278627, 32.55344527691972445 ) ) ;
#104359=ORIENTED_EDGE ( 'NONE', *, *, #642, .F. ) ;
#104365=CARTESIAN_POINT ( 'NONE',  ( -0.1687456348417130103, 51.27204578583049255, -10.24141503192701919 ) ) ;
#104374=DIRECTION ( 'NONE',  ( -0.000000000000000000, 1.000000000000000000, -0.000000000000000000 ) ) ;
#104377=ORIENTED_EDGE ( 'NONE', *, *, #10751, .F. ) ;
#104450=CARTESIAN_POINT ( 'NONE',  ( 26.11182265785232559, 35.05542332294329810, 8.043516664989388332 ) ) ;
#104456=CARTESIAN_POINT ( 'NONE',  ( -0.7751162123649483204, 54.19727782468113730, -8.015928695369900936 ) ) ;
#104476=SURFACE_STYLE_USAGE ( .BOTH. , #102897 ) ;
#104490=CARTESIAN_POINT ( 'NONE',  ( 1.106418893442917994, 12.12096734116461150, -49.90218892958102259 ) ) ;
#104491=FILL_AREA_STYLE_COLOUR ( '', #18609 ) ;
#104508=CARTESIAN_POINT ( 'NONE',  ( -27.72867908628325040, 36.41173040130990302, 9.902678004857877525 ) ) ;
#104541=STYLED_ITEM ( 'NONE', ( #19680 ), #23944 ) ;
#104546=CARTESIAN_POINT ( 'NONE',  ( -49.09793955338193427, 7.820164633611648597, 16.25544133048934725 ) ) ;
#104551=CARTESIAN_POINT ( 'NONE',  ( -30.00229752355677704, 12.60065794652347471, 39.63915577993667938 ) ) ;
#104552=( LENGTH_UNIT ( ) NAMED_UNIT ( * ) SI_UNIT ( .MILLI., .METRE. ) );
#104561=CARTESIAN_POINT ( 'NONE',  ( -16.64348903516526335, 43.75610143575153899, -4.157797401561264650 ) ) ;
#104584=CARTESIAN_POINT ( 'NONE',  ( -8.239452746273963513, 54.07618835787194200, -1.562132243825230082 ) ) ;
#104607=CARTESIAN_POINT ( 'NONE',  ( 1.005716520562355942, 27.47520070304291551, -40.24667390188346161 ) ) ;
#104619=CARTESIAN_POINT ( 'NONE',  ( -30.82452621380396351, 13.29951192218421063, -41.36733700123911461 ) ) ;
#104630=CARTESIAN_POINT ( 'NONE',  ( 4.092977972706264289, 52.07635395608964757, -6.911964971445145878 ) ) ;
#104631=CARTESIAN_POINT ( 'NONE',  ( -0.08412175410183092561, 34.17188553058034728, 29.75000000000000000 ) ) ;
#104653=SURFACE_STYLE_FILL_AREA ( #80367 ) ;
#104683=PRESENTATION_STYLE_ASSIGNMENT (( #38908 ) ) ;
#104687=CARTESIAN_POINT ( 'NONE',  ( 38.32383406387373981, 25.24657036848469360, 13.20420819894402698 ) ) ;
#104708=ORIENTED_EDGE ( 'NONE', *, *, #19691, .T. ) ;
#104728=ADVANCED_FACE ( 'NONE', ( #42360 ), #34310, .F. ) ;
#104730=FILL_AREA_STYLE ('',( #106303 ) ) ;
#104756=CARTESIAN_POINT ( 'NONE',  ( -5.290067270632268226, 54.20842449845686417, -6.031152949374520844 ) ) ;
#104780=CARTESIAN_POINT ( 'NONE',  ( 1.249493494485172995, 43.73042964061625071, -17.18013998211830540 ) ) ;
#104782=CARTESIAN_POINT ( 'NONE',  ( -49.27079747525463915, 12.96457032161196210, -15.75812555157997075 ) ) ;
#104806=CARTESIAN_POINT ( 'NONE',  ( -37.56673239365849781, 25.47613764497371136, 13.45617127781066280 ) ) ;
#104810=ORIENTED_EDGE ( 'NONE', *, *, #16465, .T. ) ;
#104832=CARTESIAN_POINT ( 'NONE',  ( 1.637502573363885733E-19, 51.26930509877138320, -10.24999999999999822 ) ) ;
#104837=CARTESIAN_POINT ( 'NONE',  ( 4.331367822450267191, 52.16488944962013363, 6.474629951035481668 ) ) ;
#104841=CARTESIAN_POINT ( 'NONE',  ( 10.45210760954369711, 43.22598471715434698, 15.39953001771810648 ) ) ;
#104855=CARTESIAN_POINT ( 'NONE',  ( -6.276528120735480165, 53.84035791979297159, 6.497148600190744361 ) ) ;
#104872=EDGE_CURVE ( 'NONE', #95845, #13222, #45035, .T. ) ;
#104886=ORIENTED_EDGE ( 'NONE', *, *, #5200, .T. ) ;
#104895=CARTESIAN_POINT ( 'NONE',  ( -23.21751746555247919, 25.98869614573810694, 30.70617127781050471 ) ) ;
#104903=CARTESIAN_POINT ( 'NONE',  ( 0.3379698803298797349, 34.18408244316042044, 29.71496935741117085 ) ) ;
#104905=SURFACE_SIDE_STYLE ('',( #39114 ) ) ;
#104907=VECTOR ( 'NONE', #40468, 1000.000000000000000 ) ;
#104912=CARTESIAN_POINT ( 'NONE',  ( -23.84475511469840470, 25.80478802837803443, 30.86282763156348707 ) ) ;
#104917=CARTESIAN_POINT ( 'NONE',  ( -0.6468308027566224139, 43.23255578745401095, -18.58280467064760799 ) ) ;
#104918=SURFACE_STYLE_FILL_AREA ( #98398 ) ;
#104930=CARTESIAN_POINT ( 'NONE',  ( 47.90347347824236834, 10.05236241843094014, -16.85535821593550665 ) ) ;
#104949=AXIS2_PLACEMENT_3D ( 'NONE', #78913, #95122, #31839 ) ;
#104958=CARTESIAN_POINT ( 'NONE',  ( 46.79790428518975176, 18.85533329945889847, 15.37169442865920033 ) ) ;
#104981=CARTESIAN_POINT ( 'NONE',  ( 23.21751746555303342, 28.11705169068991594, 30.70617127781016720 ) ) ;
#104987=B_SPLINE_CURVE_WITH_KNOTS ( 'NONE', 3,
 ( #3880, #93954, #3346, #78810, #36810, #69673, #69156, #4940, #68076, #76689, #53489, #86414, #35749, #28718, #60538, #61600, #60015, #94495, #19040, #51877, #93424, #19578, #85326, #28189, #52406, #11412, #77230, #99093, #57043, #106122 ),
 .UNSPECIFIED., .F., .F.,
 ( 4, 2, 2, 2, 2, 2, 2, 2, 2, 2, 2, 2, 2, 2, 4 ),
 ( 0.0007661829082509325969, 0.0009991316538646626087, 0.001232080399478392404, 0.001697977890705861101, 0.002163875381933329581, 0.002629772873160798278, 0.003561567855615739575, 0.004493362838070681306, 0.005425157820525623037, 0.006356952802980563033, 0.006822850294208039103, 0.007288747785435514305, 0.007754645276662990375, 0.007987594022276733180, 0.008220542767890477720 ),
 .UNSPECIFIED. ) ;
#104994=CARTESIAN_POINT ( 'NONE',  ( 25.88305778034912308, 35.08525496124520515, 8.493710876074011651 ) ) ;
#105002=CARTESIAN_POINT ( 'NONE',  ( -1.097258412180344811, 54.05209286624712206, -8.380528997215506593 ) ) ;
#105008=SURFACE_STYLE_FILL_AREA ( #14914 ) ;
#105026=( LENGTH_UNIT ( ) NAMED_UNIT ( * ) SI_UNIT ( .MILLI., .METRE. ) );
#105052=EDGE_LOOP ( 'NONE', ( #75178, #10026 ) ) ;
#105089=EDGE_LOOP ( 'NONE', ( #70324, #71604, #69000, #99265, #2425, #68469, #75163 ) ) ;
#105098=CARTESIAN_POINT ( 'NONE',  ( 28.43946827300317892, 12.73388556380912817, 40.70676336658340944 ) ) ;
#105101=CARTESIAN_POINT ( 'NONE',  ( 29.68315524077034340, 18.29184282782460969, 39.60535821593451544 ) ) ;
#105106=CARTESIAN_POINT ( 'NONE',  ( -15.39658166598003319, 44.03750247749371738, -5.597717089993270889 ) ) ;
#105107=CARTESIAN_POINT ( 'NONE',  ( -28.35330149161957536, 36.33377328164552011, -8.699764177244842855 ) ) ;
#105130=CARTESIAN_POINT ( 'NONE',  ( -5.290067270632216712, 51.34639538792298907, 8.531152949374556371 ) ) ;
#105132=MECHANICAL_DESIGN_GEOMETRIC_PRESENTATION_REPRESENTATION('',(#41388),#50008);
#105186=( NAMED_UNIT ( * ) SI_UNIT ( $, .STERADIAN. ) SOLID_ANGLE_UNIT ( ) );
#105192=STYLED_ITEM ( 'NONE', ( #42984 ), #50038 ) ;
#105202=DIRECTION ( 'NONE',  ( 0.000000000000000000, 1.000000000000000000, 0.000000000000000000 ) ) ;
#105208=CIRCLE ( 'NONE', #84577, 22.55262289886175964 ) ;
#105215=CARTESIAN_POINT ( 'NONE',  ( 36.94626557873471029, 28.08634120636191511, 11.10896912859703711 ) ) ;
#105222=CARTESIAN_POINT ( 'NONE',  ( -28.58355031029979187, 11.06033896639473468, -41.46143022647145671 ) ) ;
#105227=CARTESIAN_POINT ( 'NONE',  ( 1.218775023799697266, 25.73288003004027757, 39.17967733385442131 ) ) ;
#105239=CARTESIAN_POINT ( 'NONE',  ( 24.23541427165741169, 25.18558254665225959, 32.70087860212819919 ) ) ;
#105244=EDGE_LOOP ( 'NONE', ( #1408, #73815 ) ) ;
#105247=ORIENTED_EDGE ( 'NONE', *, *, #47450, .T. ) ;
#105262=EDGE_LOOP ( 'NONE', ( #78594, #99055, #32462, #10476 ) ) ;
#105284=ORIENTED_EDGE ( 'NONE', *, *, #34477, .F. ) ;
#105291=CARTESIAN_POINT ( 'NONE',  ( -6.496475337783281567, 53.67452587285551857, -6.917066593337933611 ) ) ;
#105303=VECTOR ( 'NONE', #48496, 1000.000000000000000 ) ;
#105331=CARTESIAN_POINT ( 'NONE',  ( -23.05203244996622658, 28.15092755562140425, -30.71439907890194831 ) ) ;
#105344=CARTESIAN_POINT ( 'NONE',  ( -1.159778043035263995, 17.01122172421377599, -50.01806045519258959 ) ) ;
#105369=CARTESIAN_POINT ( 'NONE',  ( 11.10166199660593911, 43.72034362052824008, 13.20706475317513373 ) ) ;
#105423=CARTESIAN_POINT ( 'NONE',  ( 0.5682334480337650762, 34.21852722572099736, 29.61650315422764379 ) ) ;
#105425=( LENGTH_UNIT ( ) NAMED_UNIT ( * ) SI_UNIT ( .MILLI., .METRE. ) );
#105433=ORIENTED_EDGE ( 'NONE', *, *, #88842, .T. ) ;
#105435=ORIENTED_EDGE ( 'NONE', *, *, #46407, .F. ) ;
#105437=CARTESIAN_POINT ( 'NONE',  ( 5.581309233574441675E-23, 43.17555810750860701, -18.75000000000000355 ) ) ;
#105460=ORIENTED_EDGE ( 'NONE', *, *, #30526, .F. ) ;
#105476=EDGE_CURVE ( 'NONE', #91423, #41373, #101934, .T. ) ;
#105503=B_SPLINE_CURVE_WITH_KNOTS ( 'NONE', 3,
 ( #52063, #37527, #11597, #2448, #102218, #27850, #93066, #28915, #19233, #84978, #28366, #86597, #101155, #70391, #60719, #77947, #4061, #20832, #61244, #3531, #2983, #76871, #76335, #77414 ),
 .UNSPECIFIED., .F., .F.,
 ( 4, 2, 2, 2, 2, 2, 2, 2, 2, 2, 2, 4 ),
 ( 0.002986045904103195626, 0.003488698368484360358, 0.003740024600674948796, 0.003991350832865537233, 0.004242677065056125671, 0.004494003297246713241, 0.004996655761627886647, 0.005499308226009059185, 0.005750634458199645888, 0.006001960690390231723, 0.006504613154771410333, 0.007007265619152588075 ),
 .UNSPECIFIED. ) ;
#105516=( GEOMETRIC_REPRESENTATION_CONTEXT ( 3 ) GLOBAL_UNCERTAINTY_ASSIGNED_CONTEXT ( ( #18373 ) ) GLOBAL_UNIT_ASSIGNED_CONTEXT ( ( #3066, #60794, #44066 ) ) REPRESENTATION_CONTEXT ( 'NONE', 'WORKASPACE' ) );
#105524=CARTESIAN_POINT ( 'NONE',  ( -1.221393050841994787, 53.71071939966033426, -9.310417747113787001 ) ) ;
#105546=CARTESIAN_POINT ( 'NONE',  ( 0.3378009397522571122, 26.06497163046132926, -38.28498976926001518 ) ) ;
#105552=CARTESIAN_POINT ( 'NONE',  ( -0.6415681314778590716, 35.01575306882282490, -27.42406975498120403 ) ) ;
#105557=SURFACE_SIDE_STYLE ('',( #79158 ) ) ;
#105573=CARTESIAN_POINT ( 'NONE',  ( 23.05087275028312277, 25.28743397255878023, 33.20617127781017786 ) ) ;
#105575=FACE_OUTER_BOUND ( 'NONE', #61925, .T. ) ;
#105594=CARTESIAN_POINT ( 'NONE',  ( 8.399149604396622948, 53.73754273787561431, -4.031152949375367278 ) ) ;
#105595=UNCERTAINTY_MEASURE_WITH_UNIT (LENGTH_MEASURE( 1.000000000000000082E-05 ), #11210, 'distance_accuracy_value', 'NONE');
#105612=CARTESIAN_POINT ( 'NONE',  ( 28.43259016867768452, 12.18852863928164076, 40.99039043055278597 ) ) ;
#105623=( NAMED_UNIT ( * ) PLANE_ANGLE_UNIT ( ) SI_UNIT ( $, .RADIAN. ) );
#105646=CARTESIAN_POINT ( 'NONE',  ( -46.79755470960070340, 13.68519846643612503, 15.37381431200659243 ) ) ;
#105648=EDGE_LOOP ( 'NONE', ( #64604, #49752, #92350, #28035 ) ) ;
#105656=CYLINDRICAL_SURFACE ( 'NONE', #10491, 1.250000000000001110 ) ;
#105672=EDGE_LOOP ( 'NONE', ( #19847, #81013, #35953, #28781, #92314, #101961, #12396, #91759 ) ) ;
#105677=CARTESIAN_POINT ( 'NONE',  ( -17.53729400407423000, 34.16830424740683725, -24.04411209734885801 ) ) ;
#105679=CARTESIAN_POINT ( 'NONE',  ( 49.10072971674808429, 12.98664841672423798, 16.25083509556763417 ) ) ;
#105693=CARTESIAN_POINT ( 'NONE',  ( 36.95381392810918442, 27.83278920306690551, -13.30708169601276403 ) ) ;
#105697=CARTESIAN_POINT ( 'NONE',  ( 27.10511071441176156, 34.47735702144343861, -10.05698433968637673 ) ) ;
#105702=FILL_AREA_STYLE_COLOUR ( '', #77331 ) ;
#105703=CARTESIAN_POINT ( 'NONE',  ( 21.96569361886355765, 28.02808497942503507, 31.91099187246623714 ) ) ;
#105710=CARTESIAN_POINT ( 'NONE',  ( -15.61321260267626521, 35.02176863298834064, 22.53469681359418075 ) ) ;
#105727=LINE ( 'NONE', #7554, #104907 ) ;
#105729=CARTESIAN_POINT ( 'NONE',  ( 36.34528775465977901, 28.20980455253403463, 11.89180145376659326 ) ) ;
#105733=CARTESIAN_POINT ( 'NONE',  ( 25.86069633001730139, 35.07357202603378710, -8.661875674703953365 ) ) ;
#105735=CYLINDRICAL_SURFACE ( 'NONE', #85047, 1.249999999999999334 ) ;
#105743=AXIS2_PLACEMENT_3D ( 'NONE', #54499, #22188, #79854 ) ;
#105747=CARTESIAN_POINT ( 'NONE',  ( 4.684274960302871098E-15, 26.07813853931757464, 38.25000000000000000 ) ) ;
#105752=CARTESIAN_POINT ( 'NONE',  ( -16.75187969033554936, -1.200000000000000030E-05, -23.05698433968595751 ) ) ;
#105761=CYLINDRICAL_SURFACE ( 'NONE', #67057, 13.27631144943088515 ) ;
#105770=CARTESIAN_POINT ( 'NONE',  ( 29.50962187807837012, 13.72866526111394947, -42.09567151085946790 ) ) ;
#105781=( NAMED_UNIT ( * ) PLANE_ANGLE_UNIT ( ) SI_UNIT ( $, .RADIAN. ) );
#105784=CARTESIAN_POINT ( 'NONE',  ( -16.75187969033554936, 37.11970326878314097, -21.80698433968595751 ) ) ;
#105787=CARTESIAN_POINT ( 'NONE',  ( 0.000000000000000000, 38.67090180175566871, 0.000000000000000000 ) ) ;
#105788=( LENGTH_UNIT ( ) NAMED_UNIT ( * ) SI_UNIT ( .MILLI., .METRE. ) );
#105790=CARTESIAN_POINT ( 'NONE',  ( 0.000000000000000000, 0.000000000000000000, 0.000000000000000000 ) ) ;
#105795=ORIENTED_EDGE ( 'NONE', *, *, #74405, .T. ) ;
#105798=EDGE_LOOP ( 'NONE', ( #68668, #92163 ) ) ;
#105873=CARTESIAN_POINT ( 'NONE',  ( 48.28140683493008822, 14.38570471689693875, -16.83761797438825525 ) ) ;
#105894=CARTESIAN_POINT ( 'NONE',  ( -9.761574416223039563, 51.33888487989963778, -2.428418878555363314 ) ) ;
#105895=CARTESIAN_POINT ( 'NONE',  ( -6.536939020983855819, 53.59930666568121183, 7.161232122323571758 ) ) ;
#105902=ORIENTED_EDGE ( 'NONE', *, *, #37660, .T. ) ;
#105911=CARTESIAN_POINT ( 'NONE',  ( 27.42311158548955419, 36.77212537659387692, -7.587845593855179871 ) ) ;
#105923=COLOUR_RGB ( '', 0.72549020, 0.75294118, 0.79215686) ;
#105931=CARTESIAN_POINT ( 'NONE',  ( 15.66273129163408484, 43.86900239055839990, 6.199110369967553602 ) ) ;
#105939=CARTESIAN_POINT ( 'NONE',  ( -17.62344211657769577, 45.49768958935467822, -4.615364168318502713 ) ) ;
#105945=CARTESIAN_POINT ( 'NONE',  ( 24.43733964430219530, 27.40365649514079038, -32.24112188980117111 ) ) ;
#105948=ORIENTED_EDGE ( 'NONE', *, *, #106341, .T. ) ;
#105954=CARTESIAN_POINT ( 'NONE',  ( 0.7768295077518341252, 46.10996703314370393, 16.51725890612300418 ) ) ;
#105962=CARTESIAN_POINT ( 'NONE',  ( 47.07197767030555724, 13.48831169381993256, -14.79015211622768788 ) ) ;
#105974=CARTESIAN_POINT ( 'NONE',  ( 30.64306277920978516, 7.829637822906585498, 41.65859565436451817 ) ) ;
#105989=CARTESIAN_POINT ( 'NONE',  ( 47.18437091044133069, 18.47854193719496152, 14.68206053360883878 ) ) ;
#106002=ORIENTED_EDGE ( 'NONE', *, *, #91724, .T. ) ;
#106012=CARTESIAN_POINT ( 'NONE',  ( -9.806140579452332418, 53.43725138183724255, 2.590315439319800461 ) ) ;
#106018=CARTESIAN_POINT ( 'NONE',  ( 6.517579295440401488, 53.49311649283862380, 7.569470789138253330 ) ) ;
#106031=CARTESIAN_POINT ( 'NONE',  ( -29.87444201908918728, 8.057352084660356795, -42.09618695302987845 ) ) ;
#106042=( LENGTH_UNIT ( ) NAMED_UNIT ( * ) SI_UNIT ( .MILLI., .METRE. ) );
#106063=CARTESIAN_POINT ( 'NONE',  ( 1.249203303865451753, 53.88099106177547526, -8.834200927035483986 ) ) ;
#106066=CARTESIAN_POINT ( 'NONE',  ( 2.985641311035224431E-22, 35.08181111624585213, -27.25000000000000000 ) ) ;
#106068=VERTEX_POINT ( 'NONE', #82036 ) ;
#106075=VERTEX_POINT ( 'NONE', #88560 ) ;
#106105=CARTESIAN_POINT ( 'NONE',  ( -27.71720361241088426, 34.52917361415862985, -7.705544253522235820 ) ) ;
#106116=EDGE_CURVE ( 'NONE', #34913, #45114, #31930, .T. ) ;
#106122=CARTESIAN_POINT ( 'NONE',  ( 2.470381878726035567E-14, 18.87382441218300144, 49.24999999999992184 ) ) ;
#106130=ADVANCED_FACE ( 'NONE', ( #6555 ), #90683, .T. ) ;
#106131=CARTESIAN_POINT ( 'NONE',  ( 28.54518584606585563, 18.48129625438336276, 40.33591358207591071 ) ) ;
#106164=SURFACE_STYLE_USAGE ( .BOTH. , #57611 ) ;
#106165=CARTESIAN_POINT ( 'NONE',  ( -47.36504548439823736, 12.99580092579919999, 14.54285468146515470 ) ) ;
#106174=EDGE_CURVE ( 'NONE', #29960, #90588, #42119, .T. ) ;
#106202=CARTESIAN_POINT ( 'NONE',  ( -28.98676785243937815, 9.652684557211548722, 41.90074509620628618 ) ) ;
#106210=CARTESIAN_POINT ( 'NONE',  ( 37.56673239365841255, 27.88554838446202311, -10.95617127781092037 ) ) ;
#106217=CARTESIAN_POINT ( 'NONE',  ( -37.48682946491119594, 25.78511199397625830, -10.95617127781024180 ) ) ;
#106222=CARTESIAN_POINT ( 'NONE',  ( 21.97121321732691257, 28.05118154993452961, 31.83013537814891691 ) ) ;
#106242=FACE_OUTER_BOUND ( 'NONE', #2302, .T. ) ;
#106244=B_SPLINE_CURVE_WITH_KNOTS ( 'NONE', 3,
 ( #26703, #18056, #84373, #83297, #34790, #51986, #43382, #34254, #101077, #66587, #50914, #35318, #26179, #18598, #99467, #57946, #27237, #98930, #83824, #68182, #43906, #100539 ),
 .UNSPECIFIED., .F., .F.,
 ( 4, 2, 2, 2, 2, 2, 2, 2, 2, 2, 4 ),
 ( 0.003049572450201245167, 0.003553926186014261940, 0.003806103053920776615, 0.004058279921827292157, 0.004562633657640314568, 0.005066987393453339580, 0.005571341129266364593, 0.006075694865079388739, 0.006580048600892413752, 0.006832225468798924090, 0.007084402336705432693 ),
 .UNSPECIFIED. ) ;
#106246=ORIENTED_EDGE ( 'NONE', *, *, #76130, .F. ) ;
#106254=CARTESIAN_POINT ( 'NONE',  ( 26.94627380994484156, 34.81398319875323466, -7.556984339686200869 ) ) ;
#106266=CARTESIAN_POINT ( 'NONE',  ( -29.68315524077005207, 18.29184282782459547, -39.60535821593474282 ) ) ;
#106272=CARTESIAN_POINT ( 'NONE',  ( 24.41529588775463111, 25.25633621354825564, 32.32316270052714913 ) ) ;
#106285=B_SPLINE_CURVE_WITH_KNOTS ( 'NONE', 3,
 ( #101548, #28228, #3919, #10916, #36852, #85365, #93986, #3385, #86456, #102069, #20148, #43834, #61648, #68110, #11454, #94539, #61099, #101009, #53000, #44379, #85920, #11992 ),
 .UNSPECIFIED., .F., .F.,
 ( 4, 2, 2, 2, 2, 2, 2, 2, 2, 2, 4 ),
 ( 0.003083058008555213027, 0.003587558145623166543, 0.003839808214157141783, 0.004092058282691117023, 0.004596558419759062299, 0.004848808488293035804, 0.005101058556827008442, 0.006110058830962918075, 0.006614558968030872024, 0.006866809036564852468, 0.007119059105098832912 ),
 .UNSPECIFIED. ) ;
#106286=COLOUR_RGB ( '', 0.31764706, 0.68627451, 0.89019608) ;
#106289=VECTOR ( 'NONE', #92824, 1000.000000000000000 ) ;
#106303=FILL_AREA_STYLE_COLOUR ( '', #84040 ) ;
#106328=EDGE_CURVE ( 'NONE', #56342, #95728, #5443, .T. ) ;
#106338=AXIS2_PLACEMENT_3D ( 'NONE', #14031, #63143, #39404 ) ;
#106341=EDGE_CURVE ( 'NONE', #5362, #36063, #45950, .T. ) ;
#106351=FACE_BOUND ( 'NONE', #102015, .T. ) ;
#106353=CARTESIAN_POINT ( 'NONE',  ( 1.130678585943547532, 43.42148124859406977, -18.03896404153940125 ) ) ;
#106406=CARTESIAN_POINT ( 'NONE',  ( 48.76867190053936696, 8.289666503167284262, 16.61714170247970657 ) ) ;
#106414=ORIENTED_EDGE ( 'NONE', *, *, #82009, .T. ) ;
#106420=CARTESIAN_POINT ( 'NONE',  ( -9.812526520939238495, 51.27367565803530169, -2.925190231983776368 ) ) ;
#106456=CARTESIAN_POINT ( 'NONE',  ( 27.42411589273523731, 34.37229030169084609, 10.02668682424727287 ) ) ;
#106468=CARTESIAN_POINT ( 'NONE',  ( 0.000000000000000000, 45.89575828009193259, 0.000000000000000000 ) ) ;
#106479=CARTESIAN_POINT ( 'NONE',  ( 0.1702502393396320146, 51.26930509877140452, 10.25000000000000178 ) ) ;
#106480=DIRECTION ( 'NONE',  ( -0.000000000000000000, 1.000000000000000000, 0.000000000000000000 ) ) ;
#106485=CARTESIAN_POINT ( 'NONE',  ( 0.8390624637001048436, 46.08972068689292456, 16.56986929762893013 ) ) ;
#106500=CARTESIAN_POINT ( 'NONE',  ( 0.7761051413992605674, 54.19697142896034592, 8.016680439112649381 ) ) ;
#106502=SURFACE_STYLE_FILL_AREA ( #48262 ) ;
#106509=CARTESIAN_POINT ( 'NONE',  ( -9.522512062097407082, 43.48390578715350330, 15.16028251901261648 ) ) ;
#106511=EDGE_CURVE ( 'NONE', #45114, #38179, #25554, .T. ) ;
#106516=DIRECTION ( 'NONE',  ( 0.000000000000000000, 0.000000000000000000, -1.000000000000000000 ) ) ;
#106526=STYLED_ITEM ( 'NONE', ( #88831 ), #27291 ) ;
#106559=CARTESIAN_POINT ( 'NONE',  ( 6.497272336416993532, 53.67373393826039774, 6.919306612608417062 ) ) ;
#106568=CARTESIAN_POINT ( 'NONE',  ( -8.398963767913890877, 53.73760393018520887, 4.031152949374985361 ) ) ;
#106570=CARTESIAN_POINT ( 'NONE',  ( 26.94447279565465792, 34.53217287173363559, 10.05698433968570527 ) ) ;
#106571=COLOUR_RGB ( '', 0.72549020, 0.75294118, 0.79215686) ;
#106590=UNCERTAINTY_MEASURE_WITH_UNIT (LENGTH_MEASURE( 1.000000000000000082E-05 ), #18472, 'distance_accuracy_value', 'NONE');
#106596=CARTESIAN_POINT ( 'NONE',  ( 9.508921847869231669, 46.21454289499525458, 13.17524946764673643 ) ) ;
#106609=CARTESIAN_POINT ( 'NONE',  ( -0.5677851517752953159, 35.03120528833704128, -27.38325881563803676 ) ) ;
#106623=CARTESIAN_POINT ( 'NONE',  ( 24.41576965198462190, 25.25667818450425273, -32.32162735095537442 ) ) ;
#106642=CARTESIAN_POINT ( 'NONE',  ( 1.380949872273418154E-15, 45.89575828009193259, 11.27631144943088337 ) ) ;
#106681=CARTESIAN_POINT ( 'NONE',  ( -28.46824965450743150, 18.16842165451065227, 40.55076743663460093 ) ) ;
#106684=CARTESIAN_POINT ( 'NONE',  ( -21.96339186788464204, 25.92483237897061699, 31.82890721654192845 ) ) ;
#106695=VECTOR ( 'NONE', #67820, 1000.000000000000000 ) ;
#106707=CARTESIAN_POINT ( 'NONE',  ( -47.29368197624727088, 13.12573487771091152, 14.58950938768687777 ) ) ;
#106718=CARTESIAN_POINT ( 'NONE',  ( 15.64519568958359308, 46.18931709473498159, -4.637408661950145117 ) ) ;
#106723=CARTESIAN_POINT ( 'NONE',  ( -29.99961410214337576, 17.76511157208308234, 39.64372791628625947 ) ) ;
#106725=CARTESIAN_POINT ( 'NONE',  ( 1.093227907231550722, 27.52357886411307319, -40.11142487546388935 ) ) ;
#106738=CARTESIAN_POINT ( 'NONE',  ( -16.64348903516517098, 43.75610143575153899, 4.157797401561652784 ) ) ;
#106746=CARTESIAN_POINT ( 'NONE',  ( -29.68315524076956180, 8.302504244945341227, 42.10535821593508388 ) ) ;
#106748=EDGE_CURVE ( 'NONE', #78599, #31379, #73054, .T. ) ;
#106754=CARTESIAN_POINT ( 'NONE',  ( 37.24671046105844852, 27.99421627048664973, -10.98692623331827356 ) ) ;
#106764=CARTESIAN_POINT ( 'NONE',  ( 22.89193641261745427, 27.46073252125953701, 33.16577871831020730 ) ) ;
#106776=CARTESIAN_POINT ( 'NONE',  ( -4.329583349659062996, 54.29296960176466058, 6.476735382064108926 ) ) ;
ENDSEC;
END-ISO-10303-21;
